ISO-10303-21;
HEADER;
FILE_DESCRIPTION (('STEP AP214'),
    '1' );
FILE_NAME ('straight miter gear_iso_ISO - Straight miter gear 1.5M20T 20PA 2FW ---20O10H16.576MD10.0S1.step',
    '2026-09-24T10:15:42',
    ( '' ),
    ( '' ),
    'SwSTEP 2.0',
    'SolidWorks 2026',
    '' );
FILE_SCHEMA (( 'AUTOMOTIVE_DESIGN' ));
ENDSEC;

DATA;
#15=CARTESIAN_POINT ( 'NONE',  ( 0.3137051932979775248, -0.4596302728638797519, -13.73004976592202553 ) ) ;
#20=ADVANCED_FACE ( 'NONE', ( #6722 ), #7157, .F. ) ;
#21=DIRECTION ( 'NONE',  ( -1.000000000000000000, -0.000000000000000000, -0.000000000000000000 ) ) ;
#22=CARTESIAN_POINT ( 'NONE',  ( 0.3137051932979775248, 10.83767969834815581, -8.442169467526731808 ) ) ;
#32=AXIS2_PLACEMENT_3D ( 'NONE', #18894, #175, #17469 ) ;
#33=CARTESIAN_POINT ( 'NONE',  ( 16.57210152137263393, 0.01136813053532075186, 0.009075239946108242667 ) ) ;
#34=ORIENTED_EDGE ( 'NONE', *, *, #3133, .F. ) ;
#48=ADVANCED_FACE ( 'NONE', ( #881 ), #6440, .F. ) ;
#50=CARTESIAN_POINT ( 'NONE',  ( 16.58200780006414732, 0.01080144354108870768, 0.002844973367391462511 ) ) ;
#51=CARTESIAN_POINT ( 'NONE',  ( 2.123976203522053297, -14.31368049382965069, -6.261444813538707521 ) ) ;
#58=EDGE_LOOP ( 'NONE', ( #12912, #14842, #3064, #3403, #10811, #3564 ) ) ;
#61=CARTESIAN_POINT ( 'NONE',  ( 1.846138399168762989, -3.446241763653083101, 11.95493567637849530 ) ) ;
#62=( BOUNDED_SURFACE ( )  B_SPLINE_SURFACE ( 3, 1, ( 
 ( #17504, #8616 ),
 ( #15879, #10145 ),
 ( #4407, #16068 ),
 ( #12913, #2960 ) ),
 .UNSPECIFIED., .F., .F., .T. ) 
 B_SPLINE_SURFACE_WITH_KNOTS ( ( 4, 4 ),
 ( 2, 2 ),
 ( 0.000000000000000000, 1.000000000000000000 ),
 ( 0.000000000000000000, 1.000000000000000000 ),
 .UNSPECIFIED. ) 
 GEOMETRIC_REPRESENTATION_ITEM ( )  RATIONAL_B_SPLINE_SURFACE ( (
 ( 1.000000000000000000, 1.000000000000000000),
 ( 0.9933953342250436691, 0.8357391271907733676),
 ( 0.9933953342250436691, 0.8357391271907733676),
 ( 1.000000000000000000, 1.000000000000000000) ) ) 
 REPRESENTATION_ITEM ( '' )  SURFACE ( )  );
#63=CARTESIAN_POINT ( 'NONE',  ( 0.3151926232592472954, 8.013596737356548871, -11.16039997398644879 ) ) ;
#64=ORIENTED_EDGE ( 'NONE', *, *, #16293, .T. ) ;
#70=DIRECTION ( 'NONE',  ( 0.000000000000000000, 0.000000000000000000, 1.000000000000000000 ) ) ;
#73=CARTESIAN_POINT ( 'NONE',  ( 1.861628059977118888, 9.751736252960505169, 7.751680370224894645 ) ) ;
#75=CARTESIAN_POINT ( 'NONE',  ( 0.3151928476913571364, -11.11539186930580669, -8.075547435847068911 ) ) ;
#76=ADVANCED_FACE ( 'NONE', ( #2979 ), #15573, .F. ) ;
#77=CARTESIAN_POINT ( 'NONE',  ( 3.950837973638676281, -6.316429227969562632, 13.10350451991838128 ) ) ;
#78=VERTEX_POINT ( 'NONE', #4250 ) ;
#80=ORIENTED_EDGE ( 'NONE', *, *, #5514, .F. ) ;
#83=B_SPLINE_CURVE_WITH_KNOTS ( 'NONE', 3,
 ( #3719, #12422, #3534, #6414 ),
 .UNSPECIFIED., .F., .F.,
 ( 4, 4 ),
 ( 2.117499858742978245E-17, 0.003005512676784849197 ),
 .UNSPECIFIED. ) ;
#84=CARTESIAN_POINT ( 'NONE',  ( 16.56753206892534891, -0.008432171035096417550, 0.004368917149005425125 ) ) ;
#88=B_SPLINE_CURVE_WITH_KNOTS ( 'NONE', 3,
 ( #11199, #9477, #2212, #17107 ),
 .UNSPECIFIED., .F., .F.,
 ( 4, 4 ),
 ( 2.006682199098010609E-17, 0.003005512676784850064 ),
 .UNSPECIFIED. ) ;
#90=DIRECTION ( 'NONE',  ( 0.000000000000000000, 0.000000000000000000, 1.000000000000000000 ) ) ;
#96=CARTESIAN_POINT ( 'NONE',  ( 3.664313757352972711, 10.50730552161232545, 9.645155442698788661 ) ) ;
#99=CARTESIAN_POINT ( 'NONE',  ( 0.3142011359265332593, 13.17934269988458063, 3.879426116491735854 ) ) ;
#103=CARTESIAN_POINT ( 'NONE',  ( 0.000000000000000000, 0.000000000000000000, 0.000000000000000000 ) ) ;
#104=CARTESIAN_POINT ( 'NONE',  ( 0.3151928479966097374, 6.943324946344315912E-05, 13.73922861026898623 ) ) ;
#106=CARTESIAN_POINT ( 'NONE',  ( 0.3170788640506441158, -0.1533108587035203196, -13.74111462631963576 ) ) ;
#119=VECTOR ( 'NONE', #9633, 1000.000000000000114 ) ;
#122=FACE_OUTER_BOUND ( 'NONE', #1733, .T. ) ;
#123=CARTESIAN_POINT ( 'NONE',  ( 0.4754618798421171855, 0.7484603771384397142, 13.89949764182683012 ) ) ;
#126=CARTESIAN_POINT ( 'NONE',  ( 1.846138399168762989, 4.238866729160403857, 11.69739621335923729 ) ) ;
#127=CARTESIAN_POINT ( 'NONE',  ( 0.3095370825347224519, -13.20347358821917183, 3.806662003783363613 ) ) ;
#135=ORIENTED_EDGE ( 'NONE', *, *, #17163, .F. ) ;
#139=CARTESIAN_POINT ( 'NONE',  ( 1.847372867223025406, -7.398914411685061587, 10.00438561114521185 ) ) ;
#141=CARTESIAN_POINT ( 'NONE',  ( 0.3150686449036039227, -7.951193823202478583, 11.20479228691394979 ) ) ;
#142=CARTESIAN_POINT ( 'NONE',  ( 3.377929128793398128, -5.536064832134078628, -12.84367544717941456 ) ) ;
#143=EDGE_CURVE ( 'NONE', #9064, #209, #1127, .T. ) ;
#147=CARTESIAN_POINT ( 'NONE',  ( 16.57210152137263393, 0.003862718596009277316, 0.01402404281922923004 ) ) ;
#148=CARTESIAN_POINT ( 'NONE',  ( 16.57605080000000086, 6.123233995736766282E-16, -5.000000000000000000 ) ) ;
#149=CARTESIAN_POINT ( 'NONE',  ( 16.56872352241294521, -0.001442253899401880124, -0.01033355228142401362 ) ) ;
#154=CARTESIAN_POINT ( 'NONE',  ( 16.56753206892534891, -0.004368917149005395635, -0.008432171035096433162 ) ) ;
#159=CARTESIAN_POINT ( 'NONE',  ( 1.918921323896323639, -9.738309537478938793, -7.860085869556288962 ) ) ;
#169=CARTESIAN_POINT ( 'NONE',  ( 1.846138399168762989, -3.446241763653083101, 11.95493567637849530 ) ) ;
#174=CARTESIAN_POINT ( 'NONE',  ( 8.438534575730034959, -6.862570336891077538, 0.2320579683289888395 ) ) ;
#175=DIRECTION ( 'NONE',  ( -1.000000000000000000, -0.000000000000000000, -0.000000000000000000 ) ) ;
#188=CARTESIAN_POINT ( 'NONE',  ( 0.3939822652208130327, -0.7002900021918908591, 13.80035637018651862 ) ) ;
#191=CARTESIAN_POINT ( 'NONE',  ( 16.56872352241294521, 0.01033355228142401709, -0.001442253899401843694 ) ) ;
#192=EDGE_CURVE ( 'NONE', #9203, #9252, #8222, .T. ) ;
#199=CARTESIAN_POINT ( 'NONE',  ( 1.847412631396504690, 0.04315047898452520347, -12.44294644888238643 ) ) ;
#200=EDGE_LOOP ( 'NONE', ( #4581, #15227, #12383, #13491 ) ) ;
#206=PRODUCT ( 'straight miter gear_iso_ISO - Straight miter gear 1.5M20T 20PA 2FW ---20O10H16.576MD10.0S1', 'straight miter gear_iso_ISO - Straight miter gear 1.5M20T 20PA 2FW ---20O10H16.576MD10.0S1', '', ( #2153 ) ) ;
#209=VERTEX_POINT ( 'NONE', #11985 ) ;
#210=CARTESIAN_POINT ( 'NONE',  ( 1.847168016377985333, 3.666915430942765397, -11.89018175117590559 ) ) ;
#213=DIRECTION ( 'NONE',  ( 0.7561779333270775005, 0.1688126975276512953, 0.6322161072786960379 ) ) ;
#219=CARTESIAN_POINT ( 'NONE',  ( 3.950837973638675393, -2.591948120961912849, 14.31366178983252446 ) ) ;
#220=VECTOR ( 'NONE', #13485, 1000.000000000000000 ) ;
#225=CARTESIAN_POINT ( 'NONE',  ( 3.353306896162455697, -7.069984850384722463, -12.02594772223104869 ) ) ;
#228=CARTESIAN_POINT ( 'NONE',  ( 2.636624412716062960, 2.862162146982868194, -15.80357026013419564 ) ) ;
#234=ORIENTED_EDGE ( 'NONE', *, *, #6422, .T. ) ;
#240=CARTESIAN_POINT ( 'NONE',  ( 0.3137051932979809665, -13.20008686438108647, 3.805684345189735307 ) ) ;
#242=CARTESIAN_POINT ( 'NONE',  ( 0.3148208552358926493, -7.888357771040781508, 11.24855514421872726 ) ) ;
#248=CARTESIAN_POINT ( 'NONE',  ( 2.747332970342022840, 14.49942876448592521, 7.555624153089699924 ) ) ;
#251=CARTESIAN_POINT ( 'NONE',  ( 1.846822687350021974, -11.74004266906801774, -4.121816957446323038 ) ) ;
#252=CARTESIAN_POINT ( 'NONE',  ( 0.3058872367615226295, -0.6080468242581913429, 13.72992299905059888 ) ) ;
#257=VERTEX_POINT ( 'NONE', #4999 ) ;
#258=CARTESIAN_POINT ( 'NONE',  ( 0.3150692679895937820, -7.951395415075003470, -11.20465057551034604 ) ) ;
#263=LINE ( 'NONE', #16517, #9897 ) ;
#264=CARTESIAN_POINT ( 'NONE',  ( 2.002547531651519996, -12.57989064830760206, 0.6781519942171299054 ) ) ;
#265=CARTESIAN_POINT ( 'NONE',  ( 2.636624412714236865, 15.91454522070173638, 2.161493821596668585 ) ) ;
#267=CARTESIAN_POINT ( 'NONE',  ( 0.3150692679895976678, 7.951395415075086959, 11.20465057551027854 ) ) ;
#269=EDGE_CURVE ( 'NONE', #14945, #13773, #1572, .T. ) ;
#272=EDGE_CURVE ( 'NONE', #10403, #8116, #15037, .T. ) ;
#273=CARTESIAN_POINT ( 'NONE',  ( 0.3137051932979757485, -11.37800749014125223, -7.698472063774596030 ) ) ;
#277=B_SPLINE_CURVE_WITH_KNOTS ( 'NONE', 3,
 ( #7928, #18045, #12482, #13739, #10974, #15075 ),
 .UNSPECIFIED., .F., .F.,
 ( 4, 2, 4 ),
 ( 0.000000000000000000, 0.001656992708823638600, 0.003313985417647277200 ),
 .UNSPECIFIED. ) ;
#281=CARTESIAN_POINT ( 'NONE',  ( 8.522092701127531811, -3.777034505568564349, 5.841710761610117153 ) ) ;
#286=CARTESIAN_POINT ( 'NONE',  ( 2.353870697619109720, 0.7635393531608140050, -12.92712089195301850 ) ) ;
#287=VERTEX_POINT ( 'NONE', #9120 ) ;
#288=CARTESIAN_POINT ( 'NONE',  ( 1.846524061778020531, -4.180439405448407975, 11.71897913237548039 ) ) ;
#293=CARTESIAN_POINT ( 'NONE',  ( 0.3150692679895996107, 13.01874238516610482, 4.391039771493711719 ) ) ;
#295=CARTESIAN_POINT ( 'NONE',  ( 16.56679352167444819, -0.008311568981097361419, 0.004162264567719621902 ) ) ;
#296=ORIENTED_EDGE ( 'NONE', *, *, #12237, .T. ) ;
#302=CARTESIAN_POINT ( 'NONE',  ( 1.846822687350021974, 0.2922081769261886675, -12.43915556955403190 ) ) ;
#303=ORIENTED_EDGE ( 'NONE', *, *, #12780, .T. ) ;
#304=CARTESIAN_POINT ( 'NONE',  ( 0.3132635586635995617, 11.41586812343490109, 7.641727604903931770 ) ) ;
#307=CARTESIAN_POINT ( 'NONE',  ( 0.3170788640506441158, -13.11595226728154984, -4.100430649998100030 ) ) ;
#310=CARTESIAN_POINT ( 'NONE',  ( 1.847372867223028070, 3.945260592619209028, -11.80112642014550239 ) ) ;
#311=CARTESIAN_POINT ( 'NONE',  ( 2.705023505549866147, 7.115606223895331262, -11.23800170568049062 ) ) ;
#318=EDGE_CURVE ( 'NONE', #7741, #3683, #17074, .T. ) ;
#319=CARTESIAN_POINT ( 'NONE',  ( 16.56872352241294521, -0.004907101719994693724, 0.009207754980063731845 ) ) ;
#328=CARTESIAN_POINT ( 'NONE',  ( 0.3145734862173242830, 11.29227530924457312, -7.825584895511399353 ) ) ;
#330=CARTESIAN_POINT ( 'NONE',  ( 3.950837973638675393, -2.591948120961706792, -14.31366178983255466 ) ) ;
#332=EDGE_CURVE ( 'NONE', #287, #17311, #2486, .T. ) ;
#333=DIRECTION ( 'NONE',  ( 0.7635533937278216055, -0.02138673900302784023, 0.6453904417649385383 ) ) ;
#334=B_SPLINE_CURVE_WITH_KNOTS ( 'NONE', 3,
 ( #18083, #7965, #13393, #210, #17897, #6043, #10532, #310, #6231, #6139, #10434, #16270, #11965 ),
 .UNSPECIFIED., .F., .F.,
 ( 4, 3, 3, 3, 4 ),
 ( 1.734723475976806902E-18, 0.0002299804304191479859, 0.0004599608082120235455, 0.0006467586077647999570, 0.0008336169836825983986 ),
 .UNSPECIFIED. ) ;
#340=CARTESIAN_POINT ( 'NONE',  ( 1.846955891736119737, 0.2634721419535199782, 12.44001089941741256 ) ) ;
#342=CARTESIAN_POINT ( 'NONE',  ( 0.4754618798421171855, 5.007009103465246191, 12.98792082933646519 ) ) ;
#343=FACE_OUTER_BOUND ( 'NONE', #18576, .T. ) ;
#348=VERTEX_POINT ( 'NONE', #6727 ) ;
#353=CARTESIAN_POINT ( 'NONE',  ( 0.3720661004400040439, 10.73619472937714825, -8.694226082900476271 ) ) ;
#356=CARTESIAN_POINT ( 'NONE',  ( 0.4862570985993235340, -11.67702470553359539, -7.559321496869553236 ) ) ;
#361=FACE_OUTER_BOUND ( 'NONE', #4335, .T. ) ;
#362=CARTESIAN_POINT ( 'NONE',  ( 1.846138399168762101, 11.69739621335927815, -4.238866729160283064 ) ) ;
#366=CARTESIAN_POINT ( 'NONE',  ( 0.3148208552358935930, 4.026279359288611026, -13.13564827777585187 ) ) ;
#373=EDGE_CURVE ( 'NONE', #3822, #11376, #5092, .T. ) ;
#374=EDGE_CURVE ( 'NONE', #7003, #15103, #2101, .T. ) ;
#377=CARTESIAN_POINT ( 'NONE',  ( 3.950837973638675393, -13.10350451991835818, -6.316429227969608817 ) ) ;
#378=CARTESIAN_POINT ( 'NONE',  ( 16.56782317627811096, 0.002708056627497615852, -0.009439921864426480472 ) ) ;
#379=VECTOR ( 'NONE', #1834, 1000.000000000000227 ) ;
#383=CARTESIAN_POINT ( 'NONE',  ( 16.56782317627811096, 0.007739510688079516768, 0.006045301465876390737 ) ) ;
#389=CARTESIAN_POINT ( 'NONE',  ( 1.918918678667046462, 7.860057224348842020, 9.738328798462404734 ) ) ;
#395=LINE ( 'NONE', #7672, #17465 ) ;
#402=CARTESIAN_POINT ( 'NONE',  ( 3.074695600507272086, 14.01296402267896291, -6.754521329824639153 ) ) ;
#405=CARTESIAN_POINT ( 'NONE',  ( 1.845755665166726844, 11.67596932341234250, 4.296872077620717434 ) ) ;
#411=CARTESIAN_POINT ( 'NONE',  ( 3.512766787570708260, -14.91422000116825508, -2.025881399556554552 ) ) ;
#415=VERTEX_POINT ( 'NONE', #6635 ) ;
#421=VERTEX_POINT ( 'NONE', #12452 ) ;
#422=CARTESIAN_POINT ( 'NONE',  ( 3.950837973638677170, 1.958075594453790869, 14.41405733518061538 ) ) ;
#426=AXIS2_PLACEMENT_3D ( 'NONE', #15769, #12992, #11762 ) ;
#428=EDGE_CURVE ( 'NONE', #7816, #11838, #16267, .T. ) ;
#433=CARTESIAN_POINT ( 'NONE',  ( 16.58200780006414732, -0.009393638146079803797, 0.006043560077721671885 ) ) ;
#439=CARTESIAN_POINT ( 'NONE',  ( 1.562796894703937678, 6.123233995736766282E-16, -5.000000000000000000 ) ) ;
#449=CARTESIAN_POINT ( 'NONE',  ( 2.697797270744668019, -3.226410068829341338, -12.89731672021093090 ) ) ;
#452=CARTESIAN_POINT ( 'NONE',  ( 0.4862570985993235340, -13.44146924561378498, -3.580942890621813923 ) ) ;
#454=B_SPLINE_CURVE_WITH_KNOTS ( 'NONE', 3,
 ( #13689, #7877, #16649, #3552, #2127, #15217 ),
 .UNSPECIFIED., .F., .F.,
 ( 4, 2, 4 ),
 ( 0.000000000000000000, 0.001656992708822042004, 0.003313985417644083140 ),
 .UNSPECIFIED. ) ;
#458=CARTESIAN_POINT ( 'NONE',  ( 2.123976203522053297, 15.54801196254786966, 1.531817366691807125 ) ) ;
#459=CARTESIAN_POINT ( 'NONE',  ( 2.002547531651519996, -3.242439124566736997, 12.17374746633577232 ) ) ;
#463=CARTESIAN_POINT ( 'NONE',  ( 1.846524061778019421, 11.93805390544205913, -3.506196582970981357 ) ) ;
#464=CARTESIAN_POINT ( 'NONE',  ( 1.918921323896321862, -11.69058285425787247, -4.466082741316331983 ) ) ;
#471=VERTEX_POINT ( 'NONE', #14633 ) ;
#475=CARTESIAN_POINT ( 'NONE',  ( 1.846955891736113298, -7.525208385419886348, -9.909315188408124087 ) ) ;
#482=CARTESIAN_POINT ( 'NONE',  ( 1.847412631396500693, -3.886120457021478902, 11.82061107079963413 ) ) ;
#485=CARTESIAN_POINT ( 'NONE',  ( 16.57778382496167424, -0.01092721432668986720, -0.01018821665058789253 ) ) ;
#494=CARTESIAN_POINT ( 'NONE',  ( 3.512766787570729576, 7.127386085303022867, -13.25664064834469613 ) ) ;
#499=ORIENTED_EDGE ( 'NONE', *, *, #15873, .T. ) ;
#500=CARTESIAN_POINT ( 'NONE',  ( 0.3095370825347224519, -13.20347358821911854, -3.806662003783552350 ) ) ;
#506=CARTESIAN_POINT ( 'NONE',  ( 16.57778382496167424, -0.001819584982831791388, -0.01482878558584694619 ) ) ;
#511=CARTESIAN_POINT ( 'NONE',  ( 1.918921323896322750, 12.49850046818175286, 0.6349083173280601899 ) ) ;
#512=ADVANCED_FACE ( 'NONE', ( #8707 ), #17039, .F. ) ;
#514=FACE_OUTER_BOUND ( 'NONE', #15611, .T. ) ;
#517=CARTESIAN_POINT ( 'NONE',  ( 0.3095370825347234511, 10.84046130709058708, 8.444334731364046220 ) ) ;
#518=ORIENTED_EDGE ( 'NONE', *, *, #5107, .T. ) ;
#520=CARTESIAN_POINT ( 'NONE',  ( 0.3095370825347234511, -13.20347358821917183, 3.806662003783360504 ) ) ;
#523=CARTESIAN_POINT ( 'NONE',  ( 8.438534575730034959, 3.845978796786118981, -5.688336279099003079 ) ) ;
#525=EDGE_LOOP ( 'NONE', ( #13484, #3363, #10680, #18665 ) ) ;
#526=CARTESIAN_POINT ( 'NONE',  ( 8.438534575730034959, 4.221456476902743837, -5.415535776177475391 ) ) ;
#527=EDGE_LOOP ( 'NONE', ( #14385, #18414, #1622, #8849 ) ) ;
#529=CARTESIAN_POINT ( 'NONE',  ( 3.950837973638677170, -14.31366178983255466, 2.591948120961746760 ) ) ;
#531=LINE ( 'NONE', #14948, #4574 ) ;
#538=CARTESIAN_POINT ( 'NONE',  ( 3.074695600507272086, -2.093687500612061658, 15.41438262616222765 ) ) ;
#541=CARTESIAN_POINT ( 'NONE',  ( 1.846138399168762101, -11.95493567637852905, 3.446241763652952539 ) ) ;
#542=DIRECTION ( 'NONE',  ( -1.000000000000000000, -0.000000000000000000, -0.000000000000000000 ) ) ;
#543=VECTOR ( 'NONE', #11601, 1000.000000000000114 ) ;
#546=EDGE_CURVE ( 'NONE', #1561, #10695, #8743, .T. ) ;
#548=EDGE_CURVE ( 'NONE', #4649, #6039, #7156, .T. ) ;
#549=CARTESIAN_POINT ( 'NONE',  ( 1.847034903785825577, -11.76058231742742777, -4.063013886994832013 ) ) ;
#554=( BOUNDED_SURFACE ( )  B_SPLINE_SURFACE ( 3, 1, ( 
 ( #11504, #4241 ),
 ( #10058, #15887 ),
 ( #10346, #17419 ),
 ( #4328, #14547 ) ),
 .UNSPECIFIED., .F., .F., .T. ) 
 B_SPLINE_SURFACE_WITH_KNOTS ( ( 4, 4 ),
 ( 2, 2 ),
 ( 0.000000000000000000, 1.000000000000000000 ),
 ( 0.000000000000000000, 1.000000000000000000 ),
 .UNSPECIFIED. ) 
 GEOMETRIC_REPRESENTATION_ITEM ( )  RATIONAL_B_SPLINE_SURFACE ( (
 ( 1.000000000000000000, 1.000000000000000000),
 ( 0.7792777138730160313, 0.9689936506012927220),
 ( 0.7792777138730160313, 0.9689936506012927220),
 ( 1.000000000000000000, 1.000000000000000000) ) ) 
 REPRESENTATION_ITEM ( '' )  SURFACE ( )  );
#559=CARTESIAN_POINT ( 'NONE',  ( 0.3939875929385635578, -11.57636969881029110, -7.545068896001335013 ) ) ;
#561=CARTESIAN_POINT ( 'NONE',  ( 1.977436885026408353, 1.488549889122500192, -15.33079650480466860 ) ) ;
#562=CARTESIAN_POINT ( 'NONE',  ( 1.846822687350018866, -11.92063725419901843, 3.566003975885642774 ) ) ;
#566=EDGE_CURVE ( 'NONE', #2137, #14073, #11492, .T. ) ;
#568=CARTESIAN_POINT ( 'NONE',  ( 8.522092701127531811, 5.397361180353207111, -4.388629235579518451 ) ) ;
#574=B_SPLINE_CURVE_WITH_KNOTS ( 'NONE', 3,
 ( #10643, #11000, #16817, #8132, #6783, #10544 ),
 .UNSPECIFIED., .F., .F.,
 ( 4, 2, 4 ),
 ( 8.673617379884034509E-19, 0.0001828790815886950508, 0.0003657581631773892342 ),
 .UNSPECIFIED. ) ;
#587=CARTESIAN_POINT ( 'NONE',  ( 16.57210152137263393, -0.008007331252333342933, 0.01214401161737632510 ) ) ;
#588=CARTESIAN_POINT ( 'NONE',  ( 2.320520222538862143, 13.71278186123479870, -7.743191299716691844 ) ) ;
#590=( BOUNDED_SURFACE ( )  B_SPLINE_SURFACE ( 3, 1, ( 
 ( #16855, #18019 ),
 ( #6645, #6547 ),
 ( #10853, #18107 ),
 ( #1964, #8079 ) ),
 .UNSPECIFIED., .F., .F., .T. ) 
 B_SPLINE_SURFACE_WITH_KNOTS ( ( 4, 4 ),
 ( 2, 2 ),
 ( 0.000000000000000000, 1.000000000000000000 ),
 ( 0.000000000000000000, 1.000000000000000000 ),
 .UNSPECIFIED. ) 
 GEOMETRIC_REPRESENTATION_ITEM ( )  RATIONAL_B_SPLINE_SURFACE ( (
 ( 1.000000000000000000, 1.000000000000000000),
 ( 0.7792777138730158093, 0.9689936506012928330),
 ( 0.7792777138730158093, 0.9689936506012928330),
 ( 1.000000000000000000, 1.000000000000000000) ) ) 
 REPRESENTATION_ITEM ( '' )  SURFACE ( )  );
#593=CARTESIAN_POINT ( 'NONE',  ( 2.636624412716902288, 7.605649742760546950, -14.14563173255513995 ) ) ;
#597=CARTESIAN_POINT ( 'NONE',  ( 0.3170788640506440603, -13.02120094575825249, -4.392045232375947350 ) ) ;
#604=EDGE_LOOP ( 'NONE', ( #14793, #13660, #11416, #15705, #8901, #5633, #7673, #18303, #12840, #5256, #1516, #16722, #14127, #4359, #12811, #8779, #820, #15702, #13342, #11139, #18510, #3613, #16269, #17169, #11483, #6561, #9871, #1346, #1933, #13849, #5209, #16099, #11607, #15015, #64, #7840, #14789, #5799, #11534, #1904, #788, #234, #2284, #5679, #3871, #5268, #7358, #7934, #11240, #1415, #14792, #9803, #10433, #12173, #14090, #8455, #17629, #14404, #16264, #8778, #14227, #17453, #4483, #11461 ) ) ;
#608=CARTESIAN_POINT ( 'NONE',  ( 3.074695600507147297, -15.41438262616236088, -2.093687500612132268 ) ) ;
#610=CARTESIAN_POINT ( 'NONE',  ( 0.4385251269669946939, -11.63205320541528209, 7.540955776459703053 ) ) ;
#611=ORIENTED_EDGE ( 'NONE', *, *, #1777, .T. ) ;
#612=CARTESIAN_POINT ( 'NONE',  ( 16.56872352241294521, -0.01027347319884440620, 0.001821578298044753286 ) ) ;
#614=CARTESIAN_POINT ( 'NONE',  ( 16.56753206892534891, 0.001549402974394159613, 0.009369540855502535986 ) ) ;
#617=VERTEX_POINT ( 'NONE', #10631 ) ;
#620=VERTEX_POINT ( 'NONE', #1836 ) ;
#621=DIRECTION ( 'NONE',  ( 0.7635533937278214944, -0.3966532189476670300, 0.5095610256143814354 ) ) ;
#627=CARTESIAN_POINT ( 'NONE',  ( 2.747332970342022840, -14.49942876448586482, -7.555624153089806505 ) ) ;
#630=LINE ( 'NONE', #13714, #10563 ) ;
#633=CARTESIAN_POINT ( 'NONE',  ( 0.4862570985993235340, 3.580942890621860109, -13.44146924561377254 ) ) ;
#634=CARTESIAN_POINT ( 'NONE',  ( 0.3939875929385670550, -12.90850834464103691, 4.930599594904505167 ) ) ;
#636=EDGE_LOOP ( 'NONE', ( #8757, #7356, #11328, #12997 ) ) ;
#637=ORIENTED_EDGE ( 'NONE', *, *, #9764, .F. ) ;
#639=ORIENTED_EDGE ( 'NONE', *, *, #11001, .F. ) ;
#649=CARTESIAN_POINT ( 'NONE',  ( 16.56872352241294521, -0.01027347319884365333, -0.001821578298043897851 ) ) ;
#653=ADVANCED_FACE ( 'NONE', ( #7584 ), #14245, .F. ) ;
#655=( BOUNDED_SURFACE ( )  B_SPLINE_SURFACE ( 3, 1, ( 
 ( #1723, #9084 ),
 ( #18316, #14908 ),
 ( #7574, #5133 ),
 ( #14014, #8108 ) ),
 .UNSPECIFIED., .F., .F., .T. ) 
 B_SPLINE_SURFACE_WITH_KNOTS ( ( 4, 4 ),
 ( 2, 2 ),
 ( 0.000000000000000000, 1.000000000000000000 ),
 ( 0.000000000000000000, 1.000000000000000000 ),
 .UNSPECIFIED. ) 
 GEOMETRIC_REPRESENTATION_ITEM ( )  RATIONAL_B_SPLINE_SURFACE ( (
 ( 1.000000000000000000, 1.000000000000000000),
 ( 0.9593108457356467333, 0.9995965569486454649),
 ( 0.9593108457356467333, 0.9995965569486454649),
 ( 1.000000000000000000, 1.000000000000000000) ) ) 
 REPRESENTATION_ITEM ( '' )  SURFACE ( )  );
#669=EDGE_CURVE ( 'NONE', #1858, #9927, #12604, .T. ) ;
#676=ORIENTED_EDGE ( 'NONE', *, *, #4525, .T. ) ;
#678=VERTEX_POINT ( 'NONE', #5254 ) ;
#682=EDGE_LOOP ( 'NONE', ( #16738, #16669, #5316, #11820 ) ) ;
#686=EDGE_LOOP ( 'NONE', ( #13746, #6468, #7548, #2921 ) ) ;
#688=CARTESIAN_POINT ( 'NONE',  ( 2.636624412717099908, 14.46769361191384817, -6.973567714910368309 ) ) ;
#691=( BOUNDED_SURFACE ( )  B_SPLINE_SURFACE ( 3, 1, ( 
 ( #14444, #5933 ),
 ( #10146, #4516 ),
 ( #11496, #11777 ),
 ( #17606, #1351 ) ),
 .UNSPECIFIED., .F., .F., .T. ) 
 B_SPLINE_SURFACE_WITH_KNOTS ( ( 4, 4 ),
 ( 2, 2 ),
 ( 0.000000000000000000, 1.000000000000000000 ),
 ( 0.000000000000000000, 1.000000000000000000 ),
 .UNSPECIFIED. ) 
 GEOMETRIC_REPRESENTATION_ITEM ( )  RATIONAL_B_SPLINE_SURFACE ( (
 ( 1.000000000000000000, 1.000000000000000000),
 ( 0.7792777138730160313, 0.9689936506012927220),
 ( 0.7792777138730160313, 0.9689936506012927220),
 ( 1.000000000000000000, 1.000000000000000000) ) ) 
 REPRESENTATION_ITEM ( '' )  SURFACE ( )  );
#696=CARTESIAN_POINT ( 'NONE',  ( 1.847034903785822468, -10.19974412751570014, 7.126331315909236075 ) ) ;
#697=CARTESIAN_POINT ( 'NONE',  ( 16.56782317627811096, -0.005492611183757366636, 0.008141063682853383679 ) ) ;
#698=VERTEX_POINT ( 'NONE', #9649 ) ;
#702=DIRECTION ( 'NONE',  ( 0.000000000000000000, 0.000000000000000000, 1.000000000000000000 ) ) ;
#705=ORIENTED_EDGE ( 'NONE', *, *, #17842, .F. ) ;
#708=ORIENTED_EDGE ( 'NONE', *, *, #6862, .T. ) ;
#713=CARTESIAN_POINT ( 'NONE',  ( 0.4862570985993235340, 13.44146924561385958, -3.580942890621532371 ) ) ;
#714=CIRCLE ( 'NONE', #15639, 14.54644660717763927 ) ;
#718=CARTESIAN_POINT ( 'NONE',  ( 3.950837973638676281, 6.316429227969464932, 13.10350451991842569 ) ) ;
#719=CARTESIAN_POINT ( 'NONE',  ( 0.3307726912345230752, 3.680742887039495148, -13.25328329128662119 ) ) ;
#725=CARTESIAN_POINT ( 'NONE',  ( 0.4862570985993235340, -7.559321496869506163, 11.67702470553362559 ) ) ;
#731=ORIENTED_EDGE ( 'NONE', *, *, #4525, .F. ) ;
#734=CARTESIAN_POINT ( 'NONE',  ( 2.636624412715999011, 2.161493821598055920, -15.91454522070273647 ) ) ;
#735=CARTESIAN_POINT ( 'NONE',  ( 1.847380140988740260, -11.79969976631074680, 3.949801494731721263 ) ) ;
#740=AXIS2_PLACEMENT_3D ( 'NONE', #14317, #5695, #1124 ) ;
#742=CARTESIAN_POINT ( 'NONE',  ( 1.846138399168762101, -12.43476674860266940, 0.4167076046095114505 ) ) ;
#743=ORIENTED_EDGE ( 'NONE', *, *, #4095, .F. ) ;
#752=CARTESIAN_POINT ( 'NONE',  ( 0.4862570985993235340, 13.44146924561385958, -3.580942890621532371 ) ) ;
#754=DIRECTION ( 'NONE',  ( -1.000000000000000000, -0.000000000000000000, -0.000000000000000000 ) ) ;
#755=ORIENTED_EDGE ( 'NONE', *, *, #5286, .F. ) ;
#756=CARTESIAN_POINT ( 'NONE',  ( 1.846524061778021419, 9.853584647934384932, 7.597197846158115553 ) ) ;
#758=CARTESIAN_POINT ( 'NONE',  ( 2.636624412716913390, 14.14563173255587536, -7.605649742760633991 ) ) ;
#764=( BOUNDED_SURFACE ( )  B_SPLINE_SURFACE ( 3, 1, ( 
 ( #3424, #12038 ),
 ( #1908, #4772 ),
 ( #378, #16145 ),
 ( #6202, #3224 ) ),
 .UNSPECIFIED., .F., .F., .T. ) 
 B_SPLINE_SURFACE_WITH_KNOTS ( ( 4, 4 ),
 ( 2, 2 ),
 ( 0.000000000000000000, 1.000000000000000000 ),
 ( 0.000000000000000000, 1.000000000000000000 ),
 .UNSPECIFIED. ) 
 GEOMETRIC_REPRESENTATION_ITEM ( )  RATIONAL_B_SPLINE_SURFACE ( (
 ( 1.000000000000000000, 1.000000000000000000),
 ( 0.9933953342250438912, 0.8357391271907739227),
 ( 0.9933953342250438912, 0.8357391271907739227),
 ( 1.000000000000000000, 1.000000000000000000) ) ) 
 REPRESENTATION_ITEM ( '' )  SURFACE ( )  );
#765=CARTESIAN_POINT ( 'NONE',  ( 2.002547531651519996, 12.17374746633582561, -3.242439124566524278 ) ) ;
#767=VERTEX_POINT ( 'NONE', #776 ) ;
#769=CARTESIAN_POINT ( 'NONE',  ( 0.3170788640506441158, 11.20690911610903839, 7.952793437297615675 ) ) ;
#771=CARTESIAN_POINT ( 'NONE',  ( 2.002547531651519996, -9.778737580845755062, 7.942910686618138705 ) ) ;
#774=B_SPLINE_CURVE_WITH_KNOTS ( 'NONE', 3,
 ( #11173, #9458, #16625, #6498, #10992, #16994 ),
 .UNSPECIFIED., .F., .F.,
 ( 4, 2, 4 ),
 ( 0.000000000000000000, 0.001657017934709842290, 0.003314035869419685448 ),
 .UNSPECIFIED. ) ;
#776=CARTESIAN_POINT ( 'NONE',  ( 3.950837973638676281, 12.81214529934975310, 6.888253895133341409 ) ) ;
#787=CARTESIAN_POINT ( 'NONE',  ( 16.56872352241294521, -0.007512283835804365630, 0.007240717549633862542 ) ) ;
#788=ORIENTED_EDGE ( 'NONE', *, *, #15085, .T. ) ;
#790=AXIS2_PLACEMENT_3D ( 'NONE', #1960, #9827, #3474 ) ;
#793=CARTESIAN_POINT ( 'NONE',  ( 1.845756295923357104, 11.67600463554279244, -4.296776483139357339 ) ) ;
#797=CARTESIAN_POINT ( 'NONE',  ( 8.522092701127531811, 2.505958102592620751, 6.489356537178200490 ) ) ;
#799=VERTEX_POINT ( 'NONE', #10019 ) ;
#800=FACE_OUTER_BOUND ( 'NONE', #4052, .T. ) ;
#801=EDGE_CURVE ( 'NONE', #11529, #3711, #15809, .T. ) ;
#802=CARTESIAN_POINT ( 'NONE',  ( 16.57210152137263393, 0.01402404281923039231, 0.003862718596009517575 ) ) ;
#806=AXIS2_PLACEMENT_3D ( 'NONE', #18244, #754, #1501 ) ;
#812=CARTESIAN_POINT ( 'NONE',  ( 2.002547531651519996, -10.57595306287287329, -6.845637710436306200 ) ) ;
#814=CARTESIAN_POINT ( 'NONE',  ( 0.3307726912345239634, -12.88561780039862015, 4.812300915532924606 ) ) ;
#820=ORIENTED_EDGE ( 'NONE', *, *, #18552, .T. ) ;
#821=CIRCLE ( 'NONE', #5677, 14.54644660717763927 ) ;
#842=CARTESIAN_POINT ( 'NONE',  ( 2.636624412717099908, 14.46769361191384817, -6.973567714910368309 ) ) ;
#843=DIRECTION ( 'NONE',  ( -1.000000000000000000, -0.000000000000000000, -0.000000000000000000 ) ) ;
#848=CARTESIAN_POINT ( 'NONE',  ( 1.847372867223027404, 10.00438561114523850, 7.398914411685026060 ) ) ;
#849=EDGE_CURVE ( 'NONE', #4916, #18880, #16511, .T. ) ;
#856=DIRECTION ( 'NONE',  ( -0.7561779333270775005, -0.6534392409364822019, 0.03481510524964565034 ) ) ;
#859=VERTEX_POINT ( 'NONE', #1324 ) ;
#860=DIRECTION ( 'NONE',  ( 1.000000000000000000, 0.000000000000000000, -0.000000000000000000 ) ) ;
#861=ORIENTED_EDGE ( 'NONE', *, *, #15792, .T. ) ;
#865=ORIENTED_EDGE ( 'NONE', *, *, #8599, .F. ) ;
#870=CARTESIAN_POINT ( 'NONE',  ( 0.3939875929385635023, 13.80036004410494499, -0.7003304234513649806 ) ) ;
#871=CARTESIAN_POINT ( 'NONE',  ( 8.438534575730034959, -6.862570336891073985, -0.2320579683290849293 ) ) ;
#873=( BOUNDED_SURFACE ( )  B_SPLINE_SURFACE ( 3, 1, ( 
 ( #8225, #3999 ),
 ( #4452, #18426 ),
 ( #6786, #11366 ),
 ( #2648, #1494 ) ),
 .UNSPECIFIED., .F., .F., .T. ) 
 B_SPLINE_SURFACE_WITH_KNOTS ( ( 4, 4 ),
 ( 2, 2 ),
 ( 0.000000000000000000, 1.000000000000000000 ),
 ( 0.000000000000000000, 1.000000000000000000 ),
 .UNSPECIFIED. ) 
 GEOMETRIC_REPRESENTATION_ITEM ( )  RATIONAL_B_SPLINE_SURFACE ( (
 ( 1.000000000000000000, 1.000000000000000000),
 ( 0.7792777138730158093, 0.9689936506012928330),
 ( 0.7792777138730158093, 0.9689936506012928330),
 ( 1.000000000000000000, 1.000000000000000000) ) ) 
 REPRESENTATION_ITEM ( '' )  SURFACE ( )  );
#875=EDGE_CURVE ( 'NONE', #12927, #9066, #3498, .T. ) ;
#878=CARTESIAN_POINT ( 'NONE',  ( 16.56822296793089322, -0.006547366384935564970, 0.007741272030791060237 ) ) ;
#881=FACE_OUTER_BOUND ( 'NONE', #10478, .T. ) ;
#882=CARTESIAN_POINT ( 'NONE',  ( 0.3132635586635975078, 8.495712071659401232, 10.79541209008106861 ) ) ;
#885=VERTEX_POINT ( 'NONE', #18534 ) ;
#886=CARTESIAN_POINT ( 'NONE',  ( 1.918918678667045130, -9.738328798462433156, 7.860057224348805605 ) ) ;
#887=ORIENTED_EDGE ( 'NONE', *, *, #17637, .T. ) ;
#891=CARTESIAN_POINT ( 'NONE',  ( 1.847380140988742703, -10.13114603776191380, -7.224522571381438496 ) ) ;
#901=CARTESIAN_POINT ( 'NONE',  ( 16.56872352241294521, 0.007512283835805451566, 0.007240717549634016065 ) ) ;
#902=DIRECTION ( 'NONE',  ( 0.000000000000000000, 0.000000000000000000, -1.000000000000000000 ) ) ;
#905=VECTOR ( 'NONE', #16915, 1000.000000000000114 ) ;
#906=CARTESIAN_POINT ( 'NONE',  ( 1.254009781011930613, -12.44229282923100932, -7.789615163754561422 ) ) ;
#912=ORIENTED_EDGE ( 'NONE', *, *, #7530, .F. ) ;
#916=DIRECTION ( 'NONE',  ( 0.7635533937278214944, -0.5095610256143857653, -0.3966532189476615899 ) ) ;
#918=CARTESIAN_POINT ( 'NONE',  ( 16.57778382496167424, -0.007244066302946679421, -0.01306626476309297180 ) ) ;
#919=CARTESIAN_POINT ( 'NONE',  ( 16.56753206892534891, -0.008432171035096412345, -0.004368917149004214288 ) ) ;
#920=CARTESIAN_POINT ( 'NONE',  ( 16.56872352241294521, -0.004907101719995745834, -0.009207754980064182873 ) ) ;
#922=EDGE_CURVE ( 'NONE', #2319, #4709, #14420, .T. ) ;
#924=ORIENTED_EDGE ( 'NONE', *, *, #7440, .T. ) ;
#929=CIRCLE ( 'NONE', #5160, 16.06066017081991149 ) ;
#934=CARTESIAN_POINT ( 'NONE',  ( 1.846138399168762101, -6.971848976711082280, 10.30487220521567693 ) ) ;
#936=CARTESIAN_POINT ( 'NONE',  ( 0.4862570985993235340, -7.559321496869506163, 11.67702470553362559 ) ) ;
#940=FACE_OUTER_BOUND ( 'NONE', #15985, .T. ) ;
#941=CARTESIAN_POINT ( 'NONE',  ( 1.847380140988742925, 3.949801494731767892, 11.79969976631073081 ) ) ;
#944=CARTESIAN_POINT ( 'NONE',  ( 2.320520222539219635, -3.126729907238178896, -15.43440824796753930 ) ) ;
#945=ORIENTED_EDGE ( 'NONE', *, *, #13952, .T. ) ;
#946=FACE_OUTER_BOUND ( 'NONE', #11798, .T. ) ;
#959=CARTESIAN_POINT ( 'NONE',  ( 2.636624412715138366, -11.10302021257964888, 11.60464335004044223 ) ) ;
#962=EDGE_CURVE ( 'NONE', #767, #9990, #14479, .T. ) ;
#965=PRESENTATION_STYLE_ASSIGNMENT (( #14060 ) ) ;
#971=ORIENTED_EDGE ( 'NONE', *, *, #14652, .T. ) ;
#972=DIRECTION ( 'NONE',  ( -1.000000000000000000, -0.000000000000000000, -0.000000000000000000 ) ) ;
#973=FACE_OUTER_BOUND ( 'NONE', #8848, .T. ) ;
#975=DIRECTION ( 'NONE',  ( 0.7561779333270775005, 0.4122479608995740508, -0.5081796452863232005 ) ) ;
#977=CARTESIAN_POINT ( 'NONE',  ( 0.3145734862173240054, 0.3064017202077272128, -13.73540602248380971 ) ) ;
#980=CARTESIAN_POINT ( 'NONE',  ( 16.57210152137263393, -0.005118120558001483002, 0.01361613799508852585 ) ) ;
#990=CARTESIAN_POINT ( 'NONE',  ( 1.846822687350019310, -3.566003975885607691, -11.92063725419902731 ) ) ;
#991=CARTESIAN_POINT ( 'NONE',  ( 16.56872352241294521, -0.004564908236400289435, -0.009382111268606239951 ) ) ;
#992=( LENGTH_UNIT ( ) NAMED_UNIT ( * ) SI_UNIT ( .MILLI., .METRE. ) );
#993=B_SPLINE_CURVE_WITH_KNOTS ( 'NONE', 3,
 ( #12995, #11576, #11764, #5628, #7376, #11481, #18728, #17394, #13186, #1623, #14813, #17592, #1725 ),
 .UNSPECIFIED., .F., .F.,
 ( 4, 3, 3, 3, 4 ),
 ( 0.000000000000000000, 0.0002299804304191490972, 0.0004599608082120256055, 0.0006467586077648033180, 0.0008336169836825999165 ),
 .UNSPECIFIED. ) ;
#1000=CARTESIAN_POINT ( 'NONE',  ( 1.847340342630335641, -0.1245571717074845930, -12.44248139376885831 ) ) ;
#1002=CARTESIAN_POINT ( 'NONE',  ( 0.3142011359265314829, 12.94258167753018895, -4.608101617236642689 ) ) ;
#1003=CARTESIAN_POINT ( 'NONE',  ( 2.697797270744668019, 7.053988368581864066, 11.26906156738829168 ) ) ;
#1006=CARTESIAN_POINT ( 'NONE',  ( 0.3151928479966097374, 0.000000000000000000, -13.73922861026898623 ) ) ;
#1010=ORIENTED_EDGE ( 'NONE', *, *, #143, .T. ) ;
#1013=EDGE_LOOP ( 'NONE', ( #6633, #16356, #12119, #12291 ) ) ;
#1015=DIRECTION ( 'NONE',  ( 0.000000000000000000, 0.000000000000000000, 1.000000000000000000 ) ) ;
#1016=CARTESIAN_POINT ( 'NONE',  ( 1.959283090834842200, -11.71721539537258394, 4.509128209890929107 ) ) ;
#1019=ORIENTED_EDGE ( 'NONE', *, *, #3155, .F. ) ;
#1022=VECTOR ( 'NONE', #16046, 1000.000000000000114 ) ;
#1023=LINE ( 'NONE', #11358, #11282 ) ;
#1024=CARTESIAN_POINT ( 'NONE',  ( 1.845755665166724624, -7.694641135842892332, 9.776700214453605042 ) ) ;
#1025=CARTESIAN_POINT ( 'NONE',  ( 1.845755665166725068, 11.97169564665396280, -3.386720041070604204 ) ) ;
#1028=CARTESIAN_POINT ( 'NONE',  ( 16.56872352241294521, 0.01033355228142401709, -0.001442253899401843694 ) ) ;
#1031=FACE_OUTER_BOUND ( 'NONE', #18121, .T. ) ;
#1035=CYLINDRICAL_SURFACE ( 'NONE', #4951, 5.000000000000000000 ) ;
#1041=CARTESIAN_POINT ( 'NONE',  ( 1.977436885026095270, -10.21547824869579202, 11.52792723756318694 ) ) ;
#1044=CARTESIAN_POINT ( 'NONE',  ( 3.950837973638668288, 0.000000000000000000, 0.000000000000000000 ) ) ;
#1047=CARTESIAN_POINT ( 'NONE',  ( 3.512766787570752669, -14.91422000116822311, 2.025881399556336060 ) ) ;
#1057=CARTESIAN_POINT ( 'NONE',  ( 0.3151930723728408879, -13.04315954105012310, -4.318364831037728280 ) ) ;
#1060=DIRECTION ( 'NONE',  ( -0.7561779333270775005, 0.2350349629540185170, 0.6106991889125065187 ) ) ;
#1062=VECTOR ( 'NONE', #916, 1000.000000000000227 ) ;
#1064=CARTESIAN_POINT ( 'NONE',  ( 3.512766787570762439, -10.40533104696141997, 10.87507422923886224 ) ) ;
#1067=CARTESIAN_POINT ( 'NONE',  ( 8.438534575730034959, -2.341351102130323714, 6.454982381540280478 ) ) ;
#1069=CARTESIAN_POINT ( 'NONE',  ( 3.950837973638675393, -10.51028938476224894, 10.05648675950122595 ) ) ;
#1071=EDGE_CURVE ( 'NONE', #8960, #9141, #6112, .T. ) ;
#1074=SHAPE_DEFINITION_REPRESENTATION ( #9384, #14244 ) ;
#1078=CARTESIAN_POINT ( 'NONE',  ( 1.847461586945734480, -3.877048136045296634, -11.82388984758122596 ) ) ;
#1083=CARTESIAN_POINT ( 'NONE',  ( 1.861706995891668326, -7.751853334747247359, -9.751699138048525839 ) ) ;
#1090=CARTESIAN_POINT ( 'NONE',  ( 0.3307726912345202441, 13.25328329128666205, 3.680742887039352151 ) ) ;
#1091=FACE_OUTER_BOUND ( 'NONE', #11796, .T. ) ;
#1097=CARTESIAN_POINT ( 'NONE',  ( 16.58200780006414732, -0.007066318000004643239, -0.008650561019685603162 ) ) ;
#1099=CARTESIAN_POINT ( 'NONE',  ( 0.3145734862173208413, -13.15783074029281963, 3.953068532979947314 ) ) ;
#1105=EDGE_LOOP ( 'NONE', ( #13101, #4621, #16613, #14738 ) ) ;
#1106=DIRECTION ( 'NONE',  ( -0.000000000000000000, 1.000000000000000000, 0.000000000000000000 ) ) ;
#1110=CARTESIAN_POINT ( 'NONE',  ( 1.846822687350017311, 10.23524390843949483, -7.075150813727003829 ) ) ;
#1112=ORIENTED_EDGE ( 'NONE', *, *, #15678, .T. ) ;
#1115=CARTESIAN_POINT ( 'NONE',  ( 2.002547531651519996, -12.17374746633580784, 3.242439124566603326 ) ) ;
#1117=LINE ( 'NONE', #7347, #12489 ) ;
#1120=EDGE_CURVE ( 'NONE', #13188, #8612, #18448, .T. ) ;
#1122=CARTESIAN_POINT ( 'NONE',  ( 2.636624412714237309, 15.80357026013209953, 2.862162146984226663 ) ) ;
#1124=DIRECTION ( 'NONE',  ( 0.000000000000000000, 0.000000000000000000, 1.000000000000000000 ) ) ;
#1127=B_SPLINE_CURVE_WITH_KNOTS ( 'NONE', 3,
 ( #12933, #14369, #15901, #1274, #17333, #10842, #6356, #7503, #7699, #12086 ),
 .UNSPECIFIED., .F., .F.,
 ( 4, 3, 3, 4 ),
 ( 0.0004168119862255878537, 0.0004599608082120251176, 0.0006467586077648016917, 0.0008336169836825990491 ),
 .UNSPECIFIED. ) ;
#1131=CARTESIAN_POINT ( 'NONE',  ( 3.950837973638676281, -1.958075594453890789, 14.41405733518059940 ) ) ;
#1134=VECTOR ( 'NONE', #3141, 1000.000000000000114 ) ;
#1140=CARTESIAN_POINT ( 'NONE',  ( 16.56782317627811096, -0.009228812961908680612, 0.003357783021327786360 ) ) ;
#1143=EDGE_LOOP ( 'NONE', ( #3747, #14066, #8797, #9515 ) ) ;
#1144=CARTESIAN_POINT ( 'NONE',  ( 2.002547531651519996, 0.6781519942173496185, -12.57989064830758785 ) ) ;
#1151=SURFACE_STYLE_FILL_AREA ( #9565 ) ;
#1162=CARTESIAN_POINT ( 'NONE',  ( 16.56782317627811096, -0.002708056627498708728, -0.009439921864426879458 ) ) ;
#1166=CARTESIAN_POINT ( 'NONE',  ( 0.3151928476913582466, 4.245853234426384404, 13.06671852871090778 ) ) ;
#1167=CARTESIAN_POINT ( 'NONE',  ( 2.747332970342022840, 2.409922051470906990, -16.17136872824896443 ) ) ;
#1174=B_SPLINE_CURVE_WITH_KNOTS ( 'NONE', 3,
 ( #3759, #15417, #2322, #8170, #891, #6734, #12545, #11678, #17127, #10052, #18740, #17412, #15971 ),
 .UNSPECIFIED., .F., .F.,
 ( 4, 3, 3, 3, 4 ),
 ( 2.453269466693398698E-18, 0.0002299804304191474167, 0.0004599608082120242502, 0.0006467586077648022338, 0.0008336169836825977481 ),
 .UNSPECIFIED. ) ;
#1177=( BOUNDED_SURFACE ( )  B_SPLINE_SURFACE ( 3, 1, ( 
 ( #11687, #4623 ),
 ( #6057, #1855 ),
 ( #2975, #11885 ),
 ( #4531, #13026 ) ),
 .UNSPECIFIED., .F., .F., .T. ) 
 B_SPLINE_SURFACE_WITH_KNOTS ( ( 4, 4 ),
 ( 2, 2 ),
 ( 0.000000000000000000, 1.000000000000000000 ),
 ( 0.000000000000000000, 1.000000000000000000 ),
 .UNSPECIFIED. ) 
 GEOMETRIC_REPRESENTATION_ITEM ( )  RATIONAL_B_SPLINE_SURFACE ( (
 ( 1.000000000000000000, 1.000000000000000000),
 ( 0.9593108457356467333, 0.9995965569486454649),
 ( 0.9593108457356467333, 0.9995965569486454649),
 ( 1.000000000000000000, 1.000000000000000000) ) ) 
 REPRESENTATION_ITEM ( '' )  SURFACE ( )  );
#1183=CARTESIAN_POINT ( 'NONE',  ( 16.56782317627811096, 0.007739510688078436902, -0.006045301465876656150 ) ) ;
#1196=CARTESIAN_POINT ( 'NONE',  ( 8.438534575730034959, 5.415535776177581972, -4.221456476902606170 ) ) ;
#1198=CARTESIAN_POINT ( 'NONE',  ( 16.56872352241294521, 0.009207754980063749192, 0.004907101719994666836 ) ) ;
#1203=ORIENTED_EDGE ( 'NONE', *, *, #13767, .T. ) ;
#1206=EDGE_CURVE ( 'NONE', #11439, #12620, #9798, .T. ) ;
#1208=ORIENTED_EDGE ( 'NONE', *, *, #16911, .F. ) ;
#1214=DIRECTION ( 'NONE',  ( -1.000000000000000000, -0.000000000000000000, -0.000000000000000000 ) ) ;
#1217=CARTESIAN_POINT ( 'NONE',  ( 0.3137051932979792457, 4.679953077377485116, 12.91601973349272114 ) ) ;
#1218=ORIENTED_EDGE ( 'NONE', *, *, #2619, .T. ) ;
#1219=ORIENTED_EDGE ( 'NONE', *, *, #192, .T. ) ;
#1225=CARTESIAN_POINT ( 'NONE',  ( 16.56872352241294521, 0.01027347319884366721, 0.001821578298043820656 ) ) ;
#1231=CARTESIAN_POINT ( 'NONE',  ( 1.846955891736115740, -12.44001089941741967, 0.2634721419534765685 ) ) ;
#1232=DIRECTION ( 'NONE',  ( 0.000000000000000000, 0.000000000000000000, 1.000000000000000000 ) ) ;
#1246=ORIENTED_EDGE ( 'NONE', *, *, #1941, .F. ) ;
#1247=CARTESIAN_POINT ( 'NONE',  ( 2.123976203522053741, -6.261444813538457943, -14.31368049382976260 ) ) ;
#1253=EDGE_LOOP ( 'NONE', ( #18351, #12029, #16983, #6300 ) ) ;
#1258=CARTESIAN_POINT ( 'NONE',  ( 0.3939875929385667219, -3.598491969338320384, 13.34133634968953785 ) ) ;
#1259=CARTESIAN_POINT ( 'NONE',  ( 0.3142011359265332593, -10.88514493056448096, 8.382042760265870029 ) ) ;
#1260=CARTESIAN_POINT ( 'NONE',  ( 2.636624412716062960, 6.973567714909310489, -14.46769361191320868 ) ) ;
#1266=CARTESIAN_POINT ( 'NONE',  ( 0.3307726912345213544, -10.76786801061213161, 8.558645027434234720 ) ) ;
#1273=ORIENTED_EDGE ( 'NONE', *, *, #546, .F. ) ;
#1274=CARTESIAN_POINT ( 'NONE',  ( 1.847412631396504246, -0.04315047898443813423, 12.44294644888238999 ) ) ;
#1276=CARTESIAN_POINT ( 'NONE',  ( 0.3095370825347234511, 4.681152801286343923, -12.91933430393602933 ) ) ;
#1279=CARTESIAN_POINT ( 'NONE',  ( 1.846138399168762101, 12.43476674860266584, -0.4167076046095982700 ) ) ;
#1291=CARTESIAN_POINT ( 'NONE',  ( 16.56822296793089322, 0.009385634690641620620, 0.003834730849370876320 ) ) ;
#1304=CARTESIAN_POINT ( 'NONE',  ( 3.950837973638668288, 0.000000000000000000, 0.000000000000000000 ) ) ;
#1306=CARTESIAN_POINT ( 'NONE',  ( 2.002547531651519996, -12.17374746633580784, 3.242439124566603326 ) ) ;
#1316=ORIENTED_EDGE ( 'NONE', *, *, #6908, .T. ) ;
#1320=CARTESIAN_POINT ( 'NONE',  ( 1.342453679581834924, 5.476372339890209773, -13.74702459364878315 ) ) ;
#1324=CARTESIAN_POINT ( 'NONE',  ( 2.636624412715384391, -11.60464335004044223, -11.10302021258006278 ) ) ;
#1325=CARTESIAN_POINT ( 'NONE',  ( 1.254255976357644409, -12.44256109021810097, 7.789651112956895496 ) ) ;
#1328=ORIENTED_EDGE ( 'NONE', *, *, #14692, .F. ) ;
#1331=CARTESIAN_POINT ( 'NONE',  ( 1.847168016377980670, 12.44137401948661470, -0.1868244120189998803 ) ) ;
#1337=ORIENTED_EDGE ( 'NONE', *, *, #2143, .F. ) ;
#1338=VECTOR ( 'NONE', #7072, 1000.000000000000114 ) ;
#1340=EDGE_CURVE ( 'NONE', #14073, #3822, #9891, .T. ) ;
#1343=VERTEX_POINT ( 'NONE', #6085 ) ;
#1346=ORIENTED_EDGE ( 'NONE', *, *, #6444, .T. ) ;
#1347=CARTESIAN_POINT ( 'NONE',  ( 0.3720661004400037664, -4.951033743989731839, 12.89739157014191129 ) ) ;
#1348=CARTESIAN_POINT ( 'NONE',  ( 1.846138399168762101, 12.43476674860266584, -0.4167076046095982700 ) ) ;
#1349=ORIENTED_EDGE ( 'NONE', *, *, #7948, .T. ) ;
#1351=CARTESIAN_POINT ( 'NONE',  ( 2.747332970342022840, -7.555624153089539163, -14.49942876448600693 ) ) ;
#1361=CARTESIAN_POINT ( 'NONE',  ( 2.697797270744668019, -12.89731672021093090, 3.226410068829379973 ) ) ;
#1363=CARTESIAN_POINT ( 'NONE',  ( 0.3137051932979792457, 0.4596302728641686874, -13.73004976592201487 ) ) ;
#1367=ORIENTED_EDGE ( 'NONE', *, *, #11992, .F. ) ;
#1370=VERTEX_POINT ( 'NONE', #7724 ) ;
#1372=EDGE_CURVE ( 'NONE', #1703, #15433, #2903, .T. ) ;
#1375=VERTEX_POINT ( 'NONE', #16316 ) ;
#1388=CARTESIAN_POINT ( 'NONE',  ( 0.3142011359265348691, -12.94258167753015520, 4.608101617236726177 ) ) ;
#1390=ORIENTED_EDGE ( 'NONE', *, *, #14686, .T. ) ;
#1397=EDGE_CURVE ( 'NONE', #13310, #10284, #3978, .T. ) ;
#1398=EDGE_CURVE ( 'NONE', #6394, #15029, #3299, .T. ) ;
#1403=CARTESIAN_POINT ( 'NONE',  ( 2.636624412714763555, 6.973567714907159321, 14.46769361191226722 ) ) ;
#1404=CARTESIAN_POINT ( 'NONE',  ( 0.3939875929385629472, 0.7003304234513173521, 13.80036004410494854 ) ) ;
#1405=CARTESIAN_POINT ( 'NONE',  ( 1.845756295923355328, -3.386818134580144690, 11.97166802574125022 ) ) ;
#1407=CARTESIAN_POINT ( 'NONE',  ( 0.000000000000000000, 0.000000000000000000, -13.42403576283810906 ) ) ;
#1408=CARTESIAN_POINT ( 'NONE',  ( 1.861628059977341598, 12.00316790821106139, -3.332996951203504032 ) ) ;
#1410=CARTESIAN_POINT ( 'NONE',  ( 0.4385251269669958596, -12.93791070501030660, -4.978066129061825329 ) ) ;
#1413=ORIENTED_EDGE ( 'NONE', *, *, #12049, .F. ) ;
#1415=ORIENTED_EDGE ( 'NONE', *, *, #1838, .T. ) ;
#1423=EDGE_CURVE ( 'NONE', #16417, #12155, #15163, .T. ) ;
#1424=CARTESIAN_POINT ( 'NONE',  ( 0.3137051932979792457, -3.805684345189695783, -13.20008686438109891 ) ) ;
#1426=DIRECTION ( 'NONE',  ( -0.7635533937278216055, -0.3620487483322522015, 0.5347026451755926280 ) ) ;
#1433=B_SPLINE_CURVE_WITH_KNOTS ( 'NONE', 3,
 ( #5635, #11493, #9844, #16943, #14262, #1348 ),
 .UNSPECIFIED., .F., .F.,
 ( 4, 2, 4 ),
 ( 5.421010862427522170E-19, 0.0001825746017570580189, 0.0003651492035141154957 ),
 .UNSPECIFIED. ) ;
#1438=AXIS2_PLACEMENT_3D ( 'NONE', #17621, #10448, #16285 ) ;
#1445=VERTEX_POINT ( 'NONE', #3754 ) ;
#1447=CARTESIAN_POINT ( 'NONE',  ( 0.3142011359265306503, -13.17934269988455576, -3.879426116491829557 ) ) ;
#1449=CARTESIAN_POINT ( 'NONE',  ( 0.3095370825347234511, -4.681152801286254217, 12.91933430393606486 ) ) ;
#1455=EDGE_CURVE ( 'NONE', #6145, #14563, #18139, .T. ) ;
#1456=CARTESIAN_POINT ( 'NONE',  ( 0.3150686449036046444, -4.099563462784746370, 13.11344473514187037 ) ) ;
#1457=FACE_OUTER_BOUND ( 'NONE', #2813, .T. ) ;
#1458=EDGE_CURVE ( 'NONE', #4902, #9063, #4904, .T. ) ;
#1459=EDGE_CURVE ( 'NONE', #1703, #10630, #14916, .T. ) ;
#1467=CARTESIAN_POINT ( 'NONE',  ( 16.56822296793089322, 0.008619100080558677116, -0.005339139727952955418 ) ) ;
#1472=VERTEX_POINT ( 'NONE', #12628 ) ;
#1477=B_SPLINE_CURVE_WITH_KNOTS ( 'NONE', 3,
 ( #5144, #8207, #13751, #6587 ),
 .UNSPECIFIED., .F., .F.,
 ( 4, 4 ),
 ( 0.000000000000000000, 0.002004993803842287058 ),
 .UNSPECIFIED. ) ;
#1484=CARTESIAN_POINT ( 'NONE',  ( 0.3151928476913556376, -8.075547435847033384, 11.11539186930584044 ) ) ;
#1486=( BOUNDED_SURFACE ( )  B_SPLINE_SURFACE ( 3, 1, ( 
 ( #16038, #8964 ),
 ( #18706, #1320 ),
 ( #5899, #17279 ),
 ( #2829, #8871 ) ),
 .UNSPECIFIED., .F., .F., .T. ) 
 B_SPLINE_SURFACE_WITH_KNOTS ( ( 4, 4 ),
 ( 2, 2 ),
 ( 0.000000000000000000, 1.000000000000000000 ),
 ( 0.000000000000000000, 1.000000000000000000 ),
 .UNSPECIFIED. ) 
 GEOMETRIC_REPRESENTATION_ITEM ( )  RATIONAL_B_SPLINE_SURFACE ( (
 ( 1.000000000000000000, 1.000000000000000000),
 ( 0.7792777138730160313, 0.9689936506012927220),
 ( 0.7792777138730160313, 0.9689936506012927220),
 ( 1.000000000000000000, 1.000000000000000000) ) ) 
 REPRESENTATION_ITEM ( '' )  SURFACE ( )  );
#1490=FACE_OUTER_BOUND ( 'NONE', #13629, .T. ) ;
#1492=ADVANCED_FACE ( 'NONE', ( #800 ), #9116, .F. ) ;
#1494=CARTESIAN_POINT ( 'NONE',  ( 0.4754618798421171855, -8.775436892861030458, -10.80499583390522744 ) ) ;
#1501=DIRECTION ( 'NONE',  ( 0.000000000000000000, 0.000000000000000000, 1.000000000000000000 ) ) ;
#1505=FACE_OUTER_BOUND ( 'NONE', #12424, .T. ) ;
#1506=CARTESIAN_POINT ( 'NONE',  ( 2.747332970342022840, -2.705255688517733681, -16.12459247543629104 ) ) ;
#1507=CARTESIAN_POINT ( 'NONE',  ( 2.320521194582820801, -15.43440938317095146, -3.126729093671786863 ) ) ;
#1510=LINE ( 'NONE', #14591, #1685 ) ;
#1516=ORIENTED_EDGE ( 'NONE', *, *, #12264, .T. ) ;
#1520=CARTESIAN_POINT ( 'NONE',  ( 3.950837973638668288, 0.000000000000000000, 0.000000000000000000 ) ) ;
#1524=CARTESIAN_POINT ( 'NONE',  ( 0.3095370825347233956, 7.700448427572036181, -11.38092634279620263 ) ) ;
#1525=CARTESIAN_POINT ( 'NONE',  ( 0.4754618798421167414, 11.68486377711977298, -7.564402563418342496 ) ) ;
#1527=CARTESIAN_POINT ( 'NONE',  ( 1.959212340397961327, 0.6675998551413537818, -12.53706137681889388 ) ) ;
#1531=CARTESIAN_POINT ( 'NONE',  ( 0.4862570985993252548, 11.67702470553365401, 7.559321496869467971 ) ) ;
#1535=ADVANCED_FACE ( 'NONE', ( #10046 ), #18158, .F. ) ;
#1541=ORIENTED_EDGE ( 'NONE', *, *, #7948, .F. ) ;
#1547=CARTESIAN_POINT ( 'NONE',  ( 3.512766787570759330, -7.127386085302901186, 13.25664064834469968 ) ) ;
#1549=DIRECTION ( 'NONE',  ( 0.000000000000000000, 0.000000000000000000, 1.000000000000000000 ) ) ;
#1550=B_SPLINE_CURVE_WITH_KNOTS ( 'NONE', 3,
 ( #17558, #9805, #15635, #2537, #8388, #1115 ),
 .UNSPECIFIED., .F., .F.,
 ( 4, 2, 4 ),
 ( 8.673617379884035472E-19, 0.0001828790815886942919, 0.0003657581631773877164 ),
 .UNSPECIFIED. ) ;
#1553=CARTESIAN_POINT ( 'NONE',  ( 0.4862570985993235340, 10.79774104611385965, -8.769551628660616771 ) ) ;
#1554=DIRECTION ( 'NONE',  ( 0.000000000000000000, 0.000000000000000000, 1.000000000000000000 ) ) ;
#1557=ADVANCED_FACE ( 'NONE', ( #13197 ), #5201, .F. ) ;
#1561=VERTEX_POINT ( 'NONE', #15 ) ;
#1564=ORIENTED_EDGE ( 'NONE', *, *, #11571, .T. ) ;
#1569=CARTESIAN_POINT ( 'NONE',  ( 1.847461586945730261, -7.286856109515127855, 10.08650590720933771 ) ) ;
#1572=B_SPLINE_CURVE_WITH_KNOTS ( 'NONE', 3,
 ( #9403, #1760, #9020, #422 ),
 .UNSPECIFIED., .F., .F.,
 ( 4, 4 ),
 ( 1.117853977359352840E-16, 0.002004993803842554205 ),
 .UNSPECIFIED. ) ;
#1574=CARTESIAN_POINT ( 'NONE',  ( 0.3151930723728413875, -8.137566970826446422, 11.07033375389128871 ) ) ;
#1577=CARTESIAN_POINT ( 'NONE',  ( 1.977436885025821267, -1.488549889121935976, 15.33079650480412326 ) ) ;
#1580=CARTESIAN_POINT ( 'NONE',  ( 0.3720661004400040439, 0.7231997263364806638, 13.79610186261030158 ) ) ;
#1584=ORIENTED_EDGE ( 'NONE', *, *, #7389, .T. ) ;
#1588=CARTESIAN_POINT ( 'NONE',  ( 8.438534575730034959, 2.341351102130277528, 6.454982381540297354 ) ) ;
#1592=ADVANCED_FACE ( 'NONE', ( #2677 ), #62, .F. ) ;
#1594=CARTESIAN_POINT ( 'NONE',  ( 1.977436885026404134, 10.21547824869624321, -11.52792723756320470 ) ) ;
#1596=CARTESIAN_POINT ( 'NONE',  ( 2.636624412714236865, 0.000000000000000000, 0.000000000000000000 ) ) ;
#1598=CARTESIAN_POINT ( 'NONE',  ( 1.847380140988738484, 11.79969976631077699, -3.949801494731646656 ) ) ;
#1616=AXIS2_PLACEMENT_3D ( 'NONE', #11781, #21, #15977 ) ;
#1619=CARTESIAN_POINT ( 'NONE',  ( 0.4754618798421171855, -7.564402563418553882, 11.68486377711963797 ) ) ;
#1622=ORIENTED_EDGE ( 'NONE', *, *, #17410, .T. ) ;
#1623=CARTESIAN_POINT ( 'NONE',  ( 1.847034903785823357, 7.498375632854758166, -9.929438108952064468 ) ) ;
#1624=CARTESIAN_POINT ( 'NONE',  ( 0.3151928479966097374, 1.775918418904422640E-15, 13.73922861026898623 ) ) ;
#1629=B_SPLINE_CURVE_WITH_KNOTS ( 'NONE', 3,
 ( #12405, #4960, #15276, #14990 ),
 .UNSPECIFIED., .F., .F.,
 ( 4, 4 ),
 ( 0.000000000000000000, 0.002004993803842899849 ),
 .UNSPECIFIED. ) ;
#1631=B_SPLINE_CURVE_WITH_KNOTS ( 'NONE', 3,
 ( #4696, #3344, #18074, #16639, #10719, #15008 ),
 .UNSPECIFIED., .F., .F.,
 ( 4, 2, 4 ),
 ( 4.016409351050315258E-17, 0.0002014099069817277545, 0.0004028198139634153394 ),
 .UNSPECIFIED. ) ;
#1642=ORIENTED_EDGE ( 'NONE', *, *, #9893, .F. ) ;
#1643=CARTESIAN_POINT ( 'NONE',  ( 0.000000000000000000, 0.000000000000000000, 0.000000000000000000 ) ) ;
#1648=ORIENTED_EDGE ( 'NONE', *, *, #11206, .F. ) ;
#1650=CARTESIAN_POINT ( 'NONE',  ( 2.636624412715137922, -14.46769361191291559, 6.973567714907789927 ) ) ;
#1657=VERTEX_POINT ( 'NONE', #4321 ) ;
#1658=EDGE_CURVE ( 'NONE', #3963, #18321, #8990, .T. ) ;
#1661=CARTESIAN_POINT ( 'NONE',  ( 1.861706995891668992, -11.66987142852987169, 4.359009869687201721 ) ) ;
#1665=B_SPLINE_CURVE_WITH_KNOTS ( 'NONE', 3,
 ( #4489, #16144, #10406, #1325, #17576, #14800 ),
 .UNSPECIFIED., .F., .F.,
 ( 4, 2, 4 ),
 ( 0.000000000000000000, 0.001656992708822777310, 0.003313985417645554619 ),
 .UNSPECIFIED. ) ;
#1666=CARTESIAN_POINT ( 'NONE',  ( 2.636624412715999011, 2.161493821598055920, -15.91454522070273647 ) ) ;
#1672=B_SPLINE_CURVE_WITH_KNOTS ( 'NONE', 3,
 ( #11666, #8607, #4397, #14432 ),
 .UNSPECIFIED., .F., .F.,
 ( 4, 4 ),
 ( 1.182319362138779820E-16, 0.002004993803842621859 ),
 .UNSPECIFIED. ) ;
#1673=CARTESIAN_POINT ( 'NONE',  ( 0.4754618798421171855, 11.68486377711966639, 7.564402563418515690 ) ) ;
#1675=CARTESIAN_POINT ( 'NONE',  ( 1.342453679581834924, -13.74702459364880269, -5.476372339890162699 ) ) ;
#1677=CARTESIAN_POINT ( 'NONE',  ( 16.56782317627811096, -0.005492611183758475124, -0.008141063682853461742 ) ) ;
#1678=B_SPLINE_CURVE_WITH_KNOTS ( 'NONE', 3,
 ( #8570, #7053, #8767, #11540, #9999, #13058 ),
 .UNSPECIFIED., .F., .F.,
 ( 4, 2, 4 ),
 ( 7.047314121155778821E-19, 0.001657017934710171237, 0.003314035869420342041 ),
 .UNSPECIFIED. ) ;
#1680=ORIENTED_EDGE ( 'NONE', *, *, #12410, .F. ) ;
#1682=ORIENTED_EDGE ( 'NONE', *, *, #4053, .F. ) ;
#1685=VECTOR ( 'NONE', #6293, 1000.000000000000000 ) ;
#1686=B_SPLINE_CURVE_WITH_KNOTS ( 'NONE', 3,
 ( #11949, #16251, #3132, #17784, #17880, #9082 ),
 .UNSPECIFIED., .F., .F.,
 ( 4, 2, 4 ),
 ( 0.000000000000000000, 0.001656992708821696143, 0.003313985417643392287 ),
 .UNSPECIFIED. ) ;
#1688=EDGE_LOOP ( 'NONE', ( #13705, #9023, #13242, #14848 ) ) ;
#1695=CARTESIAN_POINT ( 'NONE',  ( 1.846955891736114852, 11.74973605926570386, -4.094751675596581819 ) ) ;
#1697=CARTESIAN_POINT ( 'NONE',  ( 0.3308579732647026761, -12.88563776947742312, -4.812490080619330257 ) ) ;
#1701=AXIS2_PLACEMENT_3D ( 'NONE', #9909, #18518, #5427 ) ;
#1703=VERTEX_POINT ( 'NONE', #3351 ) ;
#1704=ORIENTED_EDGE ( 'NONE', *, *, #3086, .F. ) ;
#1705=CARTESIAN_POINT ( 'NONE',  ( 0.3095370825347234511, 13.73357284481724783, 0.4597470195090685441 ) ) ;
#1711=CARTESIAN_POINT ( 'NONE',  ( 2.002547531651519996, 0.6781519942173496185, -12.57989064830758785 ) ) ;
#1713=CARTESIAN_POINT ( 'NONE',  ( 0.3137051932979792457, -0.4596302728640728752, 13.73004976592201842 ) ) ;
#1714=FACE_OUTER_BOUND ( 'NONE', #11824, .T. ) ;
#1722=CARTESIAN_POINT ( 'NONE',  ( 0.3145729642390426295, 13.15786090015083687, 3.952965287571154729 ) ) ;
#1723=CARTESIAN_POINT ( 'NONE',  ( 16.56753206892534891, -0.001549402974393209202, 0.009369540855502124857 ) ) ;
#1725=CARTESIAN_POINT ( 'NONE',  ( 1.846138399168762101, 7.646096044340033870, -9.815003036200328879 ) ) ;
#1727=ORIENTED_EDGE ( 'NONE', *, *, #3988, .F. ) ;
#1733=EDGE_LOOP ( 'NONE', ( #13246, #1019, #8676, #6333 ) ) ;
#1741=VECTOR ( 'NONE', #13870, 1000.000000000000000 ) ;
#1742=CARTESIAN_POINT ( 'NONE',  ( 0.4862570985993235340, -8.769551628660655851, -10.79774104611382946 ) ) ;
#1748=EDGE_CURVE ( 'NONE', #3711, #4894, #334, .T. ) ;
#1749=CARTESIAN_POINT ( 'NONE',  ( 1.846138399168762101, -10.30487220521574976, 6.971848976710974810 ) ) ;
#1753=EDGE_CURVE ( 'NONE', #8074, #12492, #16369, .T. ) ;
#1754=ORIENTED_EDGE ( 'NONE', *, *, #15943, .T. ) ;
#1756=FACE_OUTER_BOUND ( 'NONE', #7700, .T. ) ;
#1757=ORIENTED_EDGE ( 'NONE', *, *, #9650, .F. ) ;
#1760=CARTESIAN_POINT ( 'NONE',  ( 3.074695600507308946, 2.093687500611960850, 15.41438262616221522 ) ) ;
#1766=CARTESIAN_POINT ( 'NONE',  ( 16.56753206892534891, -0.004368917149005391298, -0.008432171035096433162 ) ) ;
#1775=CARTESIAN_POINT ( 'NONE',  ( 2.123976203522053741, 6.261444813538558307, 14.31368049382972529 ) ) ;
#1777=EDGE_CURVE ( 'NONE', #13145, #12510, #1840, .T. ) ;
#1780=CARTESIAN_POINT ( 'NONE',  ( 0.3095370825347224519, 12.91933430393614302, -4.681152801286025955 ) ) ;
#1786=ORIENTED_EDGE ( 'NONE', *, *, #10512, .T. ) ;
#1791=VECTOR ( 'NONE', #975, 1000.000000000000000 ) ;
#1797=CARTESIAN_POINT ( 'NONE',  ( 1.845756295923360435, -4.296776483139397307, -11.67600463554277468 ) ) ;
#1802=ORIENTED_EDGE ( 'NONE', *, *, #3840, .F. ) ;
#1805=ORIENTED_EDGE ( 'NONE', *, *, #11183, .F. ) ;
#1808=CARTESIAN_POINT ( 'NONE',  ( 2.636624412717099908, 14.46769361191384817, -6.973567714910368309 ) ) ;
#1820=CONICAL_SURFACE ( 'NONE', #7320, 14.54644660717763927, 0.8559913436420816257 ) ;
#1827=CARTESIAN_POINT ( 'NONE',  ( 0.3151928478948580192, 0.0001388664989280257334, 13.73922860964089665 ) ) ;
#1834=DIRECTION ( 'NONE',  ( -0.7635533937278214944, -0.6071939193889592801, 0.2197766120036439286 ) ) ;
#1835=ORIENTED_EDGE ( 'NONE', *, *, #3867, .T. ) ;
#1836=CARTESIAN_POINT ( 'NONE',  ( 0.4862570985993235340, -13.89016912371018186, 0.7479633556561964269 ) ) ;
#1838=EDGE_CURVE ( 'NONE', #9063, #287, #6935, .T. ) ;
#1839=ORIENTED_EDGE ( 'NONE', *, *, #12750, .F. ) ;
#1840=LINE ( 'NONE', #7678, #220 ) ;
#1841=CARTESIAN_POINT ( 'NONE',  ( 0.3151930723728450512, 13.73922999529477451, 0.07645105376991474799 ) ) ;
#1847=CARTESIAN_POINT ( 'NONE',  ( 0.3148213771069381384, 10.97836617636225220, 8.260246460850757089 ) ) ;
#1848=B_SPLINE_CURVE_WITH_KNOTS ( 'NONE', 3,
 ( #1991, #12481, #16525, #464, #13650, #3411 ),
 .UNSPECIFIED., .F., .F.,
 ( 4, 2, 4 ),
 ( 0.000000000000000000, 0.0001828790815886945087, 0.0003657581631773890174 ),
 .UNSPECIFIED. ) ;
#1852=CARTESIAN_POINT ( 'NONE',  ( 1.846138399168762101, -11.69739621335925328, 4.238866729160359448 ) ) ;
#1853=EDGE_LOOP ( 'NONE', ( #6438, #10768, #2357, #755 ) ) ;
#1854=CARTESIAN_POINT ( 'NONE',  ( 3.950837973638668288, 0.000000000000000000, 0.000000000000000000 ) ) ;
#1855=CARTESIAN_POINT ( 'NONE',  ( 0.3170788640506441158, -11.02668139258447866, 8.200855617524497987 ) ) ;
#1858=VERTEX_POINT ( 'NONE', #16742 ) ;
#1866=B_SPLINE_CURVE_WITH_KNOTS ( 'NONE', 3,
 ( #14778, #8858, #1594, #11729, #17559, #7437 ),
 .UNSPECIFIED., .F., .F.,
 ( 4, 2, 4 ),
 ( 0.000000000000000000, 0.001656992708823241348, 0.003313985417646482697 ),
 .UNSPECIFIED. ) ;
#1867=CARTESIAN_POINT ( 'NONE',  ( 2.636624412715999011, 2.161493821598055920, -15.91454522070273647 ) ) ;
#1872=CARTESIAN_POINT ( 'NONE',  ( 2.697797270744667131, 13.26309265156977624, 0.9169917281807724585 ) ) ;
#1873=LINE ( 'NONE', #10858, #17961 ) ;
#1875=CARTESIAN_POINT ( 'NONE',  ( 3.353306896162455697, 12.78841260990237672, 5.573563251762143622 ) ) ;
#1877=CARTESIAN_POINT ( 'NONE',  ( 16.56679352167444819, -0.009190982326619374226, 0.001390132774595425865 ) ) ;
#1883=B_SPLINE_CURVE_WITH_KNOTS ( 'NONE', 3,
 ( #4717, #2041, #15030, #4816 ),
 .UNSPECIFIED., .F., .F.,
 ( 4, 4 ),
 ( 5.210130127421859526E-17, 0.002004993803842660023 ),
 .UNSPECIFIED. ) ;
#1886=FACE_OUTER_BOUND ( 'NONE', #200, .T. ) ;
#1889=ADVANCED_FACE ( 'NONE', ( #4299 ), #1924, .F. ) ;
#1891=CARTESIAN_POINT ( 'NONE',  ( 0.3137051932979792457, -3.805684345189695783, -13.20008686438109891 ) ) ;
#1893=CONICAL_SURFACE ( 'NONE', #9208, 14.54644660717763927, 0.8559913436420816257 ) ;
#1895=CARTESIAN_POINT ( 'NONE',  ( 3.950837973638676281, 2.591948120962007884, -14.31366178983250670 ) ) ;
#1896=CARTESIAN_POINT ( 'NONE',  ( 0.3150686449036038117, 8.199336701264542171, 11.02450593298021175 ) ) ;
#1900=CARTESIAN_POINT ( 'NONE',  ( 1.846613052777650976, 7.585914669018171352, 9.862487290071024759 ) ) ;
#1904=ORIENTED_EDGE ( 'NONE', *, *, #12004, .T. ) ;
#1907=CARTESIAN_POINT ( 'NONE',  ( 2.636624412717099908, 15.80357026013547816, -2.862162146981609201 ) ) ;
#1908=CARTESIAN_POINT ( 'NONE',  ( 16.56822296793089322, 0.003834730849370841625, -0.009385634690641637967 ) ) ;
#1910=CARTESIAN_POINT ( 'NONE',  ( 3.512766787570925864, 13.25664064834466593, -7.127386085302575225 ) ) ;
#1916=EDGE_CURVE ( 'NONE', #17275, #15858, #8409, .T. ) ;
#1917=DIRECTION ( 'NONE',  ( 0.000000000000000000, 0.000000000000000000, 1.000000000000000000 ) ) ;
#1921=CARTESIAN_POINT ( 'NONE',  ( 0.3150686449036101955, 13.11344473514187925, 4.099563462784696632 ) ) ;
#1924=( BOUNDED_SURFACE ( )  B_SPLINE_SURFACE ( 3, 1, ( 
 ( #7075, #17286 ),
 ( #16045, #2660 ),
 ( #5712, #4208 ),
 ( #2837, #7171 ) ),
 .UNSPECIFIED., .F., .F., .T. ) 
 B_SPLINE_SURFACE_WITH_KNOTS ( ( 4, 4 ),
 ( 2, 2 ),
 ( 0.000000000000000000, 1.000000000000000000 ),
 ( 0.000000000000000000, 1.000000000000000000 ),
 .UNSPECIFIED. ) 
 GEOMETRIC_REPRESENTATION_ITEM ( )  RATIONAL_B_SPLINE_SURFACE ( (
 ( 1.000000000000000000, 1.000000000000000000),
 ( 0.7792777138730160313, 0.9689936506012927220),
 ( 0.7792777138730160313, 0.9689936506012927220),
 ( 1.000000000000000000, 1.000000000000000000) ) ) 
 REPRESENTATION_ITEM ( '' )  SURFACE ( )  );
#1926=B_SPLINE_CURVE_WITH_KNOTS ( 'NONE', 3,
 ( #2849, #14526, #4309, #6031, #16156, #13098 ),
 .UNSPECIFIED., .F., .F.,
 ( 4, 2, 4 ),
 ( 0.000000000000000000, 0.001656992708822557434, 0.003313985417645114867 ),
 .UNSPECIFIED. ) ;
#1931=FACE_OUTER_BOUND ( 'NONE', #14603, .T. ) ;
#1933=ORIENTED_EDGE ( 'NONE', *, *, #6009, .T. ) ;
#1937=CARTESIAN_POINT ( 'NONE',  ( 2.123976203522053297, -15.54801196254785722, -1.531817366691915483 ) ) ;
#1938=CARTESIAN_POINT ( 'NONE',  ( 2.002547531651519996, 4.532360870844494016, -11.75462648437097180 ) ) ;
#1941=EDGE_CURVE ( 'NONE', #14610, #8961, #2571, .T. ) ;
#1944=CARTESIAN_POINT ( 'NONE',  ( 1.846955891736114852, -9.909315188408097441, 7.525208385419928092 ) ) ;
#1946=CARTESIAN_POINT ( 'NONE',  ( 0.3137051932979792457, -11.37800749014136592, 7.698472063774431717 ) ) ;
#1947=ORIENTED_EDGE ( 'NONE', *, *, #6398, .T. ) ;
#1960=CARTESIAN_POINT ( 'NONE',  ( 2.636624412714236865, 0.000000000000000000, 0.000000000000000000 ) ) ;
#1964=CARTESIAN_POINT ( 'NONE',  ( 16.56872352241294521, -0.009207754980063714498, -0.004907101719994726684 ) ) ;
#1966=DIRECTION ( 'NONE',  ( 0.7635533937278214944, 0.6204116510013490959, -0.1790966170213899034 ) ) ;
#1967=CARTESIAN_POINT ( 'NONE',  ( 2.002547531651519996, 10.57595306287302250, -6.845637710436074386 ) ) ;
#1970=CARTESIAN_POINT ( 'NONE',  ( 2.002547531651519996, -12.57989064830760206, 0.6781519942171299054 ) ) ;
#1976=ORIENTED_EDGE ( 'NONE', *, *, #11935, .F. ) ;
#1977=ORIENTED_EDGE ( 'NONE', *, *, #3834, .F. ) ;
#1979=EDGE_CURVE ( 'NONE', #8074, #16551, #11037, .T. ) ;
#1989=CARTESIAN_POINT ( 'NONE',  ( 0.4754618798421162973, -8.775436892861190330, 10.80499583390509954 ) ) ;
#1991=CARTESIAN_POINT ( 'NONE',  ( 1.846138399168762101, -11.69739621335919111, -4.238866729160527314 ) ) ;
#1992=B_SPLINE_CURVE_WITH_KNOTS ( 'NONE', 3,
 ( #6535, #882, #6723, #2043, #18366, #5181 ),
 .UNSPECIFIED., .F., .F.,
 ( 4, 2, 4 ),
 ( 1.084202172485504434E-19, 0.0002017457492448070664, 0.0004034914984896140243 ),
 .UNSPECIFIED. ) ;
#1994=VECTOR ( 'NONE', #1106, 1000.000000000000000 ) ;
#1999=ORIENTED_EDGE ( 'NONE', *, *, #13858, .F. ) ;
#2000=EDGE_CURVE ( 'NONE', #12695, #415, #12191, .T. ) ;
#2002=CONICAL_SURFACE ( 'NONE', #9915, 14.54644660717763927, 0.8559913436420816257 ) ;
#2005=CARTESIAN_POINT ( 'NONE',  ( 8.522092701127531811, -5.397361180353174248, 4.388629235579559307 ) ) ;
#2010=CARTESIAN_POINT ( 'NONE',  ( 2.636624412716913390, 14.14563173255587536, -7.605649742760633991 ) ) ;
#2011=ORIENTED_EDGE ( 'NONE', *, *, #318, .F. ) ;
#2019=ORIENTED_EDGE ( 'NONE', *, *, #8392, .T. ) ;
#2030=AXIS2_PLACEMENT_3D ( 'NONE', #15716, #11248, #17249 ) ;
#2031=ORIENTED_EDGE ( 'NONE', *, *, #4741, .F. ) ;
#2034=CARTESIAN_POINT ( 'NONE',  ( 0.3150686449036029790, 13.73846184595214304, -0.1533607327086227434 ) ) ;
#2039=CARTESIAN_POINT ( 'NONE',  ( 0.3308579732647032867, -11.46737410776358779, 7.595989242675092790 ) ) ;
#2041=CARTESIAN_POINT ( 'NONE',  ( 3.074695600507254767, -11.23985886659442635, 10.75417554975694578 ) ) ;
#2042=B_SPLINE_CURVE_WITH_KNOTS ( 'NONE', 3,
 ( #17812, #5941, #4527, #4716, #3837, #4991 ),
 .UNSPECIFIED., .F., .F.,
 ( 4, 2, 4 ),
 ( 1.084202172485504434E-19, 0.001657017934709843158, 0.003314035869419686316 ),
 .UNSPECIFIED. ) ;
#2043=CARTESIAN_POINT ( 'NONE',  ( 0.3939875929385636688, 8.678227324501120776, 10.75308190953746212 ) ) ;
#2045=ORIENTED_EDGE ( 'NONE', *, *, #16190, .T. ) ;
#2046=ORIENTED_EDGE ( 'NONE', *, *, #7348, .F. ) ;
#2050=VERTEX_POINT ( 'NONE', #936 ) ;
#2051=DIRECTION ( 'NONE',  ( 0.000000000000000000, 0.000000000000000000, 1.000000000000000000 ) ) ;
#2052=ADVANCED_FACE ( 'NONE', ( #10902 ), #12402, .F. ) ;
#2056=VECTOR ( 'NONE', #6749, 1000.000000000000227 ) ;
#2057=CARTESIAN_POINT ( 'NONE',  ( 3.512766787571172333, 14.91422000116773994, 2.025881399556380469 ) ) ;
#2062=EDGE_CURVE ( 'NONE', #10419, #14675, #774, .T. ) ;
#2070=CARTESIAN_POINT ( 'NONE',  ( 16.56822296793089322, -0.0007467251401289379167, 0.01011126603341003759 ) ) ;
#2075=LINE ( 'NONE', #10866, #2056 ) ;
#2076=EDGE_CURVE ( 'NONE', #11529, #3979, #12319, .T. ) ;
#2081=ADVANCED_FACE ( 'NONE', ( #15550 ), #11074, .F. ) ;
#2087=CARTESIAN_POINT ( 'NONE',  ( 3.377929128793393687, 12.02809354424100619, 7.136734442940879219 ) ) ;
#2090=EDGE_CURVE ( 'NONE', #8004, #6249, #5102, .T. ) ;
#2091=CARTESIAN_POINT ( 'NONE',  ( 16.58200780006414732, 0.007066318000004704822, 0.008650561019685554590 ) ) ;
#2101=CIRCLE ( 'NONE', #14295, 5.000000000000000000 ) ;
#2102=DIRECTION ( 'NONE',  ( 0.000000000000000000, 0.000000000000000000, 1.000000000000000000 ) ) ;
#2104=CARTESIAN_POINT ( 'NONE',  ( 2.747332970342022840, -14.49942876448597673, 7.555624153089596895 ) ) ;
#2105=DIRECTION ( 'NONE',  ( 1.000000000000000000, 0.000000000000000000, 0.000000000000000000 ) ) ;
#2109=CARTESIAN_POINT ( 'NONE',  ( 0.4754618798421167414, -13.45049478164062329, 3.583352865732619463 ) ) ;
#2119=CARTESIAN_POINT ( 'NONE',  ( 1.861706995891668104, 12.00328602385080679, 3.332865258614018611 ) ) ;
#2120=VERTEX_POINT ( 'NONE', #11630 ) ;
#2124=CARTESIAN_POINT ( 'NONE',  ( 2.697797270744666243, 8.537712152181008207, -10.19107313879048249 ) ) ;
#2127=CARTESIAN_POINT ( 'NONE',  ( 0.8740764193766140666, 14.27348595579769253, 0.8420116711621705718 ) ) ;
#2128=EDGE_CURVE ( 'NONE', #9839, #9866, #16275, .T. ) ;
#2137=VERTEX_POINT ( 'NONE', #1403 ) ;
#2139=CONICAL_SURFACE ( 'NONE', #12208, 16.06066017081991149, 0.7853981625000062694 ) ;
#2143=EDGE_CURVE ( 'NONE', #11376, #2137, #1678, .T. ) ;
#2144=ORIENTED_EDGE ( 'NONE', *, *, #17987, .F. ) ;
#2145=ORIENTED_EDGE ( 'NONE', *, *, #15651, .T. ) ;
#2146=DIRECTION ( 'NONE',  ( 0.000000000000000000, 0.000000000000000000, 1.000000000000000000 ) ) ;
#2147=LINE ( 'NONE', #7984, #18677 ) ;
#2153=PRODUCT_CONTEXT ( 'NONE', #3119, 'mechanical' ) ;
#2163=ORIENTED_EDGE ( 'NONE', *, *, #12769, .F. ) ;
#2165=ORIENTED_EDGE ( 'NONE', *, *, #17163, .T. ) ;
#2167=ORIENTED_EDGE ( 'NONE', *, *, #4053, .T. ) ;
#2172=CARTESIAN_POINT ( 'NONE',  ( 16.56872352241294521, -0.01033355228142500762, -0.001442253899401184716 ) ) ;
#2173=CARTESIAN_POINT ( 'NONE',  ( 1.847461586945728929, -11.82388984758122064, 3.877048136045332605 ) ) ;
#2178=CARTESIAN_POINT ( 'NONE',  ( 2.636624412715137034, -11.60464335004055947, 11.10302021257951743 ) ) ;
#2179=CARTESIAN_POINT ( 'NONE',  ( 1.846138399168762101, 0.4167076046095548603, 12.43476674860266762 ) ) ;
#2183=ORIENTED_EDGE ( 'NONE', *, *, #4663, .F. ) ;
#2184=CARTESIAN_POINT ( 'NONE',  ( 1.254009781012409341, 13.61532727684501509, -5.487405433548977030 ) ) ;
#2187=AXIS2_PLACEMENT_3D ( 'NONE', #103, #15959, #18829 ) ;
#2191=ORIENTED_EDGE ( 'NONE', *, *, #18654, .F. ) ;
#2193=CARTESIAN_POINT ( 'NONE',  ( 8.522092701127531811, 5.841710761610131364, 3.777034505568545253 ) ) ;
#2195=CARTESIAN_POINT ( 'NONE',  ( 0.4862570985993235340, 13.89016912371017476, 0.7479633556562934604 ) ) ;
#2198=CARTESIAN_POINT ( 'NONE',  ( 0.4862570985993235340, 11.67702470553376060, -7.559321496869298329 ) ) ;
#2200=ORIENTED_EDGE ( 'NONE', *, *, #5215, .F. ) ;
#2203=CARTESIAN_POINT ( 'NONE',  ( 0.4754618798421171855, 13.45049478164060019, 3.583352865732718495 ) ) ;
#2212=CARTESIAN_POINT ( 'NONE',  ( 2.705023505549863039, 3.294610156756076602, -12.88681800078729189 ) ) ;
#2214=DIRECTION ( 'NONE',  ( 0.000000000000000000, 0.000000000000000000, 1.000000000000000000 ) ) ;
#2217=CARTESIAN_POINT ( 'NONE',  ( 3.950837973638676281, -6.316429227969383220, -13.10350451991847009 ) ) ;
#2219=ORIENTED_EDGE ( 'NONE', *, *, #669, .F. ) ;
#2225=ORIENTED_EDGE ( 'NONE', *, *, #374, .F. ) ;
#2227=EDGE_LOOP ( 'NONE', ( #16799, #1977, #16713, #11656 ) ) ;
#2243=ORIENTED_EDGE ( 'NONE', *, *, #16628, .F. ) ;
#2251=ORIENTED_EDGE ( 'NONE', *, *, #6070, .T. ) ;
#2255=CARTESIAN_POINT ( 'NONE',  ( 16.57778382496167424, -0.01092721432669101385, 0.01018821665058845458 ) ) ;
#2256=CARTESIAN_POINT ( 'NONE',  ( 1.847168016377982669, -11.77471791462001782, 4.022276579849913603 ) ) ;
#2257=CARTESIAN_POINT ( 'NONE',  ( 1.342453679581834924, -3.649820028552833051, 14.34050741580205823 ) ) ;
#2261=AXIS2_PLACEMENT_3D ( 'NONE', #9546, #12421, #9369 ) ;
#2263=CARTESIAN_POINT ( 'NONE',  ( 3.074695600507255655, -6.754521329824886955, 14.01296402267885988 ) ) ;
#2267=ORIENTED_EDGE ( 'NONE', *, *, #14797, .T. ) ;
#2272=CARTESIAN_POINT ( 'NONE',  ( 16.56679352167444819, 0.009170718284672540327, 0.001518074900130682347 ) ) ;
#2275=LINE ( 'NONE', #18152, #119 ) ;
#2278=CARTESIAN_POINT ( 'NONE',  ( 0.3132635586635981184, -8.495712071659319520, -10.79541209008113256 ) ) ;
#2279=DIRECTION ( 'NONE',  ( -1.000000000000000000, -0.000000000000000000, -0.000000000000000000 ) ) ;
#2282=CARTESIAN_POINT ( 'NONE',  ( 2.636624412717140764, -2.862162146982851763, -15.80357026013259514 ) ) ;
#2284=ORIENTED_EDGE ( 'NONE', *, *, #5157, .T. ) ;
#2290=EDGE_CURVE ( 'NONE', #6145, #8886, #14680, .T. ) ;
#2306=B_SPLINE_CURVE_WITH_KNOTS ( 'NONE', 3,
 ( #6875, #12698, #14230, #5517, #18258, #15380 ),
 .UNSPECIFIED., .F., .F.,
 ( 4, 2, 4 ),
 ( 1.748223473168675632E-18, 0.0002017457492448083403, 0.0004034914984896149459 ),
 .UNSPECIFIED. ) ;
#2307=FACE_OUTER_BOUND ( 'NONE', #16486, .T. ) ;
#2310=CARTESIAN_POINT ( 'NONE',  ( 2.320521194584331148, 11.60169518685982304, -10.64885423995325198 ) ) ;
#2312=ORIENTED_EDGE ( 'NONE', *, *, #7348, .T. ) ;
#2315=VERTEX_POINT ( 'NONE', #452 ) ;
#2317=CARTESIAN_POINT ( 'NONE',  ( 2.002547531651519996, -9.778737580845755062, 7.942910686618138705 ) ) ;
#2319=VERTEX_POINT ( 'NONE', #3201 ) ;
#2320=CARTESIAN_POINT ( 'NONE',  ( 16.56872352241294521, -0.007512283835804365630, 0.007240717549633862542 ) ) ;
#2322=CARTESIAN_POINT ( 'NONE',  ( 1.846955891736119071, -10.21904526726841311, -7.098901504650468652 ) ) ;
#2336=CARTESIAN_POINT ( 'NONE',  ( 0.8740779401510443414, -12.04241618260075164, -7.708543377337893077 ) ) ;
#2343=CARTESIAN_POINT ( 'NONE',  ( 0.3307726912345200776, 12.88561780039865745, -4.812300915532842005 ) ) ;
#2344=CARTESIAN_POINT ( 'NONE',  ( 16.56822296793089322, 0.009847136207496274760, 0.002414375228568293487 ) ) ;
#2345=CIRCLE ( 'NONE', #13023, 14.54644660717763927 ) ;
#2348=EDGE_CURVE ( 'NONE', #13773, #17548, #15125, .T. ) ;
#2350=CARTESIAN_POINT ( 'NONE',  ( 2.320520222537280741, -6.542539914240626864, 14.32454429810376162 ) ) ;
#2351=EDGE_CURVE ( 'NONE', #5784, #12010, #263, .T. ) ;
#2354=LINE ( 'NONE', #3785, #9093 ) ;
#2357=ORIENTED_EDGE ( 'NONE', *, *, #13154, .T. ) ;
#2360=ORIENTED_EDGE ( 'NONE', *, *, #8599, .T. ) ;
#2361=ADVANCED_FACE ( 'NONE', ( #6089 ), #7047, .F. ) ;
#2363=CARTESIAN_POINT ( 'NONE',  ( 2.697797270744668463, -12.33058466479264936, -4.970631985779717432 ) ) ;
#2364=LINE ( 'NONE', #6493, #12802 ) ;
#2367=CARTESIAN_POINT ( 'NONE',  ( 16.56822296793089322, 0.0007467251401297140970, 0.01011126603341077831 ) ) ;
#2370=CARTESIAN_POINT ( 'NONE',  ( 1.959212340397945562, -6.829000156128106624, -10.53510106265289359 ) ) ;
#2372=CARTESIAN_POINT ( 'NONE',  ( 0.3058872367615230181, 3.664492643742949252, -13.24582953854921463 ) ) ;
#2375=CARTESIAN_POINT ( 'NONE',  ( 1.562796894703937678, 1.635200584729765362E-15, 12.15840553252917289 ) ) ;
#2386=ORIENTED_EDGE ( 'NONE', *, *, #1455, .T. ) ;
#2396=CARTESIAN_POINT ( 'NONE',  ( 0.4385251269669950824, 0.7363879510387324467, -13.84299131624728751 ) ) ;
#2397=( BOUNDED_SURFACE ( )  B_SPLINE_SURFACE ( 3, 1, ( 
 ( #17527, #4435 ),
 ( #18509, #5859 ),
 ( #14112, #8209 ),
 ( #11699, #13225 ) ),
 .UNSPECIFIED., .F., .F., .T. ) 
 B_SPLINE_SURFACE_WITH_KNOTS ( ( 4, 4 ),
 ( 2, 2 ),
 ( 0.000000000000000000, 1.000000000000000000 ),
 ( 0.000000000000000000, 1.000000000000000000 ),
 .UNSPECIFIED. ) 
 GEOMETRIC_REPRESENTATION_ITEM ( )  RATIONAL_B_SPLINE_SURFACE ( (
 ( 1.000000000000000000, 1.000000000000000000),
 ( 0.7792777138730158093, 0.9689936506012928330),
 ( 0.7792777138730158093, 0.9689936506012928330),
 ( 1.000000000000000000, 1.000000000000000000) ) ) 
 REPRESENTATION_ITEM ( '' )  SURFACE ( )  );
#2405=ORIENTED_EDGE ( 'NONE', *, *, #11806, .T. ) ;
#2407=EDGE_CURVE ( 'NONE', #9019, #11032, #3599, .T. ) ;
#2419=CARTESIAN_POINT ( 'NONE',  ( 1.847412631396507576, -3.804043368582581408, -11.84727953344286888 ) ) ;
#2420=CARTESIAN_POINT ( 'NONE',  ( 0.3720661004400040439, 13.34435358167253227, 3.575426119359231603 ) ) ;
#2422=CARTESIAN_POINT ( 'NONE',  ( 0.4862570985993235340, -11.67702470553359539, -7.559321496869553236 ) ) ;
#2427=VERTEX_POINT ( 'NONE', #12386 ) ;
#2428=ORIENTED_EDGE ( 'NONE', *, *, #11183, .T. ) ;
#2430=CARTESIAN_POINT ( 'NONE',  ( 1.846138399168762101, -0.4167076046094680408, -12.43476674860266940 ) ) ;
#2434=DIRECTION ( 'NONE',  ( -0.7635533937278214944, 0.5095610256143914274, -0.3966532189476541514 ) ) ;
#2435=CARTESIAN_POINT ( 'NONE',  ( 0.3095370825347233956, -12.91933430393611104, 4.681152801286112997 ) ) ;
#2436=LINE ( 'NONE', #5579, #11204 ) ;
#2440=ORIENTED_EDGE ( 'NONE', *, *, #14630, .T. ) ;
#2443=EDGE_CURVE ( 'NONE', #11616, #6154, #11463, .T. ) ;
#2446=CARTESIAN_POINT ( 'NONE',  ( 0.4754618798421167414, -11.68486377711971613, 7.564402563418431313 ) ) ;
#2453=CARTESIAN_POINT ( 'NONE',  ( 2.636624412715137922, -15.91454522070252153, 2.161493821597598508 ) ) ;
#2454=CARTESIAN_POINT ( 'NONE',  ( 1.847247051441592625, 3.685275815977189673, 11.88474976472813971 ) ) ;
#2457=CARTESIAN_POINT ( 'NONE',  ( 0.3095370825347233956, 0.4597470195090213041, 13.73357284481724960 ) ) ;
#2468=ADVANCED_FACE ( 'NONE', ( #1091 ), #17534, .F. ) ;
#2469=( BOUNDED_SURFACE ( )  B_SPLINE_SURFACE ( 3, 1, ( 
 ( #991, #11234 ),
 ( #14279, #2420 ),
 ( #5651, #16959 ),
 ( #8270, #6827 ) ),
 .UNSPECIFIED., .F., .F., .T. ) 
 B_SPLINE_SURFACE_WITH_KNOTS ( ( 4, 4 ),
 ( 2, 2 ),
 ( 0.000000000000000000, 1.000000000000000000 ),
 ( 0.000000000000000000, 1.000000000000000000 ),
 .UNSPECIFIED. ) 
 GEOMETRIC_REPRESENTATION_ITEM ( )  RATIONAL_B_SPLINE_SURFACE ( (
 ( 1.000000000000000000, 1.000000000000000000),
 ( 0.9933953342250438912, 0.8357391271907739227),
 ( 0.9933953342250438912, 0.8357391271907739227),
 ( 1.000000000000000000, 1.000000000000000000) ) ) 
 REPRESENTATION_ITEM ( '' )  SURFACE ( )  );
#2471=ORIENTED_EDGE ( 'NONE', *, *, #4755, .T. ) ;
#2474=CARTESIAN_POINT ( 'NONE',  ( 0.4862570985993235340, 13.89016912371017476, 0.7479633556562934604 ) ) ;
#2479=CARTESIAN_POINT ( 'NONE',  ( 16.56679352167444819, -0.004162264567718857756, 0.008311568981097966838 ) ) ;
#2480=CARTESIAN_POINT ( 'NONE',  ( 1.918921323896325193, 6.832782632379378107, 10.48468902844554052 ) ) ;
#2482=CARTESIAN_POINT ( 'NONE',  ( 2.636624412717099908, 11.60464335004051861, -11.10302021258208249 ) ) ;
#2483=CARTESIAN_POINT ( 'NONE',  ( 1.977228804422058728, -14.12033626431055211, 6.152949558601312319 ) ) ;
#2486=LINE ( 'NONE', #15588, #1791 ) ;
#2488=ORIENTED_EDGE ( 'NONE', *, *, #14493, .T. ) ;
#2489=CARTESIAN_POINT ( 'NONE',  ( 0.3142014840576534684, 3.879477880151442015, 13.17932813834296013 ) ) ;
#2492=CARTESIAN_POINT ( 'NONE',  ( 16.57778382496167424, -0.01018821665058785610, 0.01092721432668990016 ) ) ;
#2498=B_SPLINE_CURVE_WITH_KNOTS ( 'NONE', 3,
 ( #10543, #16653, #1944, #16566, #17904, #13400, #6345, #12345, #14832, #696, #3359, #6146, #1749 ),
 .UNSPECIFIED., .F., .F.,
 ( 4, 3, 3, 3, 4 ),
 ( 8.673617379884035472E-19, 0.0002299804304191502627, 0.0004599608082120273944, 0.0006467586077648031012, 0.0008336169836825989407 ),
 .UNSPECIFIED. ) ;
#2501=( BOUNDED_SURFACE ( )  B_SPLINE_SURFACE ( 3, 1, ( 
 ( #2091, #13649 ),
 ( #12302, #5033 ),
 ( #15440, #2257 ),
 ( #9345, #18227 ) ),
 .UNSPECIFIED., .F., .F., .T. ) 
 B_SPLINE_SURFACE_WITH_KNOTS ( ( 4, 4 ),
 ( 2, 2 ),
 ( 0.000000000000000000, 1.000000000000000000 ),
 ( 0.000000000000000000, 1.000000000000000000 ),
 .UNSPECIFIED. ) 
 GEOMETRIC_REPRESENTATION_ITEM ( )  RATIONAL_B_SPLINE_SURFACE ( (
 ( 1.000000000000000000, 1.000000000000000000),
 ( 0.7792777138730158093, 0.9689936506012928330),
 ( 0.7792777138730158093, 0.9689936506012928330),
 ( 1.000000000000000000, 1.000000000000000000) ) ) 
 REPRESENTATION_ITEM ( '' )  SURFACE ( )  );
#2502=( BOUNDED_SURFACE ( )  B_SPLINE_SURFACE ( 3, 1, ( 
 ( #16630, #4591 ),
 ( #14807, #10413 ),
 ( #12240, #7951 ),
 ( #13757, #10709 ) ),
 .UNSPECIFIED., .F., .F., .T. ) 
 B_SPLINE_SURFACE_WITH_KNOTS ( ( 4, 4 ),
 ( 2, 2 ),
 ( 0.000000000000000000, 1.000000000000000000 ),
 ( 0.000000000000000000, 1.000000000000000000 ),
 .UNSPECIFIED. ) 
 GEOMETRIC_REPRESENTATION_ITEM ( )  RATIONAL_B_SPLINE_SURFACE ( (
 ( 1.000000000000000000, 1.000000000000000000),
 ( 0.9933953342250438912, 0.8357391271907739227),
 ( 0.9933953342250438912, 0.8357391271907739227),
 ( 1.000000000000000000, 1.000000000000000000) ) ) 
 REPRESENTATION_ITEM ( '' )  SURFACE ( )  );
#2503=CARTESIAN_POINT ( 'NONE',  ( 0.3137051932979757485, -4.679953077377398074, -12.91601973349275134 ) ) ;
#2510=EDGE_CURVE ( 'NONE', #287, #15231, #12446, .T. ) ;
#2512=EDGE_CURVE ( 'NONE', #885, #14287, #15861, .T. ) ;
#2535=ORIENTED_EDGE ( 'NONE', *, *, #14122, .T. ) ;
#2537=CARTESIAN_POINT ( 'NONE',  ( 1.918921323896324083, -12.08297777410667173, 3.258415356426475729 ) ) ;
#2540=CARTESIAN_POINT ( 'NONE',  ( 1.846138399168762101, -6.971848976710933954, -10.30487220521577818 ) ) ;
#2542=CARTESIAN_POINT ( 'NONE',  ( 1.254009781011253821, 14.24044713813288254, 3.563484327698356324 ) ) ;
#2543=CARTESIAN_POINT ( 'NONE',  ( 1.846138399168762989, 4.238866729160403857, 11.69739621335923729 ) ) ;
#2545=B_SPLINE_CURVE_WITH_KNOTS ( 'NONE', 3,
 ( #15786, #14352, #4232, #1258, #7096, #15880 ),
 .UNSPECIFIED., .F., .F.,
 ( 4, 2, 4 ),
 ( 3.144186300207962859E-18, 0.0002017457492448088553, 0.0004034914984896145664 ),
 .UNSPECIFIED. ) ;
#2550=EDGE_LOOP ( 'NONE', ( #637, #18050, #16118, #16333, #10887, #17674 ) ) ;
#2553=ORIENTED_EDGE ( 'NONE', *, *, #12004, .F. ) ;
#2555=CARTESIAN_POINT ( 'NONE',  ( 1.847372867223026294, -12.44269075185938611, -0.1054171785007791406 ) ) ;
#2556=CARTESIAN_POINT ( 'NONE',  ( 2.636624412714236865, 0.000000000000000000, 0.000000000000000000 ) ) ;
#2560=CARTESIAN_POINT ( 'NONE',  ( 0.3132635586635978409, 13.72732610560088773, -0.5277914263193584921 ) ) ;
#2561=CARTESIAN_POINT ( 'NONE',  ( 1.847034903785822690, 12.44051878787773191, 0.2299360331934612034 ) ) ;
#2568=LINE ( 'NONE', #13868, #15057 ) ;
#2571=B_SPLINE_CURVE_WITH_KNOTS ( 'NONE', 3,
 ( #15859, #5810, #17197, #17482, #1527, #1144 ),
 .UNSPECIFIED., .F., .F.,
 ( 4, 2, 4 ),
 ( 0.000000000000000000, 0.0001828790815886946713, 0.0003657581631773893427 ),
 .UNSPECIFIED. ) ;
#2572=PLANE ( 'NONE',  #2187 ) ;
#2577=( BOUNDED_SURFACE ( )  B_SPLINE_SURFACE ( 3, 1, ( 
 ( #1198, #7036 ),
 ( #1291, #12853 ),
 ( #15621, #11158 ),
 ( #15535, #2435 ) ),
 .UNSPECIFIED., .F., .F., .T. ) 
 B_SPLINE_SURFACE_WITH_KNOTS ( ( 4, 4 ),
 ( 2, 2 ),
 ( 0.000000000000000000, 1.000000000000000000 ),
 ( 0.000000000000000000, 1.000000000000000000 ),
 .UNSPECIFIED. ) 
 GEOMETRIC_REPRESENTATION_ITEM ( )  RATIONAL_B_SPLINE_SURFACE ( (
 ( 1.000000000000000000, 1.000000000000000000),
 ( 0.9933953342250438912, 0.8357391271907739227),
 ( 0.9933953342250438912, 0.8357391271907739227),
 ( 1.000000000000000000, 1.000000000000000000) ) ) 
 REPRESENTATION_ITEM ( '' )  SURFACE ( )  );
#2582=VECTOR ( 'NONE', #12525, 1000.000000000000114 ) ;
#2585=CARTESIAN_POINT ( 'NONE',  ( 0.3145729642390374670, 4.535980493005085989, 12.96842777670208768 ) ) ;
#2586=AXIS2_PLACEMENT_3D ( 'NONE', #13929, #6682, #1015 ) ;
#2587=CARTESIAN_POINT ( 'NONE',  ( 16.58200780006414732, 0.009393638146079845430, -0.006043560077721606832 ) ) ;
#2601=ORIENTED_EDGE ( 'NONE', *, *, #14232, .F. ) ;
#2603=FILL_AREA_STYLE_COLOUR ( '', #2637 ) ;
#2607=CARTESIAN_POINT ( 'NONE',  ( 1.562796894703937678, 0.000000000000000000, 5.000000000000000000 ) ) ;
#2608=EDGE_LOOP ( 'NONE', ( #12969, #10556, #8475, #1564 ) ) ;
#2609=EDGE_CURVE ( 'NONE', #4344, #11616, #13598, .T. ) ;
#2612=CARTESIAN_POINT ( 'NONE',  ( 1.847426409206450959, -2.029922383240494730E-11, 12.44303504652081038 ) ) ;
#2613=CARTESIAN_POINT ( 'NONE',  ( 0.3137051932979809665, 13.20008686438111312, -3.805684345189650042 ) ) ;
#2615=( BOUNDED_SURFACE ( )  B_SPLINE_SURFACE ( 3, 1, ( 
 ( #9616, #17694 ),
 ( #295, #6127 ),
 ( #5670, #4265 ),
 ( #11527, #10084 ) ),
 .UNSPECIFIED., .F., .F., .T. ) 
 B_SPLINE_SURFACE_WITH_KNOTS ( ( 4, 4 ),
 ( 2, 2 ),
 ( 0.000000000000000000, 1.000000000000000000 ),
 ( 0.000000000000000000, 1.000000000000000000 ),
 .UNSPECIFIED. ) 
 GEOMETRIC_REPRESENTATION_ITEM ( )  RATIONAL_B_SPLINE_SURFACE ( (
 ( 1.000000000000000000, 1.000000000000000000),
 ( 0.9593108457356467333, 0.9995965569486454649),
 ( 0.9593108457356467333, 0.9995965569486454649),
 ( 1.000000000000000000, 1.000000000000000000) ) ) 
 REPRESENTATION_ITEM ( '' )  SURFACE ( )  );
#2619=EDGE_CURVE ( 'NONE', #14675, #8361, #3337, .T. ) ;
#2621=VERTEX_POINT ( 'NONE', #15419 ) ;
#2622=ADVANCED_FACE ( 'NONE', ( #11039 ), #590, .F. ) ;
#2627=ORIENTED_EDGE ( 'NONE', *, *, #1071, .F. ) ;
#2632=CARTESIAN_POINT ( 'NONE',  ( 0.3151930723728414985, 8.137566970826528134, -11.07033375389122831 ) ) ;
#2634=CARTESIAN_POINT ( 'NONE',  ( 2.705023505549862151, -12.88681800078730255, -3.294610156756031305 ) ) ;
#2636=EDGE_CURVE ( 'NONE', #471, #6753, #821, .T. ) ;
#2637=COLOUR_RGB ( '', 0.40784314, 0.44705882, 0.49803922) ;
#2644=DIRECTION ( 'NONE',  ( -1.000000000000000000, -0.000000000000000000, -0.000000000000000000 ) ) ;
#2648=CARTESIAN_POINT ( 'NONE',  ( 16.56872352241294521, -0.001821578298043862289, 0.01027347319884366027 ) ) ;
#2650=CARTESIAN_POINT ( 'NONE',  ( 16.56822296793089322, -0.002414375228568327748, 0.009847136207496262617 ) ) ;
#2655=EDGE_LOOP ( 'NONE', ( #16966, #18392, #2535, #3703 ) ) ;
#2656=CARTESIAN_POINT ( 'NONE',  ( 0.3939822652208134768, -3.598529276937167953, -13.34132036472940896 ) ) ;
#2660=CARTESIAN_POINT ( 'NONE',  ( 1.342453679581834924, -9.456403821038877666, 11.38190519890850183 ) ) ;
#2664=CARTESIAN_POINT ( 'NONE',  ( 1.846613052777651198, 12.43780859207240042, -0.3401093050882249558 ) ) ;
#2677=FACE_OUTER_BOUND ( 'NONE', #1853, .T. ) ;
#2681=CARTESIAN_POINT ( 'NONE',  ( 2.636624412715137922, -7.605649742761668719, 14.14563173255331741 ) ) ;
#2686=CARTESIAN_POINT ( 'NONE',  ( 0.4862570985993252548, 5.003653737315486794, 12.97920246947881395 ) ) ;
#2690=CARTESIAN_POINT ( 'NONE',  ( 0.4754618798421167414, 10.80499583390513152, 8.775436892861154803 ) ) ;
#2694=CARTESIAN_POINT ( 'NONE',  ( 1.846138399168762101, -7.646096044339819819, -9.815003036200495856 ) ) ;
#2703=CARTESIAN_POINT ( 'NONE',  ( 3.950837973638676281, -6.316429227969562632, 13.10350451991838128 ) ) ;
#2711=CARTESIAN_POINT ( 'NONE',  ( 0.3145729642390356351, -0.3065092323350255277, -13.73540280162741389 ) ) ;
#2717=ORIENTED_EDGE ( 'NONE', *, *, #16502, .F. ) ;
#2723=CARTESIAN_POINT ( 'NONE',  ( 0.3150692679895986115, 8.199139630396166112, -11.02465386701219252 ) ) ;
#2731=CARTESIAN_POINT ( 'NONE',  ( 0.3137051932979792457, 11.37800749014131263, 7.698472063774513430 ) ) ;
#2734=VERTEX_POINT ( 'NONE', #3669 ) ;
#2735=CARTESIAN_POINT ( 'NONE',  ( 3.950837973638676281, -14.41405733518061716, 1.958075594453740687 ) ) ;
#2739=ORIENTED_EDGE ( 'NONE', *, *, #15084, .T. ) ;
#2745=B_SPLINE_CURVE_WITH_KNOTS ( 'NONE', 3,
 ( #5075, #5357, #12437, #6713 ),
 .UNSPECIFIED., .F., .F.,
 ( 4, 4 ),
 ( 7.039312503357838248E-16, 0.002004993803841917561 ),
 .UNSPECIFIED. ) ;
#2748=DIRECTION ( 'NONE',  ( 0.7561779333270775005, -0.6534392409364819798, -0.03481510524965015368 ) ) ;
#2749=CARTESIAN_POINT ( 'NONE',  ( 0.3145729642390375225, -4.535980493005000724, -12.96842777670211611 ) ) ;
#2750=CARTESIAN_POINT ( 'NONE',  ( 1.846955891736114852, 12.44001089941741611, -0.2634721419535633880 ) ) ;
#2763=CARTESIAN_POINT ( 'NONE',  ( 0.3151926232592464627, -13.09050869763090219, -4.172630140040936908 ) ) ;
#2765=CARTESIAN_POINT ( 'NONE',  ( 16.56822296793089322, -0.003834730849371946210, -0.009385634690642043892 ) ) ;
#2768=ORIENTED_EDGE ( 'NONE', *, *, #12213, .F. ) ;
#2772=CARTESIAN_POINT ( 'NONE',  ( 0.4862570985993235340, -13.89016912371016943, -0.7479633556563904939 ) ) ;
#2773=CARTESIAN_POINT ( 'NONE',  ( 1.562796894703937678, 0.000000000000000000, 0.000000000000000000 ) ) ;
#2778=CARTESIAN_POINT ( 'NONE',  ( 2.002547531651519996, -12.17374746633580784, 3.242439124566603326 ) ) ;
#2785=LINE ( 'NONE', #9776, #7864 ) ;
#2790=CARTESIAN_POINT ( 'NONE',  ( 16.56753206892534891, 0.008432171035096448775, -0.004368917149005366145 ) ) ;
#2795=CARTESIAN_POINT ( 'NONE',  ( 0.3137051932979792457, -8.442169467526928983, 10.83767969834800127 ) ) ;
#2800=CARTESIAN_POINT ( 'NONE',  ( 0.3151926232592482946, -13.04305446098359056, 4.318679262939574492 ) ) ;
#2801=CARTESIAN_POINT ( 'NONE',  ( 16.56782317627811096, -0.009439921864426870785, 0.002708056627498742989 ) ) ;
#2813=EDGE_LOOP ( 'NONE', ( #12751, #16140 ) ) ;
#2821=CARTESIAN_POINT ( 'NONE',  ( 2.123976203522053297, 14.31368049382969687, 6.261444813538606269 ) ) ;
#2822=CARTESIAN_POINT ( 'NONE',  ( 16.56822296793089322, 0.009847136207495308519, -0.002414375228568875487 ) ) ;
#2829=CARTESIAN_POINT ( 'NONE',  ( 16.58200780006414732, 0.01080144354108992025, -0.002844973367390922145 ) ) ;
#2832=CARTESIAN_POINT ( 'NONE',  ( 2.002547531651519996, 3.242439124566821818, -12.17374746633574745 ) ) ;
#2837=CARTESIAN_POINT ( 'NONE',  ( 16.58200780006414732, -0.01115192838421568723, -0.0006320991582349211584 ) ) ;
#2839=CARTESIAN_POINT ( 'NONE',  ( 1.847412631396503579, 12.44294644888238999, 0.04315047898439477309 ) ) ;
#2843=DIRECTION ( 'NONE',  ( 0.000000000000000000, 0.000000000000000000, 1.000000000000000000 ) ) ;
#2845=AXIS2_PLACEMENT_3D ( 'NONE', #3105, #14681, #10686 ) ;
#2849=CARTESIAN_POINT ( 'NONE',  ( 2.636624412714994037, -14.46769361191274328, -6.973567714907344950 ) ) ;
#2853=EDGE_CURVE ( 'NONE', #14774, #9063, #7865, .T. ) ;
#2859=CARTESIAN_POINT ( 'NONE',  ( 0.3095370825347224519, 13.20347358821914519, 3.806662003783459092 ) ) ;
#2866=ORIENTED_EDGE ( 'NONE', *, *, #1916, .F. ) ;
#2867=B_SPLINE_CURVE_WITH_KNOTS ( 'NONE', 3,
 ( #6900, #18641, #6999, #10139 ),
 .UNSPECIFIED., .F., .F.,
 ( 4, 4 ),
 ( 1.582786644015060892E-17, 0.003005512676784847896 ),
 .UNSPECIFIED. ) ;
#2870=CARTESIAN_POINT ( 'NONE',  ( 2.123976203522053741, 15.54801196254787143, -1.531817366691807125 ) ) ;
#2875=CARTESIAN_POINT ( 'NONE',  ( 3.664313757352975820, -10.50730552161225972, -9.645155442698879256 ) ) ;
#2880=ORIENTED_EDGE ( 'NONE', *, *, #18640, .T. ) ;
#2881=CARTESIAN_POINT ( 'NONE',  ( 0.4754618798421171855, -10.80499583390519192, 8.775436892861074867 ) ) ;
#2884=ORIENTED_EDGE ( 'NONE', *, *, #17544, .F. ) ;
#2888=EDGE_CURVE ( 'NONE', #257, #16346, #7205, .T. ) ;
#2889=AXIS2_PLACEMENT_3D ( 'NONE', #9128, #3482, #10854 ) ;
#2894=CARTESIAN_POINT ( 'NONE',  ( 0.3137051932979792457, 7.698472063774471685, 11.37800749014133928 ) ) ;
#2897=VERTEX_POINT ( 'NONE', #1069 ) ;
#2901=ORIENTED_EDGE ( 'NONE', *, *, #373, .F. ) ;
#2903=LINE ( 'NONE', #7339, #14750 ) ;
#2904=CARTESIAN_POINT ( 'NONE',  ( 1.845756295923363099, -0.4783934145701149721, -12.43231724724606835 ) ) ;
#2905=CARTESIAN_POINT ( 'NONE',  ( 1.254255976357087521, 11.25336128106905420, 9.426444230096484134 ) ) ;
#2907=CARTESIAN_POINT ( 'NONE',  ( 3.950837973638675393, -14.31366178983251380, -2.591948120961955926 ) ) ;
#2911=ADVANCED_FACE ( 'NONE', ( #15509 ), #5378, .T. ) ;
#2913=CARTESIAN_POINT ( 'NONE',  ( 16.57778382496167424, 0.01354073047775893567, -0.006312874906843913766 ) ) ;
#2915=DIRECTION ( 'NONE',  ( 1.000000000000000000, 0.000000000000000000, 0.000000000000000000 ) ) ;
#2916=CARTESIAN_POINT ( 'NONE',  ( 0.8740779401508875779, -3.609949156401464965, 13.83508928787437142 ) ) ;
#2920=CARTESIAN_POINT ( 'NONE',  ( 1.846822687350019088, 7.075150813727119292, 10.23524390843941845 ) ) ;
#2921=ORIENTED_EDGE ( 'NONE', *, *, #4580, .F. ) ;
#2927=VERTEX_POINT ( 'NONE', #10804 ) ;
#2944=ADVANCED_FACE ( 'NONE', ( #16350 ), #2502, .F. ) ;
#2952=ORIENTED_EDGE ( 'NONE', *, *, #922, .F. ) ;
#2953=CARTESIAN_POINT ( 'NONE',  ( 2.002547531651519996, 12.17374746633578475, 3.242439124566693476 ) ) ;
#2955=CARTESIAN_POINT ( 'NONE',  ( 16.56753206892534891, -0.008432171035096412345, -0.004368917149004214288 ) ) ;
#2960=CARTESIAN_POINT ( 'NONE',  ( 0.4754618798421162973, 7.564402563418467729, 11.68486377711969304 ) ) ;
#2963=DIRECTION ( 'NONE',  ( -1.000000000000000000, -0.000000000000000000, -0.000000000000000000 ) ) ;
#2964=B_SPLINE_CURVE_WITH_KNOTS ( 'NONE', 3,
 ( #15830, #5502, #8854, #2905, #11724, #16123 ),
 .UNSPECIFIED., .F., .F.,
 ( 4, 2, 4 ),
 ( 0.000000000000000000, 0.001656992708821599649, 0.003313985417643199299 ),
 .UNSPECIFIED. ) ;
#2966=DIRECTION ( 'NONE',  ( 0.000000000000000000, 0.000000000000000000, -1.000000000000000000 ) ) ;
#2967=CARTESIAN_POINT ( 'NONE',  ( 0.3939875929385612263, 10.75308190953755982, -8.678227324501007089 ) ) ;
#2970=CARTESIAN_POINT ( 'NONE',  ( 0.3720661004400040439, -4.951033743989553315, -12.89739157014198057 ) ) ;
#2973=ORIENTED_EDGE ( 'NONE', *, *, #875, .F. ) ;
#2974=CARTESIAN_POINT ( 'NONE',  ( 1.861706995891667882, 4.359009869687244354, 11.66987142852985748 ) ) ;
#2975=CARTESIAN_POINT ( 'NONE',  ( 16.56679352167444819, 0.006526964904752344775, -0.006618561353600113835 ) ) ;
#2977=ADVANCED_FACE ( 'NONE', ( #6312 ), #4479, .F. ) ;
#2978=EDGE_LOOP ( 'NONE', ( #8962, #14482, #14596, #6626 ) ) ;
#2979=FACE_OUTER_BOUND ( 'NONE', #18901, .T. ) ;
#2982=ORIENTED_EDGE ( 'NONE', *, *, #3153, .T. ) ;
#2991=CARTESIAN_POINT ( 'NONE',  ( 0.4754618798421171855, 3.583352865732860604, -13.45049478164055756 ) ) ;
#2993=CARTESIAN_POINT ( 'NONE',  ( 16.58200780006414732, -0.002844973367390960309, -0.01080144354108991157 ) ) ;
#2996=CARTESIAN_POINT ( 'NONE',  ( 1.846138399168762101, -6.971848976710933954, -10.30487220521577818 ) ) ;
#2997=ORIENTED_EDGE ( 'NONE', *, *, #3840, .T. ) ;
#3002=CARTESIAN_POINT ( 'NONE',  ( 1.861628059977343597, -9.751736252960316875, -7.751680370225499495 ) ) ;
#3003=CARTESIAN_POINT ( 'NONE',  ( 2.320521194583477165, -6.542541239686160637, -14.32454473829993447 ) ) ;
#3004=CARTESIAN_POINT ( 'NONE',  ( 3.950837973638677170, -1.958075594453692503, -14.41405733518062959 ) ) ;
#3006=CARTESIAN_POINT ( 'NONE',  ( 3.377929128793393687, 1.296196549818942501, 13.92579934231096317 ) ) ;
#3007=DIRECTION ( 'NONE',  ( -0.7635533937278216055, 0.1790966170214010056, -0.6204116510013458763 ) ) ;
#3008=DIRECTION ( 'NONE',  ( -0.7635533937278216055, 0.02138673900301891681, 0.6453904417649388714 ) ) ;
#3010=CARTESIAN_POINT ( 'NONE',  ( 2.636624412715435462, -15.80357026013316712, -2.862162146983298516 ) ) ;
#3012=CARTESIAN_POINT ( 'NONE',  ( 2.636624412714242194, 14.46769361191244485, 6.973567714906650394 ) ) ;
#3014=CARTESIAN_POINT ( 'NONE',  ( 16.57605080000000086, 6.799999999999999822, 1.500000000000000000 ) ) ;
#3021=ORIENTED_EDGE ( 'NONE', *, *, #3475, .T. ) ;
#3029=VERTEX_POINT ( 'NONE', #16999 ) ;
#3031=CARTESIAN_POINT ( 'NONE',  ( 0.3151926232592538457, -4.318679262939536301, -13.04305446098360122 ) ) ;
#3037=ORIENTED_EDGE ( 'NONE', *, *, #4714, .T. ) ;
#3038=B_SPLINE_CURVE_WITH_KNOTS ( 'NONE', 3,
 ( #12645, #5387, #17050, #6921 ),
 .UNSPECIFIED., .F., .F.,
 ( 4, 4 ),
 ( 1.684670163748776910E-17, 0.003005512676784852233 ),
 .UNSPECIFIED. ) ;
#3039=CARTESIAN_POINT ( 'NONE',  ( 3.950837973638675393, 2.591948120961804936, 14.31366178983254578 ) ) ;
#3040=CARTESIAN_POINT ( 'NONE',  ( 0.3151926232592474064, 0.07678256780557664307, 13.73922722301401578 ) ) ;
#3042=EDGE_CURVE ( 'NONE', #17275, #4049, #9930, .T. ) ;
#3043=CARTESIAN_POINT ( 'NONE',  ( 0.3095370825347224519, -0.4597470195089233824, -13.73357284481725316 ) ) ;
#3044=EDGE_CURVE ( 'NONE', #16174, #17311, #10874, .T. ) ;
#3047=ORIENTED_EDGE ( 'NONE', *, *, #13523, .F. ) ;
#3052=CARTESIAN_POINT ( 'NONE',  ( 2.353870697619111496, 8.216087327473076130, -10.00946331859655203 ) ) ;
#3060=CARTESIAN_POINT ( 'NONE',  ( 16.58200780006414732, 0.006043560077721710048, -0.009393638146078546122 ) ) ;
#3061=CARTESIAN_POINT ( 'NONE',  ( 3.950837973638668288, 0.000000000000000000, 0.000000000000000000 ) ) ;
#3062=CARTESIAN_POINT ( 'NONE',  ( 2.353870697619109720, 10.90705766126230536, -6.980654702310723714 ) ) ;
#3064=ORIENTED_EDGE ( 'NONE', *, *, #7041, .F. ) ;
#3078=( BOUNDED_SURFACE ( )  B_SPLINE_SURFACE ( 3, 1, ( 
 ( #7423, #17835 ),
 ( #7328, #1675 ),
 ( #13141, #51 ),
 ( #2993, #13234 ) ),
 .UNSPECIFIED., .F., .F., .T. ) 
 B_SPLINE_SURFACE_WITH_KNOTS ( ( 4, 4 ),
 ( 2, 2 ),
 ( 0.000000000000000000, 1.000000000000000000 ),
 ( 0.000000000000000000, 1.000000000000000000 ),
 .UNSPECIFIED. ) 
 GEOMETRIC_REPRESENTATION_ITEM ( )  RATIONAL_B_SPLINE_SURFACE ( (
 ( 1.000000000000000000, 1.000000000000000000),
 ( 0.7792777138730160313, 0.9689936506012927220),
 ( 0.7792777138730160313, 0.9689936506012927220),
 ( 1.000000000000000000, 1.000000000000000000) ) ) 
 REPRESENTATION_ITEM ( '' )  SURFACE ( )  );
#3081=CARTESIAN_POINT ( 'NONE',  ( 3.950837973638668288, 0.000000000000000000, 0.000000000000000000 ) ) ;
#3083=CARTESIAN_POINT ( 'NONE',  ( 16.56872352241294521, 0.007240717549633888563, 0.007512283835804339609 ) ) ;
#3085=ORIENTED_EDGE ( 'NONE', *, *, #8316, .F. ) ;
#3086=EDGE_CURVE ( 'NONE', #9019, #4326, #3904, .T. ) ;
#3098=EDGE_LOOP ( 'NONE', ( #15137, #11889, #11163, #16800 ) ) ;
#3099=ORIENTED_EDGE ( 'NONE', *, *, #13998, .T. ) ;
#3102=FACE_OUTER_BOUND ( 'NONE', #9668, .T. ) ;
#3105=CARTESIAN_POINT ( 'NONE',  ( 2.636624412714236865, 0.000000000000000000, 0.000000000000000000 ) ) ;
#3106=CYLINDRICAL_SURFACE ( 'NONE', #3645, 5.000000000000000000 ) ;
#3108=VECTOR ( 'NONE', #3705, 1000.000000000000000 ) ;
#3111=CARTESIAN_POINT ( 'NONE',  ( 0.3137051932979757485, -11.37800749014125223, -7.698472063774596030 ) ) ;
#3116=( BOUNDED_SURFACE ( )  B_SPLINE_SURFACE ( 3, 1, ( 
 ( #18559, #5461 ),
 ( #802, #9848 ),
 ( #18288, #15684 ),
 ( #2587, #1167 ) ),
 .UNSPECIFIED., .F., .F., .T. ) 
 B_SPLINE_SURFACE_WITH_KNOTS ( ( 4, 4 ),
 ( 2, 2 ),
 ( 0.000000000000000000, 1.000000000000000000 ),
 ( 0.000000000000000000, 1.000000000000000000 ),
 .UNSPECIFIED. ) 
 GEOMETRIC_REPRESENTATION_ITEM ( )  RATIONAL_B_SPLINE_SURFACE ( (
 ( 1.000000000000000000, 1.000000000000000000),
 ( 0.7792777138730160313, 0.9689936506012927220),
 ( 0.7792777138730160313, 0.9689936506012927220),
 ( 1.000000000000000000, 1.000000000000000000) ) ) 
 REPRESENTATION_ITEM ( '' )  SURFACE ( )  );
#3119=APPLICATION_CONTEXT ( 'automotive_design' ) ;
#3125=CARTESIAN_POINT ( 'NONE',  ( 0.8740779401510754276, -9.070947476926809472, -11.05257166392059354 ) ) ;
#3132=CARTESIAN_POINT ( 'NONE',  ( 1.977436885025100510, 3.321781585409006698, 15.04044112860174209 ) ) ;
#3133=EDGE_CURVE ( 'NONE', #5702, #15056, #4013, .T. ) ;
#3134=CARTESIAN_POINT ( 'NONE',  ( 0.3148213771069380829, 12.99360322443203053, 4.463459503829039221 ) ) ;
#3141=DIRECTION ( 'NONE',  ( -0.7561779333270775005, -0.4122479608995667788, -0.5081796452863290847 ) ) ;
#3142=AXIS2_PLACEMENT_3D ( 'NONE', #18873, #11618, #4642 ) ;
#3153=EDGE_CURVE ( 'NONE', #10713, #13922, #15202, .T. ) ;
#3155=EDGE_CURVE ( 'NONE', #2315, #15773, #4666, .T. ) ;
#3160=CARTESIAN_POINT ( 'NONE',  ( 3.512766787570714477, -14.81029789862161117, -2.682019731918549255 ) ) ;
#3161=CARTESIAN_POINT ( 'NONE',  ( 16.57210152137263393, -0.003862718596009374894, -0.01402404281922920576 ) ) ;
#3162=CARTESIAN_POINT ( 'NONE',  ( 16.57778382496167424, -0.006312874906843772387, 0.01354073047775764503 ) ) ;
#3164=CARTESIAN_POINT ( 'NONE',  ( 16.57210152137263393, 0.0006600038696347836076, 0.01453130299868640209 ) ) ;
#3170=CARTESIAN_POINT ( 'NONE',  ( 0.3150686449036038117, 11.02450593298030412, -8.199336701264417826 ) ) ;
#3172=ORIENTED_EDGE ( 'NONE', *, *, #8065, .F. ) ;
#3173=CARTESIAN_POINT ( 'NONE',  ( 0.4754618798421162973, 5.007009103465432709, -12.98792082933639058 ) ) ;
#3174=EDGE_LOOP ( 'NONE', ( #4378, #7091, #14507, #18389 ) ) ;
#3175=CARTESIAN_POINT ( 'NONE',  ( 1.846524061778019199, 10.27028962889607477, -7.023652644192158512 ) ) ;
#3177=CARTESIAN_POINT ( 'NONE',  ( 3.074695600507123761, 2.093687500612191776, -15.41438262616238575 ) ) ;
#3181=VECTOR ( 'NONE', #11726, 1000.000000000000000 ) ;
#3186=CARTESIAN_POINT ( 'NONE',  ( 16.58200780006414732, 0.01041078477703982763, -0.004047297414157931088 ) ) ;
#3189=CARTESIAN_POINT ( 'NONE',  ( 1.847412631396500693, -11.82061107079961992, -3.886120457021520647 ) ) ;
#3191=VERTEX_POINT ( 'NONE', #1407 ) ;
#3195=VERTEX_POINT ( 'NONE', #1306 ) ;
#3196=( BOUNDED_SURFACE ( )  B_SPLINE_SURFACE ( 3, 1, ( 
 ( #5197, #7488 ),
 ( #8719, #16176 ),
 ( #7203, #14641 ),
 ( #11681, #6050 ) ),
 .UNSPECIFIED., .F., .F., .T. ) 
 B_SPLINE_SURFACE_WITH_KNOTS ( ( 4, 4 ),
 ( 2, 2 ),
 ( 0.000000000000000000, 1.000000000000000000 ),
 ( 0.000000000000000000, 1.000000000000000000 ),
 .UNSPECIFIED. ) 
 GEOMETRIC_REPRESENTATION_ITEM ( )  RATIONAL_B_SPLINE_SURFACE ( (
 ( 1.000000000000000000, 1.000000000000000000),
 ( 0.9593108457356467333, 0.9995965569486454649),
 ( 0.9593108457356467333, 0.9995965569486454649),
 ( 1.000000000000000000, 1.000000000000000000) ) ) 
 REPRESENTATION_ITEM ( '' )  SURFACE ( )  );
#3199=CONICAL_SURFACE ( 'NONE', #3536, 16.06066017081991149, 0.7853981625000062694 ) ;
#3201=CARTESIAN_POINT ( 'NONE',  ( 0.4862570985993235340, -3.580942890621579444, -13.44146924561384537 ) ) ;
#3202=CARTESIAN_POINT ( 'NONE',  ( 3.950837973638676281, 12.81214529934975310, 6.888253895133341409 ) ) ;
#3204=CARTESIAN_POINT ( 'NONE',  ( 16.58200780006414732, 0.007066318000006001528, -0.008650561019685833880 ) ) ;
#3207=CARTESIAN_POINT ( 'NONE',  ( 1.861706995891666550, -4.359009869687166194, -11.66987142852988946 ) ) ;
#3210=LINE ( 'NONE', #3014, #7055 ) ;
#3211=EDGE_CURVE ( 'NONE', #11605, #8961, #1117, .T. ) ;
#3213=CARTESIAN_POINT ( 'NONE',  ( 1.847461586945728707, 7.341074796295939286, 10.04711372545047254 ) ) ;
#3216=EDGE_CURVE ( 'NONE', #14389, #9064, #18605, .T. ) ;
#3220=CARTESIAN_POINT ( 'NONE',  ( 1.847372867223024961, -7.228345833872678483, -10.12831093686730100 ) ) ;
#3224=CARTESIAN_POINT ( 'NONE',  ( 0.3095370825347233956, 4.681152801286161846, 12.91933430393609683 ) ) ;
#3226=ORIENTED_EDGE ( 'NONE', *, *, #6065, .F. ) ;
#3239=CARTESIAN_POINT ( 'NONE',  ( 0.4862570985993252548, 11.67702470553365401, 7.559321496869467971 ) ) ;
#3245=ADVANCED_FACE ( 'NONE', ( #17561 ), #1820, .T. ) ;
#3252=CARTESIAN_POINT ( 'NONE',  ( 8.438534575730034959, -1.899950616255234870, 6.598402093327873530 ) ) ;
#3253=CARTESIAN_POINT ( 'NONE',  ( 0.3137051932979757485, 13.73004976592202020, -0.4596302728640235258 ) ) ;
#3255=CARTESIAN_POINT ( 'NONE',  ( 16.57605080000000086, 0.000000000000000000, 0.000000000000000000 ) ) ;
#3256=CARTESIAN_POINT ( 'NONE',  ( 1.977436885026283564, -11.52792723756319582, -10.21547824869606202 ) ) ;
#3261=CARTESIAN_POINT ( 'NONE',  ( 3.950837973638675393, 6.888253895133479965, -12.81214529934967672 ) ) ;
#3262=CARTESIAN_POINT ( 'NONE',  ( 0.3150686449036065317, 11.20479228691397822, 7.951193823202440392 ) ) ;
#3264=CARTESIAN_POINT ( 'NONE',  ( 0.3095370825347224519, -7.700448427571953580, 11.38092634279625770 ) ) ;
#3266=ORIENTED_EDGE ( 'NONE', *, *, #12410, .T. ) ;
#3272=ADVANCED_FACE ( 'NONE', ( #10488 ), #2139, .T. ) ;
#3273=ORIENTED_EDGE ( 'NONE', *, *, #12565, .F. ) ;
#3274=DIRECTION ( 'NONE',  ( -0.7635533937278214944, 0.3620487483322560873, -0.5347026451755899634 ) ) ;
#3280=CARTESIAN_POINT ( 'NONE',  ( 0.3939822652208125331, -13.34132036472939831, 3.598529276937210142 ) ) ;
#3292=ADVANCED_FACE ( 'NONE', ( #361 ), #15681, .F. ) ;
#3294=EDGE_CURVE ( 'NONE', #5775, #4723, #18331, .T. ) ;
#3296=B_SPLINE_CURVE_WITH_KNOTS ( 'NONE', 3,
 ( #13885, #12456, #15592, #14075, #12733, #3758 ),
 .UNSPECIFIED., .F., .F.,
 ( 4, 2, 4 ),
 ( 1.939479807224432123E-18, 0.001657017934711440621, 0.003314035869422879074 ),
 .UNSPECIFIED. ) ;
#3297=ORIENTED_EDGE ( 'NONE', *, *, #3555, .F. ) ;
#3299=B_SPLINE_CURVE_WITH_KNOTS ( 'NONE', 3,
 ( #16121, #4652, #3002, #159, #11821, #14965 ),
 .UNSPECIFIED., .F., .F.,
 ( 4, 2, 4 ),
 ( 8.940560153363745023E-19, 0.0001828790815886946442, 0.0003657581631773883669 ),
 .UNSPECIFIED. ) ;
#3300=EDGE_CURVE ( 'NONE', #10695, #9114, #18797, .T. ) ;
#3301=DIRECTION ( 'NONE',  ( 0.7561779333270773895, 0.2350349629540228469, -0.6106991889125047424 ) ) ;
#3302=EDGE_CURVE ( 'NONE', #15569, #3029, #11735, .T. ) ;
#3311=CARTESIAN_POINT ( 'NONE',  ( 2.636624412714237309, 11.10302021257826866, 11.60464335004050973 ) ) ;
#3315=CARTESIAN_POINT ( 'NONE',  ( 1.846138399168762101, 7.646096044339892650, 9.815003036200437236 ) ) ;
#3317=( BOUNDED_SURFACE ( )  B_SPLINE_SURFACE ( 3, 1, ( 
 ( #14236, #8503 ),
 ( #8592, #7267 ),
 ( #1140, #12982 ),
 ( #12332, #1524 ) ),
 .UNSPECIFIED., .F., .F., .T. ) 
 B_SPLINE_SURFACE_WITH_KNOTS ( ( 4, 4 ),
 ( 2, 2 ),
 ( 0.000000000000000000, 1.000000000000000000 ),
 ( 0.000000000000000000, 1.000000000000000000 ),
 .UNSPECIFIED. ) 
 GEOMETRIC_REPRESENTATION_ITEM ( )  RATIONAL_B_SPLINE_SURFACE ( (
 ( 1.000000000000000000, 1.000000000000000000),
 ( 0.9933953342250438912, 0.8357391271907739227),
 ( 0.9933953342250438912, 0.8357391271907739227),
 ( 1.000000000000000000, 1.000000000000000000) ) ) 
 REPRESENTATION_ITEM ( '' )  SURFACE ( )  );
#3318=ORIENTED_EDGE ( 'NONE', *, *, #9650, .T. ) ;
#3320=VERTEX_POINT ( 'NONE', #13252 ) ;
#3321=CARTESIAN_POINT ( 'NONE',  ( 1.977228804423517117, 14.12033626431153444, -6.152949558602713864 ) ) ;
#3325=CARTESIAN_POINT ( 'NONE',  ( 1.254009781011991453, -9.426200207651724838, -11.25324419414228494 ) ) ;
#3327=CARTESIAN_POINT ( 'NONE',  ( 3.950837973638677170, 12.81214529934985080, -6.888253895133152227 ) ) ;
#3334=VECTOR ( 'NONE', #8773, 1000.000000000000000 ) ;
#3336=CARTESIAN_POINT ( 'NONE',  ( 2.697797270744666243, -13.26309265156976558, -0.9169917281808652731 ) ) ;
#3337=B_SPLINE_CURVE_WITH_KNOTS ( 'NONE', 3,
 ( #3761, #18379, #9587, #6736 ),
 .UNSPECIFIED., .F., .F.,
 ( 4, 4 ),
 ( 0.000000000000000000, 0.002004993803842607548 ),
 .UNSPECIFIED. ) ;
#3339=EDGE_CURVE ( 'NONE', #18321, #5518, #1477, .T. ) ;
#3344=CARTESIAN_POINT ( 'NONE',  ( 0.4385251269669978025, 12.93791070501034390, 4.978066129061732070 ) ) ;
#3345=B_SPLINE_CURVE_WITH_KNOTS ( 'NONE', 3,
 ( #264, #13641, #12016, #16518, #16220, #14971 ),
 .UNSPECIFIED., .F., .F.,
 ( 4, 2, 4 ),
 ( 5.421010862427522170E-19, 0.0001825746017570591031, 0.0003651492035141176641 ),
 .UNSPECIFIED. ) ;
#3348=CARTESIAN_POINT ( 'NONE',  ( 16.56679352167444819, 0.008252760440870499439, 0.004277682826582289259 ) ) ;
#3351=CARTESIAN_POINT ( 'NONE',  ( 0.4862570985993252548, -5.003653737315580052, 12.97920246947877665 ) ) ;
#3352=CARTESIAN_POINT ( 'NONE',  ( 1.342453679581834924, -14.76648944001038544, -0.9602753779832271519 ) ) ;
#3356=ADVANCED_FACE ( 'NONE', ( #15361 ), #8378, .F. ) ;
#3357=ORIENTED_EDGE ( 'NONE', *, *, #11407, .T. ) ;
#3359=CARTESIAN_POINT ( 'NONE',  ( 1.846822687350018644, -10.23524390843944687, 7.075150813727085541 ) ) ;
#3363=ORIENTED_EDGE ( 'NONE', *, *, #2609, .F. ) ;
#3365=ADVANCED_FACE ( 'NONE', ( #13930 ), #17655, .F. ) ;
#3372=ORIENTED_EDGE ( 'NONE', *, *, #13975, .F. ) ;
#3374=ORIENTED_EDGE ( 'NONE', *, *, #8392, .F. ) ;
#3375=CARTESIAN_POINT ( 'NONE',  ( 16.56872352241294521, 0.007240717549633888563, 0.007512283835804339609 ) ) ;
#3380=CARTESIAN_POINT ( 'NONE',  ( 2.636624412714236865, 0.000000000000000000, 0.000000000000000000 ) ) ;
#3381=ADVANCED_FACE ( 'NONE', ( #5047 ), #18269, .F. ) ;
#3387=CARTESIAN_POINT ( 'NONE',  ( 0.4384471787762797002, 3.577367180593735263, -13.39294437382614333 ) ) ;
#3400=CARTESIAN_POINT ( 'NONE',  ( 0.3095370825347234511, -7.700448427571787491, -11.38092634279637139 ) ) ;
#3403=ORIENTED_EDGE ( 'NONE', *, *, #9073, .T. ) ;
#3404=CARTESIAN_POINT ( 'NONE',  ( 1.861628059977341154, -12.44564375541077084, -0.5393144007391572625 ) ) ;
#3405=CARTESIAN_POINT ( 'NONE',  ( 0.8740779401508861346, -7.708543377337782054, 12.04241618260063618 ) ) ;
#3406=CARTESIAN_POINT ( 'NONE',  ( 0.3058872367615226295, -8.562166468153792565, 10.75034008168912791 ) ) ;
#3409=CARTESIAN_POINT ( 'NONE',  ( 0.8740764193768004731, -5.211550415969136374, 13.31469591265773289 ) ) ;
#3411=CARTESIAN_POINT ( 'NONE',  ( 2.002547531651519996, -11.75462648437098601, -4.532360870844453160 ) ) ;
#3412=EDGE_CURVE ( 'NONE', #4344, #8099, #2364, .T. ) ;
#3421=CARTESIAN_POINT ( 'NONE',  ( 1.847034903785819360, -7.126331315909195219, -10.19974412751572679 ) ) ;
#3422=DIRECTION ( 'NONE',  ( 0.000000000000000000, 0.000000000000000000, 1.000000000000000000 ) ) ;
#3424=CARTESIAN_POINT ( 'NONE',  ( 16.56872352241294521, 0.004907101719994633009, -0.009207754980063766539 ) ) ;
#3425=CARTESIAN_POINT ( 'NONE',  ( 2.636624412714292376, 11.60464335004048309, 11.10302021257707850 ) ) ;
#3426=ORIENTED_EDGE ( 'NONE', *, *, #4017, .T. ) ;
#3427=CARTESIAN_POINT ( 'NONE',  ( 1.847380140988739594, -3.740232970470839913, 11.86779270755357807 ) ) ;
#3430=B_SPLINE_CURVE_WITH_KNOTS ( 'NONE', 3,
 ( #3484, #16771, #1872, #7995, #4836, #13620 ),
 .UNSPECIFIED., .F., .F.,
 ( 4, 2, 4 ),
 ( 0.000000000000000000, 0.001500839035891553090, 0.003001678071783106180 ),
 .UNSPECIFIED. ) ;
#3434=( BOUNDED_SURFACE ( )  B_SPLINE_SURFACE ( 3, 1, ( 
 ( #5843, #3264 ),
 ( #6149, #7397 ),
 ( #7302, #13497 ),
 ( #9200, #10348 ) ),
 .UNSPECIFIED., .F., .F., .T. ) 
 B_SPLINE_SURFACE_WITH_KNOTS ( ( 4, 4 ),
 ( 2, 2 ),
 ( 0.000000000000000000, 1.000000000000000000 ),
 ( 0.000000000000000000, 1.000000000000000000 ),
 .UNSPECIFIED. ) 
 GEOMETRIC_REPRESENTATION_ITEM ( )  RATIONAL_B_SPLINE_SURFACE ( (
 ( 1.000000000000000000, 1.000000000000000000),
 ( 0.9593108457356467333, 0.9995965569486454649),
 ( 0.9593108457356467333, 0.9995965569486454649),
 ( 1.000000000000000000, 1.000000000000000000) ) ) 
 REPRESENTATION_ITEM ( '' )  SURFACE ( )  );
#3435=ORIENTED_EDGE ( 'NONE', *, *, #5415, .T. ) ;
#3437=CARTESIAN_POINT ( 'NONE',  ( 16.56872352241294521, 0.009382111268607367521, 0.004564908236399998868 ) ) ;
#3439=CARTESIAN_POINT ( 'NONE',  ( 16.56679352167444819, -0.008311568981098013675, -0.004162264567718770153 ) ) ;
#3446=CARTESIAN_POINT ( 'NONE',  ( 3.074695600507442172, 6.754521329824937581, 14.01296402267882435 ) ) ;
#3450=CARTESIAN_POINT ( 'NONE',  ( 0.3150692679895987780, 13.73846569174797061, 0.1531143455845020152 ) ) ;
#3453=ORIENTED_EDGE ( 'NONE', *, *, #16965, .T. ) ;
#3454=EDGE_CURVE ( 'NONE', #10942, #7454, #3977, .T. ) ;
#3459=EDGE_CURVE ( 'NONE', #16368, #9780, #9473, .T. ) ;
#3464=CARTESIAN_POINT ( 'NONE',  ( 16.56872352241294521, -0.009382111268607402216, -0.004564908236399935551 ) ) ;
#3465=CARTESIAN_POINT ( 'NONE',  ( 0.4862570985993235340, -13.89016912371016943, -0.7479633556563904939 ) ) ;
#3466=CARTESIAN_POINT ( 'NONE',  ( 0.4862570985993235340, 7.559321496869426227, 11.67702470553367711 ) ) ;
#3471=DIRECTION ( 'NONE',  ( 0.7561779333270775005, 0.6534392409364817578, 0.03481510524965471948 ) ) ;
#3473=CIRCLE ( 'NONE', #15071, 14.54644660717763927 ) ;
#3474=DIRECTION ( 'NONE',  ( 0.000000000000000000, 0.000000000000000000, 1.000000000000000000 ) ) ;
#3475=EDGE_CURVE ( 'NONE', #8324, #15452, #10593, .T. ) ;
#3476=LINE ( 'NONE', #13510, #15540 ) ;
#3478=CARTESIAN_POINT ( 'NONE',  ( 0.3151928476913592458, -13.73922860838471749, 0.0002082997483299325046 ) ) ;
#3482=DIRECTION ( 'NONE',  ( -1.000000000000000000, -0.000000000000000000, -0.000000000000000000 ) ) ;
#3484=CARTESIAN_POINT ( 'NONE',  ( 2.002547531651519996, 12.57989064830759496, 0.6781519942172178350 ) ) ;
#3486=CARTESIAN_POINT ( 'NONE',  ( 16.56872352241294521, -0.001821578298043862289, 0.01027347319884366027 ) ) ;
#3491=CARTESIAN_POINT ( 'NONE',  ( 1.847372867223028070, 11.80112642014554325, 3.945260592619082907 ) ) ;
#3492=ORIENTED_EDGE ( 'NONE', *, *, #14232, .T. ) ;
#3498=B_SPLINE_CURVE_WITH_KNOTS ( 'NONE', 3,
 ( #18810, #14511, #17101, #4203, #15384, #14604 ),
 .UNSPECIFIED., .F., .F.,
 ( 4, 2, 4 ),
 ( 0.000000000000000000, 0.001500839035891551572, 0.003001678071783103145 ),
 .UNSPECIFIED. ) ;
#3499=B_SPLINE_CURVE_WITH_KNOTS ( 'NONE', 3,
 ( #6104, #6296, #11927, #7352, #17765, #4668, #9060, #13452, #9156, #366, #6193, #17470, #12027 ),
 .UNSPECIFIED., .F., .F.,
 ( 4, 3, 3, 3, 4 ),
 ( 4.670885906470169154E-18, 0.0002299780670421063087, 0.0004599561239687901203, 0.0006896788984287873046, 0.0009194956271626388705 ),
 .UNSPECIFIED. ) ;
#3502=CARTESIAN_POINT ( 'NONE',  ( 0.3137051932979757485, 8.442169467526850823, 10.83767969834806166 ) ) ;
#3504=CARTESIAN_POINT ( 'NONE',  ( 2.002547531651519996, -3.242439124566566910, -12.17374746633581495 ) ) ;
#3508=LINE ( 'NONE', #9346, #12008 ) ;
#3518=CARTESIAN_POINT ( 'NONE',  ( 1.847412631396502913, -7.278870946904175909, -10.09191835241971269 ) ) ;
#3519=AXIS2_PLACEMENT_3D ( 'NONE', #13638, #17846, #9145 ) ;
#3526=CARTESIAN_POINT ( 'NONE',  ( 3.512766787570756222, -14.81029789862160762, 2.682019731918325878 ) ) ;
#3533=CARTESIAN_POINT ( 'NONE',  ( 1.342453679581834924, 13.74702459364884533, 5.476372339890065000 ) ) ;
#3534=CARTESIAN_POINT ( 'NONE',  ( 2.705023505549866591, -8.489131503859701056, -10.24007717649589821 ) ) ;
#3535=VECTOR ( 'NONE', #17026, 1000.000000000000000 ) ;
#3536=AXIS2_PLACEMENT_3D ( 'NONE', #17761, #2915, #16428 ) ;
#3538=VERTEX_POINT ( 'NONE', #16671 ) ;
#3539=CARTESIAN_POINT ( 'NONE',  ( 16.56753206892534891, -0.009389754735542257466, -0.001421777558675915579 ) ) ;
#3546=EDGE_LOOP ( 'NONE', ( #17706, #13999, #7238, #5022 ) ) ;
#3547=CARTESIAN_POINT ( 'NONE',  ( 3.353306896162453477, 9.252610477110421172, -10.44017738170046528 ) ) ;
#3549=LINE ( 'NONE', #7874, #9457 ) ;
#3550=EDGE_CURVE ( 'NONE', #14483, #11305, #531, .T. ) ;
#3552=CARTESIAN_POINT ( 'NONE',  ( 1.254255976357310010, 14.64488542023430817, 1.011593778944276822 ) ) ;
#3555=EDGE_CURVE ( 'NONE', #12470, #14610, #3476, .T. ) ;
#3560=CARTESIAN_POINT ( 'NONE',  ( 0.3170788640506440603, 4.392045232375992647, -13.02120094575823472 ) ) ;
#3564=ORIENTED_EDGE ( 'NONE', *, *, #11134, .F. ) ;
#3570=CARTESIAN_POINT ( 'NONE',  ( 3.950837973638675393, -14.31366178983251380, -2.591948120961955926 ) ) ;
#3574=MECHANICAL_DESIGN_GEOMETRIC_PRESENTATION_REPRESENTATION('',(#9380),#4792);
#3578=DIRECTION ( 'NONE',  ( 0.000000000000000000, 0.000000000000000000, 1.000000000000000000 ) ) ;
#3588=EDGE_CURVE ( 'NONE', #16388, #17458, #12871, .T. ) ;
#3590=CARTESIAN_POINT ( 'NONE',  ( 0.3132635586635980074, -13.21855946425834283, -3.740017578711901436 ) ) ;
#3595=VERTEX_POINT ( 'NONE', #16395 ) ;
#3597=AXIS2_PLACEMENT_3D ( 'NONE', #17049, #8177, #902 ) ;
#3599=LINE ( 'NONE', #9435, #7790 ) ;
#3601=DIRECTION ( 'NONE',  ( -1.000000000000000000, 0.000000000000000000, 0.000000000000000000 ) ) ;
#3602=CARTESIAN_POINT ( 'NONE',  ( 1.846613052777650976, -11.72395935470501627, 4.166957398589803852 ) ) ;
#3609=VECTOR ( 'NONE', #4223, 1000.000000000000114 ) ;
#3610=ADVANCED_FACE ( 'NONE', ( #4829 ), #10966, .F. ) ;
#3612=ORIENTED_EDGE ( 'NONE', *, *, #8033, .F. ) ;
#3613=ORIENTED_EDGE ( 'NONE', *, *, #13490, .T. ) ;
#3614=EDGE_LOOP ( 'NONE', ( #10398, #2183, #12262, #11327 ) ) ;
#3622=ORIENTED_EDGE ( 'NONE', *, *, #11001, .T. ) ;
#3624=CARTESIAN_POINT ( 'NONE',  ( 2.747332970342022840, -16.12459247543628393, 2.705255688517782975 ) ) ;
#3632=B_SPLINE_CURVE_WITH_KNOTS ( 'NONE', 3,
 ( #8619, #10148, #7296, #17042, #8347, #14164 ),
 .UNSPECIFIED., .F., .F.,
 ( 4, 2, 4 ),
 ( 4.072016404827931570E-17, 0.0002014099069817292182, 0.0004028198139634177246 ),
 .UNSPECIFIED. ) ;
#3634=ORIENTED_EDGE ( 'NONE', *, *, #6315, .F. ) ;
#3635=CARTESIAN_POINT ( 'NONE',  ( 1.845756295923359325, 11.97166802574126088, 3.386818134580099837 ) ) ;
#3645=AXIS2_PLACEMENT_3D ( 'NONE', #18041, #3601, #15345 ) ;
#3652=B_SPLINE_CURVE_WITH_KNOTS ( 'NONE', 3,
 ( #765, #18339, #6240, #3812, #9548, #15376 ),
 .UNSPECIFIED., .F., .F.,
 ( 4, 2, 4 ),
 ( 1.939479807224432123E-18, 0.001500839035891553524, 0.003001678071783104879 ),
 .UNSPECIFIED. ) ;
#3654=CARTESIAN_POINT ( 'NONE',  ( 0.3939822652208131992, -11.57634296752772229, 7.545099438011985349 ) ) ;
#3657=CARTESIAN_POINT ( 'NONE',  ( 16.56753206892534891, -0.006760771273035160941, 0.006669401563385170262 ) ) ;
#3663=CARTESIAN_POINT ( 'NONE',  ( 0.4754618798421162973, 11.68486377711966817, 7.564402563418513026 ) ) ;
#3666=CARTESIAN_POINT ( 'NONE',  ( 0.3142011359265340920, -13.73310835363014348, 0.3830873813805846240 ) ) ;
#3669=CARTESIAN_POINT ( 'NONE',  ( 0.3137051932979757485, -7.698472063774552510, 11.37800749014128421 ) ) ;
#3673=CARTESIAN_POINT ( 'NONE',  ( 0.4862570985993235340, 5.003653737315670647, -12.97920246947874112 ) ) ;
#3674=DIRECTION ( 'NONE',  ( 0.7561779333270775005, 0.03481510524965243658, -0.6534392409364818688 ) ) ;
#3676=CARTESIAN_POINT ( 'NONE',  ( 2.320520222536482713, 14.32454429810331220, 6.542539914239615229 ) ) ;
#3677=EDGE_CURVE ( 'NONE', #3979, #6216, #3296, .T. ) ;
#3678=ADVANCED_FACE ( 'NONE', ( #6911 ), #3116, .F. ) ;
#3683=VERTEX_POINT ( 'NONE', #8429 ) ;
#3688=ORIENTED_EDGE ( 'NONE', *, *, #2076, .F. ) ;
#3689=CARTESIAN_POINT ( 'NONE',  ( 2.636624412714237309, 11.10302021257826866, 11.60464335004050973 ) ) ;
#3690=CARTESIAN_POINT ( 'NONE',  ( 1.846955891736117072, -11.74973605926567188, 4.094751675596655538 ) ) ;
#3693=AXIS2_PLACEMENT_3D ( 'NONE', #4193, #2644, #5429 ) ;
#3697=LINE ( 'NONE', #568, #4485 ) ;
#3699=ADVANCED_FACE ( 'NONE', ( #8714 ), #691, .F. ) ;
#3700=B_SPLINE_CURVE_WITH_KNOTS ( 'NONE', 3,
 ( #13804, #7911, #5204, #9226 ),
 .UNSPECIFIED., .F., .F.,
 ( 4, 4 ),
 ( 1.226634733346699349E-18, 0.003005512676784830983 ),
 .UNSPECIFIED. ) ;
#3701=ORIENTED_EDGE ( 'NONE', *, *, #16940, .F. ) ;
#3703=ORIENTED_EDGE ( 'NONE', *, *, #18691, .F. ) ;
#3705=DIRECTION ( 'NONE',  ( 0.000000000000000000, 0.000000000000000000, -1.000000000000000000 ) ) ;
#3710=DIRECTION ( 'NONE',  ( -0.7561779333270775005, -0.03481510524964337439, -0.6534392409364823129 ) ) ;
#3711=VERTEX_POINT ( 'NONE', #17505 ) ;
#3712=CARTESIAN_POINT ( 'NONE',  ( 1.847412631396505356, 10.04119192206686328, 7.348689888531877656 ) ) ;
#3713=EDGE_CURVE ( 'NONE', #7024, #4649, #17671, .T. ) ;
#3716=CARTESIAN_POINT ( 'NONE',  ( 1.861628059977343819, -7.751680370225458638, 9.751736252960339968 ) ) ;
#3717=( BOUNDED_SURFACE ( )  B_SPLINE_SURFACE ( 3, 1, ( 
 ( #15226, #517 ),
 ( #4908, #16570 ),
 ( #10738, #13699 ),
 ( #612, #6436 ) ),
 .UNSPECIFIED., .F., .F., .T. ) 
 B_SPLINE_SURFACE_WITH_KNOTS ( ( 4, 4 ),
 ( 2, 2 ),
 ( 0.000000000000000000, 1.000000000000000000 ),
 ( 0.000000000000000000, 1.000000000000000000 ),
 .UNSPECIFIED. ) 
 GEOMETRIC_REPRESENTATION_ITEM ( )  RATIONAL_B_SPLINE_SURFACE ( (
 ( 1.000000000000000000, 1.000000000000000000),
 ( 0.9933953342250436691, 0.8357391271907733676),
 ( 0.9933953342250436691, 0.8357391271907733676),
 ( 1.000000000000000000, 1.000000000000000000) ) ) 
 REPRESENTATION_ITEM ( '' )  SURFACE ( )  );
#3719=CARTESIAN_POINT ( 'NONE',  ( 3.950837973638675393, -10.05648675950118509, -10.51028938476228980 ) ) ;
#3720=CARTESIAN_POINT ( 'NONE',  ( 0.3145729642390391323, 11.29233589755992639, 7.825496023201352180 ) ) ;
#3734=CARTESIAN_POINT ( 'NONE',  ( 0.4862570985993235340, -13.44146924561383827, 3.580942890621619412 ) ) ;
#3737=B_SPLINE_CURVE_WITH_KNOTS ( 'NONE', 3,
 ( #77, #8109, #2263, #16883 ),
 .UNSPECIFIED., .F., .F.,
 ( 4, 4 ),
 ( 0.000000000000000000, 0.002004993803842710330 ),
 .UNSPECIFIED. ) ;
#3738=CARTESIAN_POINT ( 'NONE',  ( 0.8740779401512095426, 7.708543377337996994, -12.04241618260087776 ) ) ;
#3742=DIRECTION ( 'NONE',  ( 0.000000000000000000, -1.000000000000000000, 0.000000000000000000 ) ) ;
#3744=CARTESIAN_POINT ( 'NONE',  ( 0.3058872367615226295, 3.664492643742762290, 13.24582953854926615 ) ) ;
#3747=ORIENTED_EDGE ( 'NONE', *, *, #8085, .T. ) ;
#3752=B_SPLINE_CURVE_WITH_KNOTS ( 'NONE', 3,
 ( #15372, #2278, #12504, #6970, #15556, #15932 ),
 .UNSPECIFIED., .F., .F.,
 ( 4, 2, 4 ),
 ( 3.897476843869763523E-18, 0.0002017457492448077711, 0.0004034914984896116391 ),
 .UNSPECIFIED. ) ;
#3754=CARTESIAN_POINT ( 'NONE',  ( 0.3151928479966097374, 1.775918418904422640E-15, 13.73922861026898623 ) ) ;
#3758=CARTESIAN_POINT ( 'NONE',  ( 2.636624412716062960, 2.862162146982868194, -15.80357026013419564 ) ) ;
#3759=CARTESIAN_POINT ( 'NONE',  ( 1.846138399168762101, -10.30487220521565028, -6.971848976711123136 ) ) ;
#3761=CARTESIAN_POINT ( 'NONE',  ( 2.636624412714237309, 15.91454522070173638, -2.161493821596664144 ) ) ;
#3765=CARTESIAN_POINT ( 'NONE',  ( 0.4754618798421162973, 0.7484603771386368898, -13.89949764182681768 ) ) ;
#3766=CARTESIAN_POINT ( 'NONE',  ( 1.846138399168762101, -0.4167076046096411246, 12.43476674860266407 ) ) ;
#3769=CARTESIAN_POINT ( 'NONE',  ( 1.977436885025421809, 14.12046670317507058, 6.153171729167918436 ) ) ;
#3770=CARTESIAN_POINT ( 'NONE',  ( 0.4862570985993235340, -13.44146924561378498, -3.580942890621813923 ) ) ;
#3785=CARTESIAN_POINT ( 'NONE',  ( 8.438534575730034959, 4.221456476902665678, 5.415535776177536675 ) ) ;
#3786=AXIS2_PLACEMENT_3D ( 'NONE', #7955, #2279, #8129 ) ;
#3788=CARTESIAN_POINT ( 'NONE',  ( 1.977228804422057395, -11.52787183731166820, 10.21522664410399095 ) ) ;
#3797=CARTESIAN_POINT ( 'NONE',  ( 1.342453679581834924, -13.74702459364888263, 5.476372339889963747 ) ) ;
#3804=EDGE_CURVE ( 'NONE', #2427, #15958, #17415, .T. ) ;
#3812=CARTESIAN_POINT ( 'NONE',  ( 3.353306896162457029, 13.62210141459500079, -3.007732942432275181 ) ) ;
#3818=CARTESIAN_POINT ( 'NONE',  ( 2.705023505549862595, -10.24007717649586624, 8.489131503859741912 ) ) ;
#3820=ADVANCED_FACE ( 'NONE', ( #11966 ), #11186, .F. ) ;
#3821=CARTESIAN_POINT ( 'NONE',  ( 2.636624412714236865, 0.000000000000000000, 0.000000000000000000 ) ) ;
#3822=VERTEX_POINT ( 'NONE', #12254 ) ;
#3824=CARTESIAN_POINT ( 'NONE',  ( 1.846524061778018311, -12.43723828841088341, -0.3544704288993787422 ) ) ;
#3825=( BOUNDED_SURFACE ( )  B_SPLINE_SURFACE ( 3, 1, ( 
 ( #50, #11905 ),
 ( #4353, #1775 ),
 ( #4449, #10275 ),
 ( #7620, #342 ) ),
 .UNSPECIFIED., .F., .F., .T. ) 
 B_SPLINE_SURFACE_WITH_KNOTS ( ( 4, 4 ),
 ( 2, 2 ),
 ( 0.000000000000000000, 1.000000000000000000 ),
 ( 0.000000000000000000, 1.000000000000000000 ),
 .UNSPECIFIED. ) 
 GEOMETRIC_REPRESENTATION_ITEM ( )  RATIONAL_B_SPLINE_SURFACE ( (
 ( 1.000000000000000000, 1.000000000000000000),
 ( 0.7792777138730158093, 0.9689936506012928330),
 ( 0.7792777138730158093, 0.9689936506012928330),
 ( 1.000000000000000000, 1.000000000000000000) ) ) 
 REPRESENTATION_ITEM ( '' )  SURFACE ( )  );
#3826=ORIENTED_EDGE ( 'NONE', *, *, #7287, .F. ) ;
#3834=EDGE_CURVE ( 'NONE', #4049, #9141, #14000, .T. ) ;
#3837=CARTESIAN_POINT ( 'NONE',  ( 2.320521194581854463, 13.71278319227944920, 7.743190876766304243 ) ) ;
#3839=LINE ( 'NONE', #11388, #10292 ) ;
#3840=EDGE_CURVE ( 'NONE', #6348, #78, #3549, .T. ) ;
#3845=ORIENTED_EDGE ( 'NONE', *, *, #18010, .T. ) ;
#3849=CARTESIAN_POINT ( 'NONE',  ( 0.3142011359265305948, -8.382042760265827397, -10.88514493056451471 ) ) ;
#3859=DIRECTION ( 'NONE',  ( 0.000000000000000000, 0.000000000000000000, 1.000000000000000000 ) ) ;
#3861=( BOUNDED_SURFACE ( )  B_SPLINE_SURFACE ( 3, 1, ( 
 ( #2172, #10688 ),
 ( #4946, #8009 ),
 ( #2255, #12389 ),
 ( #12215, #10778 ) ),
 .UNSPECIFIED., .F., .F., .T. ) 
 B_SPLINE_SURFACE_WITH_KNOTS ( ( 4, 4 ),
 ( 2, 2 ),
 ( 0.000000000000000000, 1.000000000000000000 ),
 ( 0.000000000000000000, 1.000000000000000000 ),
 .UNSPECIFIED. ) 
 GEOMETRIC_REPRESENTATION_ITEM ( )  RATIONAL_B_SPLINE_SURFACE ( (
 ( 1.000000000000000000, 1.000000000000000000),
 ( 0.7792777138730160313, 0.9689936506012927220),
 ( 0.7792777138730160313, 0.9689936506012927220),
 ( 1.000000000000000000, 1.000000000000000000) ) ) 
 REPRESENTATION_ITEM ( '' )  SURFACE ( )  );
#3863=CARTESIAN_POINT ( 'NONE',  ( 0.3939875929385635578, -4.930599594904470528, -12.90850834464105645 ) ) ;
#3864=CARTESIAN_POINT ( 'NONE',  ( 0.3095370825347224519, 4.681152801286160070, 12.91933430393609861 ) ) ;
#3866=EDGE_CURVE ( 'NONE', #11500, #1343, #12189, .T. ) ;
#3867=EDGE_CURVE ( 'NONE', #7021, #1472, #15580, .T. ) ;
#3871=ORIENTED_EDGE ( 'NONE', *, *, #5215, .T. ) ;
#3874=ORIENTED_EDGE ( 'NONE', *, *, #13221, .T. ) ;
#3883=CARTESIAN_POINT ( 'NONE',  ( 0.3095370825347224519, 13.73357284481724783, 0.4597470195090653799 ) ) ;
#3884=CARTESIAN_POINT ( 'NONE',  ( 0.3142011359265295956, -0.3830873813805367734, -13.73310835363015059 ) ) ;
#3887=CARTESIAN_POINT ( 'NONE',  ( 0.4754618798421162973, 12.98792082933644743, 5.007009103465295929 ) ) ;
#3890=EDGE_CURVE ( 'NONE', #13188, #11529, #88, .T. ) ;
#3892=EDGE_LOOP ( 'NONE', ( #7918, #9491, #3226, #5493 ) ) ;
#3897=CARTESIAN_POINT ( 'NONE',  ( 1.342453679581834924, -12.51077660954471504, 7.902645620902405632 ) ) ;
#3899=CARTESIAN_POINT ( 'NONE',  ( 1.847034903785828019, -7.498375632854680006, 9.929438108952115982 ) ) ;
#3901=DIRECTION ( 'NONE',  ( -0.7561779333270775005, 0.1688126975276644792, -0.6322161072786924851 ) ) ;
#3902=CARTESIAN_POINT ( 'NONE',  ( 1.846138399168762101, 0.4167076046095548603, 12.43476674860266762 ) ) ;
#3904=LINE ( 'NONE', #6866, #16080 ) ;
#3905=B_SPLINE_CURVE_WITH_KNOTS ( 'NONE', 3,
 ( #14282, #14365, #18661, #1083, #10066, #2694 ),
 .UNSPECIFIED., .F., .F.,
 ( 4, 2, 4 ),
 ( 3.499941646806256644E-17, 0.0001825746017570581273, 0.0003651492035140812891 ),
 .UNSPECIFIED. ) ;
#3908=CARTESIAN_POINT ( 'NONE',  ( 1.847461586945732925, 3.877048136045379234, 11.82388984758120287 ) ) ;
#3909=CARTESIAN_POINT ( 'NONE',  ( 16.56753206892534891, 0.009389754735542245323, 0.001421777558675984534 ) ) ;
#3910=CARTESIAN_POINT ( 'NONE',  ( 2.636624412716062515, -6.973567714909003179, -14.46769361191335790 ) ) ;
#3919=CARTESIAN_POINT ( 'NONE',  ( 1.847461586945731371, -12.44326124954594448, 0.03350899125588503030 ) ) ;
#3922=CARTESIAN_POINT ( 'NONE',  ( 2.320520222537280297, -10.64885284335050741, 11.60169517779339898 ) ) ;
#3929=ORIENTED_EDGE ( 'NONE', *, *, #15678, .F. ) ;
#3933=CARTESIAN_POINT ( 'NONE',  ( 16.56872352241294521, -0.009382111268607402216, -0.004564908236399935551 ) ) ;
#3936=B_SPLINE_CURVE_WITH_KNOTS ( 'NONE', 3,
 ( #10502, #13552, #475, #16339, #9254, #17967, #3518, #3220, #6302, #3421, #4866, #12135, #15083 ),
 .UNSPECIFIED., .F., .F.,
 ( 4, 3, 3, 3, 4 ),
 ( 0.000000000000000000, 0.0002299804304191505879, 0.0004599608082120279365, 0.0006467586077648024507, 0.0008336169836825989407 ),
 .UNSPECIFIED. ) ;
#3948=CARTESIAN_POINT ( 'NONE',  ( 0.3150686449036064207, -11.02450593298024195, 8.199336701264503091 ) ) ;
#3957=CARTESIAN_POINT ( 'NONE',  ( 1.846138399168762101, -7.646096044339819819, -9.815003036200495856 ) ) ;
#3963=VERTEX_POINT ( 'NONE', #8326 ) ;
#3967=EDGE_CURVE ( 'NONE', #421, #885, #12722, .T. ) ;
#3969=CARTESIAN_POINT ( 'NONE',  ( 2.002547531651519996, -11.75462648437098601, -4.532360870844453160 ) ) ;
#3973=CARTESIAN_POINT ( 'NONE',  ( 2.747332970342022840, -7.289199830147212289, 14.63517873738944708 ) ) ;
#3974=CARTESIAN_POINT ( 'NONE',  ( 0.3137051932979775248, -12.91601973349273891, 4.679953077377436266 ) ) ;
#3975=FACE_OUTER_BOUND ( 'NONE', #6217, .T. ) ;
#3977=B_SPLINE_CURVE_WITH_KNOTS ( 'NONE', 3,
 ( #16893, #7317, #6961, #16192, #6066, #14656, #12771, #7507, #8922, #15631, #1110, #3175, #10459 ),
 .UNSPECIFIED., .F., .F.,
 ( 4, 3, 3, 3, 4 ),
 ( 3.127317220692750759E-18, 0.0002299804304191474438, 0.0004599608082120254971, 0.0006467586077648028843, 0.0008336169836825993744 ),
 .UNSPECIFIED. ) ;
#3978=B_SPLINE_CURVE_WITH_KNOTS ( 'NONE', 3,
 ( #10286, #17751, #449, #12111, #17845, #13532 ),
 .UNSPECIFIED., .F., .F.,
 ( 4, 2, 4 ),
 ( 0.000000000000000000, 0.001500839035891548753, 0.003001678071783097507 ),
 .UNSPECIFIED. ) ;
#3979=VERTEX_POINT ( 'NONE', #8145 ) ;
#3981=EDGE_LOOP ( 'NONE', ( #17144, #1208, #10696, #2884 ) ) ;
#3983=CARTESIAN_POINT ( 'NONE',  ( 3.353306896162455697, -12.78841260990234119, -5.573563251762232440 ) ) ;
#3985=CARTESIAN_POINT ( 'NONE',  ( 8.522092701127531811, -6.722964936702111594, 1.786985377232005900 ) ) ;
#3988=EDGE_CURVE ( 'NONE', #9141, #10419, #6577, .T. ) ;
#3996=CARTESIAN_POINT ( 'NONE',  ( 0.4754618798421162973, -7.564402563418551217, 11.68486377711963975 ) ) ;
#3997=CARTESIAN_POINT ( 'NONE',  ( 3.353306896162456585, 5.573563251762281290, -12.78841260990232165 ) ) ;
#3999=CARTESIAN_POINT ( 'NONE',  ( 2.747332970342022840, -11.45495994260709161, -11.66639548242820190 ) ) ;
#4001=CARTESIAN_POINT ( 'NONE',  ( 16.56872352241294521, -0.004564908236400289435, -0.009382111268606239951 ) ) ;
#4002=B_SPLINE_CURVE_WITH_KNOTS ( 'NONE', 3,
 ( #15134, #7978, #12622, #4911, #5088, #3465 ),
 .UNSPECIFIED., .F., .F.,
 ( 4, 2, 4 ),
 ( 0.000000000000000000, 0.001656992708822831520, 0.003313985417645663040 ),
 .UNSPECIFIED. ) ;
#4005=ORIENTED_EDGE ( 'NONE', *, *, #3550, .T. ) ;
#4013=B_SPLINE_CURVE_WITH_KNOTS ( 'NONE', 3,
 ( #2540, #15555, #12324, #5242, #2370, #6780 ),
 .UNSPECIFIED., .F., .F.,
 ( 4, 2, 4 ),
 ( 0.000000000000000000, 0.0001828790815886951050, 0.0003657581631773902100 ),
 .UNSPECIFIED. ) ;
#4017=EDGE_CURVE ( 'NONE', #6216, #17983, #18585, .T. ) ;
#4024=CARTESIAN_POINT ( 'NONE',  ( 2.353870697619111496, -4.720869121224215093, 12.05847592522641953 ) ) ;
#4026=CARTESIAN_POINT ( 'NONE',  ( 0.3137051932979792457, -12.91601973349266963, -4.679953077377624560 ) ) ;
#4030=ORIENTED_EDGE ( 'NONE', *, *, #3967, .F. ) ;
#4033=CARTESIAN_POINT ( 'NONE',  ( 0.3137051932979809665, -3.805684345189881856, 13.20008686438104739 ) ) ;
#4037=DIRECTION ( 'NONE',  ( -1.000000000000000000, 0.000000000000000000, -0.000000000000000000 ) ) ;
#4049=VERTEX_POINT ( 'NONE', #15950 ) ;
#4051=FACE_OUTER_BOUND ( 'NONE', #17350, .T. ) ;
#4052=EDGE_LOOP ( 'NONE', ( #18755, #15723, #15542, #5809 ) ) ;
#4053=EDGE_CURVE ( 'NONE', #8937, #15252, #14748, .T. ) ;
#4054=EDGE_LOOP ( 'NONE', ( #15434, #6932, #5823, #12054 ) ) ;
#4057=ORIENTED_EDGE ( 'NONE', *, *, #373, .T. ) ;
#4061=CARTESIAN_POINT ( 'NONE',  ( 0.3142014840576502488, 13.17932813834300099, -3.879477880151306568 ) ) ;
#4065=CARTESIAN_POINT ( 'NONE',  ( 0.3137051932979757485, 7.698472063774634222, -11.37800749014122736 ) ) ;
#4066=CARTESIAN_POINT ( 'NONE',  ( 1.342453679581834924, 3.649820028552932971, -14.34050741580202981 ) ) ;
#4070=EDGE_CURVE ( 'NONE', #8886, #12927, #18639, .T. ) ;
#4075=ORIENTED_EDGE ( 'NONE', *, *, #14290, .F. ) ;
#4079=CARTESIAN_POINT ( 'NONE',  ( 2.636624412716062960, -2.161493821598612808, -15.91454522070331912 ) ) ;
#4084=CARTESIAN_POINT ( 'NONE',  ( 8.438534575730034959, 0.2320579683290127926, 6.862570336891076650 ) ) ;
#4085=CARTESIAN_POINT ( 'NONE',  ( 0.8740779401509238822, -13.83508928787439096, -3.609949156401517367 ) ) ;
#4091=ORIENTED_EDGE ( 'NONE', *, *, #2407, .F. ) ;
#4095=EDGE_CURVE ( 'NONE', #4709, #14938, #10917, .T. ) ;
#4098=CARTESIAN_POINT ( 'NONE',  ( 0.3095370825347224519, 4.681152801286340370, -12.91933430393602933 ) ) ;
#4100=B_SPLINE_CURVE_WITH_KNOTS ( 'NONE', 3,
 ( #10365, #4730, #3177, #1867 ),
 .UNSPECIFIED., .F., .F.,
 ( 4, 4 ),
 ( 0.000000000000000000, 0.002004993803842355579 ),
 .UNSPECIFIED. ) ;
#4101=CARTESIAN_POINT ( 'NONE',  ( 16.56782317627811096, 0.009814734722106368062, -0.0003415813796015080314 ) ) ;
#4103=CARTESIAN_POINT ( 'NONE',  ( 3.512766787570723803, -13.25664064834472100, -7.127386085302978458 ) ) ;
#4105=CARTESIAN_POINT ( 'NONE',  ( 2.636624412715384391, -11.60464335004044223, -11.10302021258006278 ) ) ;
#4109=CARTESIAN_POINT ( 'NONE',  ( 1.918921323896325193, 3.258415356426521026, 12.08297777410666285 ) ) ;
#4110=CARTESIAN_POINT ( 'NONE',  ( 0.3137051932979792457, -13.73004976592201842, -0.4596302728641207813 ) ) ;
#4112=EDGE_CURVE ( 'NONE', #17568, #15056, #8596, .T. ) ;
#4115=APPLICATION_CONTEXT ( 'automotive_design' ) ;
#4118=DIRECTION ( 'NONE',  ( 0.7561779333270775005, -0.4122479608995778255, 0.5081796452863200919 ) ) ;
#4120=CARTESIAN_POINT ( 'NONE',  ( 3.950837973638676281, 14.31366178983253512, 2.591948120961855118 ) ) ;
#4129=ORIENTED_EDGE ( 'NONE', *, *, #18031, .F. ) ;
#4130=CARTESIAN_POINT ( 'NONE',  ( 0.3095370825347224519, 12.91933430393608084, 4.681152801286204479 ) ) ;
#4132=CARTESIAN_POINT ( 'NONE',  ( 0.3151928476913592458, -4.245457024760312947, 13.06684726503524807 ) ) ;
#4137=B_SPLINE_CURVE_WITH_KNOTS ( 'NONE', 3,
 ( #11537, #5782, #7139, #16122, #3003, #5685 ),
 .UNSPECIFIED., .F., .F.,
 ( 4, 2, 4 ),
 ( 0.000000000000000000, 0.001657017934711440188, 0.003314035869422880375 ),
 .UNSPECIFIED. ) ;
#4139=B_SPLINE_CURVE_WITH_KNOTS ( 'NONE', 3,
 ( #8632, #15894, #14179, #8360, #17054, #9865 ),
 .UNSPECIFIED., .F., .F.,
 ( 4, 2, 4 ),
 ( 3.556447555475521540E-17, 0.0001825746017570583171, 0.0003651492035140810723 ),
 .UNSPECIFIED. ) ;
#4141=CARTESIAN_POINT ( 'NONE',  ( 0.3095370825347234511, 0.4597470195092124290, -13.73357284481724250 ) ) ;
#4143=B_SPLINE_CURVE_WITH_KNOTS ( 'NONE', 3,
 ( #7443, #14500, #73, #13064, #16228, #5792 ),
 .UNSPECIFIED., .F., .F.,
 ( 4, 2, 4 ),
 ( 8.940560153363745023E-19, 0.0001828790815881870750, 0.0003657581631763732284 ),
 .UNSPECIFIED. ) ;
#4144=CARTESIAN_POINT ( 'NONE',  ( 0.3137051932979792457, -10.83767969834809008, 8.442169467526815296 ) ) ;
#4146=FACE_OUTER_BOUND ( 'NONE', #6470, .T. ) ;
#4147=ORIENTED_EDGE ( 'NONE', *, *, #2090, .F. ) ;
#4148=DIRECTION ( 'NONE',  ( -1.000000000000000000, -0.000000000000000000, -0.000000000000000000 ) ) ;
#4149=CARTESIAN_POINT ( 'NONE',  ( 0.3720661004400040439, 8.694226082900595287, 10.73619472937705233 ) ) ;
#4150=VERTEX_POINT ( 'NONE', #14996 ) ;
#4159=LINE ( 'NONE', #9978, #18499 ) ;
#4163=( BOUNDED_SURFACE ( )  B_SPLINE_SURFACE ( 3, 1, ( 
 ( #84, #1705 ),
 ( #10312, #15940 ),
 ( #14602, #8678 ),
 ( #6008, #4380 ) ),
 .UNSPECIFIED., .F., .F., .T. ) 
 B_SPLINE_SURFACE_WITH_KNOTS ( ( 4, 4 ),
 ( 2, 2 ),
 ( 0.000000000000000000, 1.000000000000000000 ),
 ( 0.000000000000000000, 1.000000000000000000 ),
 .UNSPECIFIED. ) 
 GEOMETRIC_REPRESENTATION_ITEM ( )  RATIONAL_B_SPLINE_SURFACE ( (
 ( 1.000000000000000000, 1.000000000000000000),
 ( 0.9933953342250436691, 0.8357391271907733676),
 ( 0.9933953342250436691, 0.8357391271907733676),
 ( 1.000000000000000000, 1.000000000000000000) ) ) 
 REPRESENTATION_ITEM ( '' )  SURFACE ( )  );
#4166=LINE ( 'NONE', #1196, #13360 ) ;
#4168=DIRECTION ( 'NONE',  ( 0.000000000000000000, 1.000000000000000000, 0.000000000000000000 ) ) ;
#4173=ORIENTED_EDGE ( 'NONE', *, *, #9481, .F. ) ;
#4174=B_SPLINE_CURVE_WITH_KNOTS ( 'NONE', 3,
 ( #6637, #9211, #12453, #15140 ),
 .UNSPECIFIED., .F., .F.,
 ( 4, 4 ),
 ( 4.873469348537302793E-16, 0.002004993803842133101 ),
 .UNSPECIFIED. ) ;
#4180=B_SPLINE_CURVE_WITH_KNOTS ( 'NONE', 3,
 ( #4947, #3602, #3690, #2256, #735, #2173, #12216, #13645, #8010, #17955, #562, #10970, #12390 ),
 .UNSPECIFIED., .F., .F.,
 ( 4, 3, 3, 3, 4 ),
 ( 1.734723475976807094E-18, 0.0002299804304191486635, 0.0004599608082120272860, 0.0006467586077648025591, 0.0008336169836825982902 ),
 .UNSPECIFIED. ) ;
#4181=LINE ( 'NONE', #12863, #9350 ) ;
#4193=CARTESIAN_POINT ( 'NONE',  ( 3.950837973638668288, 0.000000000000000000, 0.000000000000000000 ) ) ;
#4202=ORIENTED_EDGE ( 'NONE', *, *, #15921, .F. ) ;
#4203=CARTESIAN_POINT ( 'NONE',  ( 3.353306896162455697, 3.007732942432417289, 13.62210141459496171 ) ) ;
#4208=CARTESIAN_POINT ( 'NONE',  ( 2.123976203522053297, -10.37815841598499667, 11.67822624909921814 ) ) ;
#4209=VECTOR ( 'NONE', #6742, 1000.000000000000227 ) ;
#4210=CARTESIAN_POINT ( 'NONE',  ( 0.3142014840576518586, -3.879477880151352753, -13.17932813834298678 ) ) ;
#4213=CARTESIAN_POINT ( 'NONE',  ( 1.846138399168762989, 11.69739621335922308, 4.238866729160444713 ) ) ;
#4215=LINE ( 'NONE', #10031, #15340 ) ;
#4216=B_SPLINE_CURVE_WITH_KNOTS ( 'NONE', 3,
 ( #6219, #13284, #7280, #199, #10136, #13384, #11860, #302, #15960, #10329 ),
 .UNSPECIFIED., .F., .F.,
 ( 4, 3, 3, 4 ),
 ( 0.0004168119862248656667, 0.0004599608082120252802, 0.0006467586077648016917, 0.0008336169836825988323 ),
 .UNSPECIFIED. ) ;
#4219=CARTESIAN_POINT ( 'NONE',  ( 2.636624412714236865, 0.000000000000000000, 0.000000000000000000 ) ) ;
#4223=DIRECTION ( 'NONE',  ( -0.7561779333270775005, -0.6106991889125072959, 0.2350349629540161855 ) ) ;
#4232=CARTESIAN_POINT ( 'NONE',  ( 0.3307726912345235748, -3.680742887039399669, 13.25328329128664606 ) ) ;
#4237=ORIENTED_EDGE ( 'NONE', *, *, #4371, .F. ) ;
#4240=FACE_OUTER_BOUND ( 'NONE', #18688, .T. ) ;
#4241=CARTESIAN_POINT ( 'NONE',  ( 0.4754618798421167414, 8.775436892861268490, -10.80499583390503560 ) ) ;
#4243=CARTESIAN_POINT ( 'NONE',  ( 2.123976203522053297, 11.67822624909925544, 10.37815841598495936 ) ) ;
#4250=CARTESIAN_POINT ( 'NONE',  ( 0.4862570985993235340, 8.769551628660735787, 10.79774104611376373 ) ) ;
#4252=CARTESIAN_POINT ( 'NONE',  ( 0.3058872367615226295, 4.821066432589507400, -12.87003593440623206 ) ) ;
#4253=VECTOR ( 'NONE', #8146, 1000.000000000000114 ) ;
#4258=CARTESIAN_POINT ( 'NONE',  ( 0.3151926232592475174, -8.013596737356467159, 11.16039997398650918 ) ) ;
#4265=CARTESIAN_POINT ( 'NONE',  ( 0.3170788640506440603, 11.20690911610915208, -7.952793437297452250 ) ) ;
#4267=ORIENTED_EDGE ( 'NONE', *, *, #18778, .T. ) ;
#4274=CARTESIAN_POINT ( 'NONE',  ( 2.636624412714242194, 14.46769361191244485, 6.973567714906650394 ) ) ;
#4277=CARTESIAN_POINT ( 'NONE',  ( 0.3137051932979775248, 0.4596302728639756197, 13.73004976592202198 ) ) ;
#4281=ADVANCED_FACE ( 'NONE', ( #1714 ), #5306, .F. ) ;
#4282=CARTESIAN_POINT ( 'NONE',  ( 1.959212340397942231, 12.12975361829680310, -3.239239832448903122 ) ) ;
#4283=CARTESIAN_POINT ( 'NONE',  ( 1.847372867223028070, 3.744745203533978106, 11.86627781945709792 ) ) ;
#4286=CARTESIAN_POINT ( 'NONE',  ( 2.002547531651519996, 4.532360870844494016, -11.75462648437097180 ) ) ;
#4288=ORIENTED_EDGE ( 'NONE', *, *, #1459, .F. ) ;
#4292=EDGE_CURVE ( 'NONE', #17548, #14697, #14995, .T. ) ;
#4294=CARTESIAN_POINT ( 'NONE',  ( 0.4385251269669980800, -3.577373010348622540, -13.39302348765812312 ) ) ;
#4299=FACE_OUTER_BOUND ( 'NONE', #14872, .T. ) ;
#4304=CARTESIAN_POINT ( 'NONE',  ( 1.846138399168762101, -12.43476674860266229, -0.4167076046096845898 ) ) ;
#4307=ORIENTED_EDGE ( 'NONE', *, *, #9073, .F. ) ;
#4309=CARTESIAN_POINT ( 'NONE',  ( 1.977436885025838142, -14.12046670317529440, -6.153171729168441573 ) ) ;
#4310=CARTESIAN_POINT ( 'NONE',  ( 2.002547531651519996, 9.778737580845815458, -7.942910686618064986 ) ) ;
#4311=EDGE_LOOP ( 'NONE', ( #17254, #12858, #4692, #15941 ) ) ;
#4312=EDGE_CURVE ( 'NONE', #11465, #5954, #2275, .T. ) ;
#4316=ORIENTED_EDGE ( 'NONE', *, *, #374, .T. ) ;
#4320=ORIENTED_EDGE ( 'NONE', *, *, #272, .T. ) ;
#4321=CARTESIAN_POINT ( 'NONE',  ( 2.636624412714237309, 14.14563173255211126, 7.605649742762011556 ) ) ;
#4325=DIRECTION ( 'NONE',  ( -1.000000000000000000, 0.000000000000000000, -0.000000000000000000 ) ) ;
#4326=VERTEX_POINT ( 'NONE', #5422 ) ;
#4328=CARTESIAN_POINT ( 'NONE',  ( 16.58200780006414732, 0.01115192838421568376, 0.0006320991582350033409 ) ) ;
#4330=FACE_OUTER_BOUND ( 'NONE', #13068, .T. ) ;
#4331=CARTESIAN_POINT ( 'NONE',  ( 3.950837973638676281, -6.888253895133199300, -12.81214529934982949 ) ) ;
#4335=EDGE_LOOP ( 'NONE', ( #11113, #10310, #18052, #4606 ) ) ;
#4342=CARTESIAN_POINT ( 'NONE',  ( 0.3058872367615226295, -13.72992299905059355, -0.6080468242582393046 ) ) ;
#4343=VECTOR ( 'NONE', #14895, 1000.000000000000114 ) ;
#4344=VERTEX_POINT ( 'NONE', #6778 ) ;
#4346=CARTESIAN_POINT ( 'NONE',  ( 16.56753206892534891, 0.009389754735542247058, 0.001421777558675981282 ) ) ;
#4347=DIRECTION ( 'NONE',  ( -1.000000000000000000, -0.000000000000000000, -0.000000000000000000 ) ) ;
#4351=CARTESIAN_POINT ( 'NONE',  ( 2.747332970342022840, -16.17136872824900351, 2.409922051470623661 ) ) ;
#4353=CARTESIAN_POINT ( 'NONE',  ( 16.57778382496167424, 0.01466529584256671612, -0.002851818597093459199 ) ) ;
#4355=EDGE_LOOP ( 'NONE', ( #2045, #6769, #17331, #4147 ) ) ;
#4356=ORIENTED_EDGE ( 'NONE', *, *, #10209, .T. ) ;
#4357=AXIS2_PLACEMENT_3D ( 'NONE', #10857, #10567, #4735 ) ;
#4359=ORIENTED_EDGE ( 'NONE', *, *, #13647, .T. ) ;
#4360=B_SPLINE_CURVE_WITH_KNOTS ( 'NONE', 3,
 ( #8863, #1410, #10302, #1697, #11641, #12025 ),
 .UNSPECIFIED., .F., .F.,
 ( 4, 2, 4 ),
 ( 4.225718824587268470E-17, 0.0002014099069817298145, 0.0004028198139634173993 ),
 .UNSPECIFIED. ) ;
#4363=ADVANCED_FACE ( 'NONE', ( #18418 ), #13123, .F. ) ;
#4371=EDGE_CURVE ( 'NONE', #3595, #10401, #15282, .T. ) ;
#4376=VERTEX_POINT ( 'NONE', #758 ) ;
#4378=ORIENTED_EDGE ( 'NONE', *, *, #1372, .F. ) ;
#4379=VERTEX_POINT ( 'NONE', #6591 ) ;
#4380=CARTESIAN_POINT ( 'NONE',  ( 0.4754618798421162973, 13.89949764182682657, 0.7484603771384912285 ) ) ;
#4387=ORIENTED_EDGE ( 'NONE', *, *, #5486, .F. ) ;
#4391=CARTESIAN_POINT ( 'NONE',  ( 1.846822687350018422, 11.74004266906804617, 4.121816957446238661 ) ) ;
#4392=CARTESIAN_POINT ( 'NONE',  ( 1.918918678667044908, -6.832809802519085096, 10.48466773720559608 ) ) ;
#4393=ADVANCED_FACE ( 'NONE', ( #14494 ), #10504, .T. ) ;
#4397=CARTESIAN_POINT ( 'NONE',  ( 3.512766787570769544, 10.87507422923904166, -10.40533104696121214 ) ) ;
#4401=ORIENTED_EDGE ( 'NONE', *, *, #14384, .T. ) ;
#4403=ORIENTED_EDGE ( 'NONE', *, *, #1748, .T. ) ;
#4404=CARTESIAN_POINT ( 'NONE',  ( 0.3137051932979775248, -0.4596302728638797519, -13.73004976592202553 ) ) ;
#4407=CARTESIAN_POINT ( 'NONE',  ( 16.56822296793089322, -0.009847136207496290372, -0.002414375228568220195 ) ) ;
#4410=CARTESIAN_POINT ( 'NONE',  ( 0.3145729642390375225, -3.952965287571204023, 13.15786090015082799 ) ) ;
#4411=CARTESIAN_POINT ( 'NONE',  ( 0.3939822652208163078, 3.598529276937260324, 13.34132036472938410 ) ) ;
#4416=CARTESIAN_POINT ( 'NONE',  ( 16.56782317627811096, -0.006045301465876417625, 0.007739510688079494216 ) ) ;
#4418=CARTESIAN_POINT ( 'NONE',  ( 3.353306896162455697, -13.62210141459498125, 3.007732942432364442 ) ) ;
#4419=CARTESIAN_POINT ( 'NONE',  ( 16.56782317627811096, -0.002708056627497679603, 0.009439921864426459655 ) ) ;
#4425=CARTESIAN_POINT ( 'NONE',  ( 0.3170788640506441158, -13.02120094575831288, 4.392045232375760833 ) ) ;
#4427=ORIENTED_EDGE ( 'NONE', *, *, #9427, .T. ) ;
#4435=CARTESIAN_POINT ( 'NONE',  ( 2.747332970342022840, 11.45495994260717865, 11.66639548242811486 ) ) ;
#4446=CARTESIAN_POINT ( 'NONE',  ( 0.000000000000000000, 6.799999999999999822, -1.500000000000000000 ) ) ;
#4449=CARTESIAN_POINT ( 'NONE',  ( 16.57210152137263393, 0.01214401161737518019, -0.008007331252332923130 ) ) ;
#4452=CARTESIAN_POINT ( 'NONE',  ( 16.57778382496167424, -0.01306626476309294925, 0.007244066302946726259 ) ) ;
#4455=VERTEX_POINT ( 'NONE', #4277 ) ;
#4457=VERTEX_POINT ( 'NONE', #9906 ) ;
#4459=CARTESIAN_POINT ( 'NONE',  ( 3.377929128793394575, 5.536064832134161229, 12.84367544717937548 ) ) ;
#4461=DIRECTION ( 'NONE',  ( -0.7635533937278216055, -0.02138673900301441000, -0.6453904417649389824 ) ) ;
#4462=ORIENTED_EDGE ( 'NONE', *, *, #9719, .T. ) ;
#4464=CARTESIAN_POINT ( 'NONE',  ( 0.4384471787762819206, -11.63197976518323173, -7.540925784514680430 ) ) ;
#4467=CARTESIAN_POINT ( 'NONE',  ( 3.512766787570746452, -10.40533104696126898, -10.87507422923902034 ) ) ;
#4472=EDGE_CURVE ( 'NONE', #6482, #13762, #11542, .T. ) ;
#4475=CARTESIAN_POINT ( 'NONE',  ( 1.847412631396501803, 7.278870946904251404, 10.09191835241965407 ) ) ;
#4476=ORIENTED_EDGE ( 'NONE', *, *, #4714, .F. ) ;
#4479=( BOUNDED_SURFACE ( )  B_SPLINE_SURFACE ( 3, 1, ( 
 ( #13564, #14998 ),
 ( #485, #12147 ),
 ( #16545, #7567 ),
 ( #10618, #11853 ) ),
 .UNSPECIFIED., .F., .F., .T. ) 
 B_SPLINE_SURFACE_WITH_KNOTS ( ( 4, 4 ),
 ( 2, 2 ),
 ( 0.000000000000000000, 1.000000000000000000 ),
 ( 0.000000000000000000, 1.000000000000000000 ),
 .UNSPECIFIED. ) 
 GEOMETRIC_REPRESENTATION_ITEM ( )  RATIONAL_B_SPLINE_SURFACE ( (
 ( 1.000000000000000000, 1.000000000000000000),
 ( 0.7792777138730158093, 0.9689936506012928330),
 ( 0.7792777138730158093, 0.9689936506012928330),
 ( 1.000000000000000000, 1.000000000000000000) ) ) 
 REPRESENTATION_ITEM ( '' )  SURFACE ( )  );
#4483=ORIENTED_EDGE ( 'NONE', *, *, #2000, .T. ) ;
#4484=FACE_OUTER_BOUND ( 'NONE', #9467, .T. ) ;
#4485=VECTOR ( 'NONE', #6481, 1000.000000000000000 ) ;
#4486=AXIS2_PLACEMENT_3D ( 'NONE', #6509, #12330, #12156 ) ;
#4489=CARTESIAN_POINT ( 'NONE',  ( 2.636624412715093513, -14.14563173255330142, 7.605649742761597665 ) ) ;
#4497=CARTESIAN_POINT ( 'NONE',  ( 0.3150692679895970572, -4.099798979280757649, -13.11337225490256664 ) ) ;
#4506=CARTESIAN_POINT ( 'NONE',  ( 0.3145729642390401870, 0.3065092323351212289, 13.73540280162740501 ) ) ;
#4508=FACE_OUTER_BOUND ( 'NONE', #18140, .T. ) ;
#4511=ORIENTED_EDGE ( 'NONE', *, *, #5487, .T. ) ;
#4514=ORIENTED_EDGE ( 'NONE', *, *, #9413, .F. ) ;
#4516=CARTESIAN_POINT ( 'NONE',  ( 1.342453679581834924, -7.902645620902353230, -12.51077660954474702 ) ) ;
#4521=EDGE_CURVE ( 'NONE', #4455, #7381, #13840, .T. ) ;
#4523=CARTESIAN_POINT ( 'NONE',  ( 3.950837973638668288, 0.000000000000000000, 0.000000000000000000 ) ) ;
#4525=EDGE_CURVE ( 'NONE', #11172, #3195, #1550, .T. ) ;
#4526=CARTESIAN_POINT ( 'NONE',  ( 16.56872352241294521, 0.004564908236400220913, 0.009382111268606271176 ) ) ;
#4527=CARTESIAN_POINT ( 'NONE',  ( 1.254009781011257374, 12.44229282923036628, 7.789615163754328719 ) ) ;
#4528=CARTESIAN_POINT ( 'NONE',  ( 2.747332970342022840, 16.12459247543629814, -2.705255688517677282 ) ) ;
#4529=VERTEX_POINT ( 'NONE', #12777 ) ;
#4530=CARTESIAN_POINT ( 'NONE',  ( 2.002547531651519996, 11.75462648437108015, -4.532360870844206246 ) ) ;
#4531=CARTESIAN_POINT ( 'NONE',  ( 16.56753206892534891, 0.004253784598196178393, -0.008490833999798937798 ) ) ;
#4533=VERTEX_POINT ( 'NONE', #18603 ) ;
#4538=ORIENTED_EDGE ( 'NONE', *, *, #8316, .T. ) ;
#4542=CARTESIAN_POINT ( 'NONE',  ( 2.636624412716062960, -2.161493821598612808, -15.91454522070331912 ) ) ;
#4543=CARTESIAN_POINT ( 'NONE',  ( 0.3132642857406535697, -13.21852905223341601, 3.740125687984681591 ) ) ;
#4546=CARTESIAN_POINT ( 'NONE',  ( 2.705023505549862151, -4.909285963183986468, -12.36217802824811152 ) ) ;
#4547=CARTESIAN_POINT ( 'NONE',  ( 1.847340342630339860, 0.1245571717073309381, 12.44248139376886186 ) ) ;
#4549=CARTESIAN_POINT ( 'NONE',  ( 0.3939822652208154752, 7.545099438012025317, 11.57634296752770453 ) ) ;
#4552=CARTESIAN_POINT ( 'NONE',  ( 1.977228804422059394, -15.33060379559095310, 1.488378900182341091 ) ) ;
#4554=ORIENTED_EDGE ( 'NONE', *, *, #3216, .F. ) ;
#4555=EDGE_LOOP ( 'NONE', ( #5703, #8496, #14934, #1218 ) ) ;
#4556=ORIENTED_EDGE ( 'NONE', *, *, #18749, .F. ) ;
#4572=CARTESIAN_POINT ( 'NONE',  ( 0.3137051932979792457, -10.83767969834796929, -8.442169467526971616 ) ) ;
#4574=VECTOR ( 'NONE', #18016, 1000.000000000000114 ) ;
#4579=FACE_OUTER_BOUND ( 'NONE', #11931, .T. ) ;
#4580=EDGE_CURVE ( 'NONE', #15061, #14742, #3345, .T. ) ;
#4581=ORIENTED_EDGE ( 'NONE', *, *, #4472, .F. ) ;
#4586=CARTESIAN_POINT ( 'NONE',  ( 3.950837973638668288, 14.41405733518061538, -1.958075594453841273 ) ) ;
#4591=CARTESIAN_POINT ( 'NONE',  ( 0.4754618798421162973, 12.98792082933651493, -5.007009103465114741 ) ) ;
#4593=CARTESIAN_POINT ( 'NONE',  ( 1.846138399168762101, 6.971848976711159551, -10.30487220521562541 ) ) ;
#4596=ORIENTED_EDGE ( 'NONE', *, *, #801, .T. ) ;
#4597=CARTESIAN_POINT ( 'NONE',  ( 2.636624412714134280, 2.862162146984768896, 15.80357026013147426 ) ) ;
#4603=CARTESIAN_POINT ( 'NONE',  ( 3.950837973638676281, 6.316429227969464932, 13.10350451991842569 ) ) ;
#4606=ORIENTED_EDGE ( 'NONE', *, *, #3044, .F. ) ;
#4608=CARTESIAN_POINT ( 'NONE',  ( 0.3939822652208120890, -10.75310269629515325, -8.678192463540291612 ) ) ;
#4613=ORIENTED_EDGE ( 'NONE', *, *, #4521, .F. ) ;
#4616=CARTESIAN_POINT ( 'NONE',  ( 0.4754618798421162973, 13.45049478164064638, -3.583352865732528425 ) ) ;
#4620=CARTESIAN_POINT ( 'NONE',  ( 2.353870697619111940, -6.980654702310762794, -10.90705766126227871 ) ) ;
#4621=ORIENTED_EDGE ( 'NONE', *, *, #1423, .F. ) ;
#4623=CARTESIAN_POINT ( 'NONE',  ( 0.3095370825347224519, -10.84046130709064570, 8.444334731363969837 ) ) ;
#4625=ORIENTED_EDGE ( 'NONE', *, *, #16628, .T. ) ;
#4629=CARTESIAN_POINT ( 'NONE',  ( 0.3720661004400037664, 4.951033743989821545, -12.89739157014187221 ) ) ;
#4630=EDGE_CURVE ( 'NONE', #3711, #6002, #10295, .T. ) ;
#4632=ORIENTED_EDGE ( 'NONE', *, *, #13975, .T. ) ;
#4635=EDGE_CURVE ( 'NONE', #10713, #859, #12618, .T. ) ;
#4636=CARTESIAN_POINT ( 'NONE',  ( 0.3151930723728451622, -13.73922999529477451, -0.07645105377001075453 ) ) ;
#4640=CARTESIAN_POINT ( 'NONE',  ( 0.4862570985993235340, -0.7479633556563419772, 13.89016912371017121 ) ) ;
#4642=DIRECTION ( 'NONE',  ( 0.000000000000000000, 0.000000000000000000, 1.000000000000000000 ) ) ;
#4647=CARTESIAN_POINT ( 'NONE',  ( 16.56872352241294521, -0.007512283835805501873, -0.007240717549633963156 ) ) ;
#4649=VERTEX_POINT ( 'NONE', #10587 ) ;
#4652=CARTESIAN_POINT ( 'NONE',  ( 1.845755665166724402, -9.776700214453573068, -7.694641135842929636 ) ) ;
#4654=CARTESIAN_POINT ( 'NONE',  ( 16.56753206892534891, -0.009389754735541561842, 0.001421777558676752366 ) ) ;
#4661=CARTESIAN_POINT ( 'NONE',  ( 16.56872352241294521, -0.001821578298044716857, -0.01027347319884440967 ) ) ;
#4663=EDGE_CURVE ( 'NONE', #13528, #5954, #12918, .T. ) ;
#4664=CARTESIAN_POINT ( 'NONE',  ( 1.959283090834840646, -4.509128209890892691, -11.71721539537259282 ) ) ;
#4665=CARTESIAN_POINT ( 'NONE',  ( 1.977228804421386821, 10.21522664410325021, 11.52787183731143017 ) ) ;
#4666=B_SPLINE_CURVE_WITH_KNOTS ( 'NONE', 3,
 ( #17173, #4085, #12779, #11731, #1507, #3010 ),
 .UNSPECIFIED., .F., .F.,
 ( 4, 2, 4 ),
 ( 1.939479807224432123E-18, 0.001657017934710795738, 0.003314035869421589307 ),
 .UNSPECIFIED. ) ;
#4667=CARTESIAN_POINT ( 'NONE',  ( 0.3145729642390400205, -11.29233589755986600, -7.825496023201434781 ) ) ;
#4668=CARTESIAN_POINT ( 'NONE',  ( 0.3151930723728413319, 4.318364831037771800, -13.04315954105010533 ) ) ;
#4673=ORIENTED_EDGE ( 'NONE', *, *, #6444, .F. ) ;
#4675=ORIENTED_EDGE ( 'NONE', *, *, #12320, .T. ) ;
#4676=DIRECTION ( 'NONE',  ( 0.000000000000000000, 0.000000000000000000, 1.000000000000000000 ) ) ;
#4692=ORIENTED_EDGE ( 'NONE', *, *, #4826, .T. ) ;
#4694=CARTESIAN_POINT ( 'NONE',  ( 3.950837973638677170, 10.51028938476232355, -10.05648675950114956 ) ) ;
#4696=CARTESIAN_POINT ( 'NONE',  ( 0.4862570985993252548, 12.97920246947879441, 5.003653737315533867 ) ) ;
#4697=CIRCLE ( 'NONE', #12020, 16.06066017081991149 ) ;
#4705=CARTESIAN_POINT ( 'NONE',  ( 16.56872352241294521, 0.007240717549633990044, -0.007512283835805476720 ) ) ;
#4709=VERTEX_POINT ( 'NONE', #1891 ) ;
#4714=EDGE_CURVE ( 'NONE', #767, #3595, #18877, .T. ) ;
#4716=CARTESIAN_POINT ( 'NONE',  ( 1.977228804421389485, 13.27756617201186096, 7.806978995470745808 ) ) ;
#4717=CARTESIAN_POINT ( 'NONE',  ( 2.636624412715137034, -11.60464335004055947, 11.10302021257951743 ) ) ;
#4720=CARTESIAN_POINT ( 'NONE',  ( 2.705023505549867924, 12.36217802824812573, -4.909285963183943835 ) ) ;
#4721=CARTESIAN_POINT ( 'NONE',  ( 2.705023505549867036, 12.88681800078732387, 3.294610156755938934 ) ) ;
#4723=VERTEX_POINT ( 'NONE', #3502 ) ;
#4730=CARTESIAN_POINT ( 'NONE',  ( 3.512766787570694493, 2.025881399556607843, -14.91422000116826041 ) ) ;
#4731=CARTESIAN_POINT ( 'NONE',  ( 0.4862570985993235340, -13.44146924561383827, 3.580942890621619412 ) ) ;
#4735=DIRECTION ( 'NONE',  ( 0.000000000000000000, 0.000000000000000000, 1.000000000000000000 ) ) ;
#4738=CARTESIAN_POINT ( 'NONE',  ( 0.3308579732647042304, 7.595989242675130093, 11.46737410776356469 ) ) ;
#4739=CONICAL_SURFACE ( 'NONE', #10538, 14.54644660717763927, 0.8559913436420816257 ) ;
#4740=CARTESIAN_POINT ( 'NONE',  ( 0.3137051932979757485, -4.679953077377398074, -12.91601973349275134 ) ) ;
#4741=EDGE_CURVE ( 'NONE', #14233, #2734, #10121, .T. ) ;
#4742=CARTESIAN_POINT ( 'NONE',  ( 16.56753206892534891, -0.009369540855502119653, -0.001549402974393242162 ) ) ;
#4743=CARTESIAN_POINT ( 'NONE',  ( 1.254009781011620417, -14.64464726212587919, 1.011465182608038305 ) ) ;
#4744=ORIENTED_EDGE ( 'NONE', *, *, #13858, .T. ) ;
#4755=EDGE_CURVE ( 'NONE', #18593, #859, #7976, .T. ) ;
#4757=CARTESIAN_POINT ( 'NONE',  ( 16.58200780006414732, 0.006043560077721704844, 0.009393638146079782980 ) ) ;
#4760=CARTESIAN_POINT ( 'NONE',  ( 0.4862570985993252548, -3.580942890621766406, 13.44146924561379741 ) ) ;
#4765=ORIENTED_EDGE ( 'NONE', *, *, #2853, .F. ) ;
#4772=CARTESIAN_POINT ( 'NONE',  ( 0.3720661004400040439, 4.951033743989640357, 12.89739157014194859 ) ) ;
#4783=CARTESIAN_POINT ( 'NONE',  ( 0.4862570985993235340, 13.89016912371017476, -0.7479633556562934604 ) ) ;
#4784=( BOUNDED_SURFACE ( )  B_SPLINE_SURFACE ( 3, 1, ( 
 ( #15797, #2690 ),
 ( #8537, #7106 ),
 ( #11506, #4243 ),
 ( #15980, #17421 ) ),
 .UNSPECIFIED., .F., .F., .F. ) 
 B_SPLINE_SURFACE_WITH_KNOTS ( ( 4, 4 ),
 ( 2, 2 ),
 ( 0.000000000000000000, 1.000000000000000000 ),
 ( 0.000000000000000000, 1.000000000000000000 ),
 .UNSPECIFIED. ) 
 GEOMETRIC_REPRESENTATION_ITEM ( )  RATIONAL_B_SPLINE_SURFACE ( (
 ( 1.000000000000000000, 1.000000000000000000),
 ( 0.7792777138730160313, 0.9689936506012927220),
 ( 0.7792777138730160313, 0.9689936506012927220),
 ( 1.000000000000000000, 1.000000000000000000) ) ) 
 REPRESENTATION_ITEM ( '' )  SURFACE ( )  );
#4787=CARTESIAN_POINT ( 'NONE',  ( 0.3095370825347224519, 10.84046130709058886, 8.444334731364044444 ) ) ;
#4792=( GEOMETRIC_REPRESENTATION_CONTEXT ( 3 ) GLOBAL_UNCERTAINTY_ASSIGNED_CONTEXT ( ( #17636 ) ) GLOBAL_UNIT_ASSIGNED_CONTEXT ( ( #9937, #13963, #11205 ) ) REPRESENTATION_CONTEXT ( 'NONE', 'WORKASPACE' ) );
#4794=AXIS2_PLACEMENT_3D ( 'NONE', #11229, #17043, #4037 ) ;
#4799=EDGE_CURVE ( 'NONE', #12775, #4529, #5903, .T. ) ;
#4800=VERTEX_POINT ( 'NONE', #8407 ) ;
#4802=ADVANCED_FACE ( 'NONE', ( #14414 ), #3317, .F. ) ;
#4803=CARTESIAN_POINT ( 'NONE',  ( 0.3142014840576500267, 13.73311050063163918, 0.3830336514509360413 ) ) ;
#4805=CARTESIAN_POINT ( 'NONE',  ( 1.959212340397946450, 11.71715421693498449, 4.509090217468559203 ) ) ;
#4806=CARTESIAN_POINT ( 'NONE',  ( 0.4385251269669978580, 3.577373010348713134, 13.39302348765809825 ) ) ;
#4814=CARTESIAN_POINT ( 'NONE',  ( 16.57778382496167424, 0.01482878558584569718, 0.001819584982831951199 ) ) ;
#4816=CARTESIAN_POINT ( 'NONE',  ( 3.950837973638675393, -10.51028938476224894, 10.05648675950122595 ) ) ;
#4819=CARTESIAN_POINT ( 'NONE',  ( 16.56872352241294521, 0.004564908236399969378, -0.009382111268607383134 ) ) ;
#4820=EDGE_LOOP ( 'NONE', ( #5513, #14002, #18082, #4091 ) ) ;
#4822=CARTESIAN_POINT ( 'NONE',  ( 0.3142011359265348691, 10.88514493056454135, -8.382042760265784764 ) ) ;
#4824=CARTESIAN_POINT ( 'NONE',  ( 3.074695600507125981, -2.772091048739183439, -15.30693405987811673 ) ) ;
#4826=EDGE_CURVE ( 'NONE', #9203, #7454, #11654, .T. ) ;
#4827=ADVANCED_FACE ( 'NONE', ( #17194 ), #13249, .T. ) ;
#4829=FACE_OUTER_BOUND ( 'NONE', #686, .T. ) ;
#4830=CARTESIAN_POINT ( 'NONE',  ( 0.3137051932979792457, -13.73004976592201842, -0.4596302728641207813 ) ) ;
#4833=VECTOR ( 'NONE', #7619, 1000.000000000000000 ) ;
#4836=CARTESIAN_POINT ( 'NONE',  ( 3.664313757352960721, 14.16986885736091750, 1.627055439596312159 ) ) ;
#4841=CARTESIAN_POINT ( 'NONE',  ( 1.846524061778021419, -11.71897913237546263, -4.180439405448447054 ) ) ;
#4842=CARTESIAN_POINT ( 'NONE',  ( 0.3939875929385635023, -7.545068896001288827, 11.57636969881031241 ) ) ;
#4847=CARTESIAN_POINT ( 'NONE',  ( 0.3148213771069321987, -7.888490156175138601, -11.24846294176320960 ) ) ;
#4849=CARTESIAN_POINT ( 'NONE',  ( 0.3095370825347234511, -12.91933430393604532, -4.681152801286298626 ) ) ;
#4852=PRODUCT_DEFINITION_CONTEXT ( 'detailed design', #4115, 'design' ) ;
#4854=CARTESIAN_POINT ( 'NONE',  ( 0.4862570985993235340, 0.7479633556564388996, -13.89016912371016765 ) ) ;
#4856=CARTESIAN_POINT ( 'NONE',  ( 16.56822296793089322, -0.0007467251401297892322, -0.01011126603341077311 ) ) ;
#4857=CARTESIAN_POINT ( 'NONE',  ( 16.57210152137263393, -0.01136813053532068768, -0.009075239946108325934 ) ) ;
#4860=FACE_OUTER_BOUND ( 'NONE', #3614, .T. ) ;
#4862=ORIENTED_EDGE ( 'NONE', *, *, #1916, .T. ) ;
#4864=ORIENTED_EDGE ( 'NONE', *, *, #15449, .T. ) ;
#4866=CARTESIAN_POINT ( 'NONE',  ( 1.846822687350015757, -7.075150813727044685, -10.23524390843947529 ) ) ;
#4868=CARTESIAN_POINT ( 'NONE',  ( 2.320520222539028232, 15.43440824797023225, -3.126729907237324912 ) ) ;
#4873=CARTESIAN_POINT ( 'NONE',  ( 2.002547531651519996, -11.75462648437105173, 4.532360870844282630 ) ) ;
#4874=ORIENTED_EDGE ( 'NONE', *, *, #3454, .T. ) ;
#4879=ADVANCED_FACE ( 'NONE', ( #14700 ), #764, .F. ) ;
#4884=CARTESIAN_POINT ( 'NONE',  ( 16.56872352241294521, -0.009207754980064163791, 0.004907101719995779661 ) ) ;
#4886=B_SPLINE_CURVE_WITH_KNOTS ( 'NONE', 3,
 ( #11952, #10520, #389, #13918, #6670, #8982 ),
 .UNSPECIFIED., .F., .F.,
 ( 4, 2, 4 ),
 ( 3.499941646806256644E-17, 0.0001825746017570582086, 0.0003651492035140814518 ),
 .UNSPECIFIED. ) ;
#4894=VERTEX_POINT ( 'NONE', #10612 ) ;
#4895=CARTESIAN_POINT ( 'NONE',  ( 16.56753206892534891, 0.009369540855502530782, -0.001549402974394192573 ) ) ;
#4900=CARTESIAN_POINT ( 'NONE',  ( 0.3308579732646986238, -7.595989242675048381, -11.46737410776362509 ) ) ;
#4902=VERTEX_POINT ( 'NONE', #9072 ) ;
#4904=B_SPLINE_CURVE_WITH_KNOTS ( 'NONE', 3,
 ( #15505, #1064, #5189, #12819 ),
 .UNSPECIFIED., .F., .F.,
 ( 4, 4 ),
 ( 0.000000000000000000, 0.002004993803842713366 ),
 .UNSPECIFIED. ) ;
#4908=CARTESIAN_POINT ( 'NONE',  ( 16.56782317627811096, -0.009814734722107087972, -0.0003415813796005906337 ) ) ;
#4911=CARTESIAN_POINT ( 'NONE',  ( 1.254255976357675717, -14.64488542023465101, -1.011593778944541278 ) ) ;
#4912=CARTESIAN_POINT ( 'NONE',  ( 2.636624412714237309, 7.605649742761960042, 14.14563173255213613 ) ) ;
#4914=ORIENTED_EDGE ( 'NONE', *, *, #17637, .F. ) ;
#4916=VERTEX_POINT ( 'NONE', #16442 ) ;
#4922=CARTESIAN_POINT ( 'NONE',  ( 1.846138399168762101, 11.69739621335927815, -4.238866729160283064 ) ) ;
#4926=CARTESIAN_POINT ( 'NONE',  ( 1.846138399168762101, -10.30487220521565028, -6.971848976711123136 ) ) ;
#4932=EDGE_CURVE ( 'NONE', #16968, #10713, #9111, .T. ) ;
#4934=CARTESIAN_POINT ( 'NONE',  ( 1.847168016377984889, -11.89018175117591980, -3.666915430942724097 ) ) ;
#4936=ORIENTED_EDGE ( 'NONE', *, *, #2348, .T. ) ;
#4938=ORIENTED_EDGE ( 'NONE', *, *, #6158, .T. ) ;
#4946=CARTESIAN_POINT ( 'NONE',  ( 16.57210152137263393, -0.01361613799508957709, 0.005118120558002058063 ) ) ;
#4947=CARTESIAN_POINT ( 'NONE',  ( 1.846138399168762101, -11.69739621335925328, 4.238866729160359448 ) ) ;
#4950=CARTESIAN_POINT ( 'NONE',  ( 3.377929128793395019, 9.234024516648318581, 10.50432311212905923 ) ) ;
#4951=AXIS2_PLACEMENT_3D ( 'NONE', #15564, #14231, #8498 ) ;
#4956=ORIENTED_EDGE ( 'NONE', *, *, #1753, .T. ) ;
#4958=ORIENTED_EDGE ( 'NONE', *, *, #15956, .T. ) ;
#4960=CARTESIAN_POINT ( 'NONE',  ( 3.512766787571010241, 14.81029789862133583, -2.682019731918177996 ) ) ;
#4971=CARTESIAN_POINT ( 'NONE',  ( 2.002547531651519996, -0.6781519942172617998, 12.57989064830759318 ) ) ;
#4973=ORIENTED_EDGE ( 'NONE', *, *, #1340, .T. ) ;
#4974=CARTESIAN_POINT ( 'NONE',  ( 3.074695600507183268, 7.366518011946177502, -13.70113613813200537 ) ) ;
#4975=ORIENTED_EDGE ( 'NONE', *, *, #11491, .T. ) ;
#4981=EDGE_CURVE ( 'NONE', #6753, #6997, #10463, .T. ) ;
#4984=CARTESIAN_POINT ( 'NONE',  ( 0.3132642857406562342, -10.79548167658028213, -8.495623922778184678 ) ) ;
#4990=CARTESIAN_POINT ( 'NONE',  ( 3.950837973638668288, 0.000000000000000000, 0.000000000000000000 ) ) ;
#4991=CARTESIAN_POINT ( 'NONE',  ( 2.636624412714237309, 14.14563173255211126, 7.605649742762011556 ) ) ;
#4996=CARTESIAN_POINT ( 'NONE',  ( 0.3720661004400037664, -13.34435358167255181, 3.575426119359132571 ) ) ;
#4999=CARTESIAN_POINT ( 'NONE',  ( 3.950837973638677170, 6.316429227969654114, -13.10350451991833687 ) ) ;
#5000=EDGE_LOOP ( 'NONE', ( #2046, #9577, #2405, #6108 ) ) ;
#5007=CARTESIAN_POINT ( 'NONE',  ( 16.56822296793089322, 0.002414375228568254022, -0.009847136207496285168 ) ) ;
#5009=CARTESIAN_POINT ( 'NONE',  ( 0.3939822652208125886, 13.34132036472942318, -3.598529276937123544 ) ) ;
#5011=CARTESIAN_POINT ( 'NONE',  ( 2.123976203522053297, -1.531817366691861304, 15.54801196254786255 ) ) ;
#5015=CARTESIAN_POINT ( 'NONE',  ( 2.697797270744666687, -8.537712152180933600, 10.19107313879054466 ) ) ;
#5016=CARTESIAN_POINT ( 'NONE',  ( 0.4862570985993252548, 12.97920246947879441, 5.003653737315533867 ) ) ;
#5019=CARTESIAN_POINT ( 'NONE',  ( 2.002547531651519996, -10.57595306287296921, 6.845637710436153434 ) ) ;
#5022=ORIENTED_EDGE ( 'NONE', *, *, #548, .F. ) ;
#5025=VERTEX_POINT ( 'NONE', #7018 ) ;
#5030=CARTESIAN_POINT ( 'NONE',  ( 3.950837973638675393, 10.05648675950126325, 10.51028938476221342 ) ) ;
#5033=CARTESIAN_POINT ( 'NONE',  ( 2.123976203522053741, -3.347755036806012274, 15.26039569100259108 ) ) ;
#5041=CIRCLE ( 'NONE', #12970, 16.06066017081991149 ) ;
#5043=AXIS2_PLACEMENT_3D ( 'NONE', #3081, #4347, #10172 ) ;
#5046=CARTESIAN_POINT ( 'NONE',  ( 1.254255976358459757, 14.24071337840876694, -3.563435620217374478 ) ) ;
#5047=FACE_OUTER_BOUND ( 'NONE', #7449, .T. ) ;
#5049=VERTEX_POINT ( 'NONE', #12742 ) ;
#5054=EDGE_CURVE ( 'NONE', #14675, #10843, #5917, .T. ) ;
#5057=( BOUNDED_SURFACE ( )  B_SPLINE_SURFACE ( 3, 1, ( 
 ( #12595, #5510 ),
 ( #5336, #11363 ),
 ( #11180, #10107 ),
 ( #3909, #9731 ) ),
 .UNSPECIFIED., .F., .F., .T. ) 
 B_SPLINE_SURFACE_WITH_KNOTS ( ( 4, 4 ),
 ( 2, 2 ),
 ( 0.000000000000000000, 1.000000000000000000 ),
 ( 0.000000000000000000, 1.000000000000000000 ),
 .UNSPECIFIED. ) 
 GEOMETRIC_REPRESENTATION_ITEM ( )  RATIONAL_B_SPLINE_SURFACE ( (
 ( 1.000000000000000000, 1.000000000000000000),
 ( 0.9593108457356467333, 0.9995965569486454649),
 ( 0.9593108457356467333, 0.9995965569486454649),
 ( 1.000000000000000000, 1.000000000000000000) ) ) 
 REPRESENTATION_ITEM ( '' )  SURFACE ( )  );
#5061=CIRCLE ( 'NONE', #790, 16.06066017081991149 ) ;
#5071=B_SPLINE_CURVE_WITH_KNOTS ( 'NONE', 3,
 ( #8810, #16468, #12066, #14638, #15018, #1938 ),
 .UNSPECIFIED., .F., .F.,
 ( 4, 2, 4 ),
 ( 0.000000000000000000, 0.0001828790815886940750, 0.0003657581631773881500 ),
 .UNSPECIFIED. ) ;
#5075=CARTESIAN_POINT ( 'NONE',  ( 2.636624412714237309, 15.80357026013209953, 2.862162146984226663 ) ) ;
#5078=ADVANCED_FACE ( 'NONE', ( #15890 ), #4784, .F. ) ;
#5080=CARTESIAN_POINT ( 'NONE',  ( 1.861628059977341598, 12.44564375541077617, 0.5393144007390715533 ) ) ;
#5083=CARTESIAN_POINT ( 'NONE',  ( 3.377929128793395908, -12.84367544717939680, 5.536064832134110603 ) ) ;
#5084=ORIENTED_EDGE ( 'NONE', *, *, #8168, .F. ) ;
#5088=CARTESIAN_POINT ( 'NONE',  ( 0.8740764193767950330, -14.27348595579787371, -0.8420116711623154560 ) ) ;
#5089=CARTESIAN_POINT ( 'NONE',  ( 16.56822296793089322, 0.005339139727952666586, -0.008619100080559792543 ) ) ;
#5092=LINE ( 'NONE', #797, #10325 ) ;
#5095=DIRECTION ( 'NONE',  ( -1.000000000000000000, -0.000000000000000000, -0.000000000000000000 ) ) ;
#5100=FACE_OUTER_BOUND ( 'NONE', #16616, .T. ) ;
#5101=ADVANCED_FACE ( 'NONE', ( #4330 ), #6743, .F. ) ;
#5102=B_SPLINE_CURVE_WITH_KNOTS ( 'NONE', 3,
 ( #12500, #9363, #6777, #5237, #6860, #12684, #3712, #848, #18511, #5421, #8211, #756, #15195 ),
 .UNSPECIFIED., .F., .F.,
 ( 4, 3, 3, 3, 4 ),
 ( 2.453269466693398698E-18, 0.0002299804304191500187, 0.0004599608082120258223, 0.0006467586077648020170, 0.0008336169836825994828 ),
 .UNSPECIFIED. ) ;
#5104=CARTESIAN_POINT ( 'NONE',  ( 0.3132642857406530146, 13.21852905223344088, -3.740125687984594993 ) ) ;
#5107=EDGE_CURVE ( 'NONE', #13762, #8587, #15031, .T. ) ;
#5108=CARTESIAN_POINT ( 'NONE',  ( 16.57210152137263393, -0.01402404281923042353, -0.003862718596009419997 ) ) ;
#5110=CARTESIAN_POINT ( 'NONE',  ( 1.845755665166725068, 10.33920510797153369, -6.920419570228236950 ) ) ;
#5111=CARTESIAN_POINT ( 'NONE',  ( 1.254255976358046087, 5.487601330835574664, -13.61551404021248857 ) ) ;
#5112=CIRCLE ( 'NONE', #14261, 14.54644660717763927 ) ;
#5113=CARTESIAN_POINT ( 'NONE',  ( 16.56782317627811096, 0.0003415813796014688375, 0.009814734722106369796 ) ) ;
#5114=CARTESIAN_POINT ( 'NONE',  ( 0.4862570985993235340, -12.97920246947883172, 5.003653737315437944 ) ) ;
#5126=B_SPLINE_CURVE_WITH_KNOTS ( 'NONE', 3,
 ( #16687, #3590, #18208, #8089, #13899, #3770 ),
 .UNSPECIFIED., .F., .F.,
 ( 4, 2, 4 ),
 ( 3.144186300207962859E-18, 0.0002017457492448081777, 0.0004034914984896132112 ),
 .UNSPECIFIED. ) ;
#5133=CARTESIAN_POINT ( 'NONE',  ( 0.3170788640506440603, -4.100430649997872656, -13.11595226728161911 ) ) ;
#5138=ORIENTED_EDGE ( 'NONE', *, *, #2143, .T. ) ;
#5140=FACE_OUTER_BOUND ( 'NONE', #527, .T. ) ;
#5143=DIRECTION ( 'NONE',  ( 0.7635533937278216055, 0.3966532189476633663, -0.5095610256143844330 ) ) ;
#5144=CARTESIAN_POINT ( 'NONE',  ( 3.950837973638676281, 10.05648675950141602, -10.51028938476206953 ) ) ;
#5148=CARTESIAN_POINT ( 'NONE',  ( 2.002547531651519996, -7.942910686618240845, 9.778737580845669797 ) ) ;
#5156=ADVANCED_FACE ( 'NONE', ( #7690 ), #3434, .F. ) ;
#5157=EDGE_CURVE ( 'NONE', #5049, #6997, #14777, .T. ) ;
#5159=B_SPLINE_CURVE_WITH_KNOTS ( 'NONE', 3,
 ( #10699, #9163, #10893, #7841 ),
 .UNSPECIFIED., .F., .F.,
 ( 4, 4 ),
 ( 0.000000000000000000, 0.002004993803842800969 ),
 .UNSPECIFIED. ) ;
#5160=AXIS2_PLACEMENT_3D ( 'NONE', #10028, #15862, #1917 ) ;
#5162=ORIENTED_EDGE ( 'NONE', *, *, #9337, .F. ) ;
#5166=ORIENTED_EDGE ( 'NONE', *, *, #11622, .T. ) ;
#5174=AXIS2_PLACEMENT_3D ( 'NONE', #9830, #15662, #8410 ) ;
#5181=CARTESIAN_POINT ( 'NONE',  ( 0.4862570985993235340, 8.769551628660735787, 10.79774104611376373 ) ) ;
#5182=CARTESIAN_POINT ( 'NONE',  ( 1.846138399168762989, -4.238866729160486457, 11.69739621335920710 ) ) ;
#5185=CARTESIAN_POINT ( 'NONE',  ( 3.950837973638675393, -13.10350451991835818, -6.316429227969608817 ) ) ;
#5186=EDGE_CURVE ( 'NONE', #10401, #1657, #2042, .T. ) ;
#5189=CARTESIAN_POINT ( 'NONE',  ( 3.074695600507260984, -10.75417554975707013, 11.23985886659431621 ) ) ;
#5193=CARTESIAN_POINT ( 'NONE',  ( 0.4385251269669947494, 13.39302348765813910, -3.577373010348575910 ) ) ;
#5194=EDGE_CURVE ( 'NONE', #471, #8324, #8201, .T. ) ;
#5197=CARTESIAN_POINT ( 'NONE',  ( 16.56753206892534891, 0.001421777558676785977, 0.009389754735541558373 ) ) ;
#5201=( BOUNDED_SURFACE ( )  B_SPLINE_SURFACE ( 3, 1, ( 
 ( #13109, #14725 ),
 ( #13296, #5546 ),
 ( #18842, #5931 ),
 ( #5736, #17407 ) ),
 .UNSPECIFIED., .F., .F., .T. ) 
 B_SPLINE_SURFACE_WITH_KNOTS ( ( 4, 4 ),
 ( 2, 2 ),
 ( 0.000000000000000000, 1.000000000000000000 ),
 ( 0.000000000000000000, 1.000000000000000000 ),
 .UNSPECIFIED. ) 
 GEOMETRIC_REPRESENTATION_ITEM ( )  RATIONAL_B_SPLINE_SURFACE ( (
 ( 1.000000000000000000, 1.000000000000000000),
 ( 0.9593108457356467333, 0.9995965569486454649),
 ( 0.9593108457356467333, 0.9995965569486454649),
 ( 1.000000000000000000, 1.000000000000000000) ) ) 
 REPRESENTATION_ITEM ( '' )  SURFACE ( )  );
#5203=AXIS2_PLACEMENT_3D ( 'NONE', #3255, #9100, #14057 ) ;
#5204=CARTESIAN_POINT ( 'NONE',  ( 2.705023505549863039, 13.27418276223636084, -0.8488853074253436271 ) ) ;
#5209=ORIENTED_EDGE ( 'NONE', *, *, #6980, .T. ) ;
#5215=EDGE_CURVE ( 'NONE', #13145, #698, #14787, .T. ) ;
#5217=CARTESIAN_POINT ( 'NONE',  ( 1.959212340397962882, -12.53706137681889210, -0.6675998551413099280 ) ) ;
#5229=ORIENTED_EDGE ( 'NONE', *, *, #3588, .F. ) ;
#5233=CARTESIAN_POINT ( 'NONE',  ( 2.353870697619111052, -12.05847592522640355, -4.720869121224258613 ) ) ;
#5237=CARTESIAN_POINT ( 'NONE',  ( 1.847168016377981781, 10.17509564929258836, 7.161712042621497076 ) ) ;
#5240=CARTESIAN_POINT ( 'NONE',  ( 2.002547531651519996, 0.6781519942171739812, 12.57989064830759851 ) ) ;
#5242=CARTESIAN_POINT ( 'NONE',  ( 1.918921323896324971, -6.832782632379298171, -10.48468902844559913 ) ) ;
#5253=ORIENTED_EDGE ( 'NONE', *, *, #6704, .F. ) ;
#5254=CARTESIAN_POINT ( 'NONE',  ( 2.636624412715138366, -15.91454522070249311, -2.161493821597819665 ) ) ;
#5256=ORIENTED_EDGE ( 'NONE', *, *, #4095, .T. ) ;
#5258=CARTESIAN_POINT ( 'NONE',  ( 0.4384471787762834749, 13.84291427302851574, -0.7363690479466810102 ) ) ;
#5261=EDGE_CURVE ( 'NONE', #17548, #7381, #12172, .T. ) ;
#5262=ADVANCED_FACE ( 'NONE', ( #16568 ), #8674, .F. ) ;
#5263=CARTESIAN_POINT ( 'NONE',  ( 8.438534575730034959, 6.862570336891075762, 0.2320579683290369954 ) ) ;
#5268=ORIENTED_EDGE ( 'NONE', *, *, #9337, .T. ) ;
#5273=( BOUNDED_SURFACE ( )  B_SPLINE_SURFACE ( 3, 1, ( 
 ( #4884, #15099 ),
 ( #587, #3533 ),
 ( #12325, #2821 ),
 ( #8577, #15641 ) ),
 .UNSPECIFIED., .F., .F., .T. ) 
 B_SPLINE_SURFACE_WITH_KNOTS ( ( 4, 4 ),
 ( 2, 2 ),
 ( 0.000000000000000000, 1.000000000000000000 ),
 ( 0.000000000000000000, 1.000000000000000000 ),
 .UNSPECIFIED. ) 
 GEOMETRIC_REPRESENTATION_ITEM ( )  RATIONAL_B_SPLINE_SURFACE ( (
 ( 1.000000000000000000, 1.000000000000000000),
 ( 0.7792777138730160313, 0.9689936506012927220),
 ( 0.7792777138730160313, 0.9689936506012927220),
 ( 1.000000000000000000, 1.000000000000000000) ) ) 
 REPRESENTATION_ITEM ( '' )  SURFACE ( )  );
#5279=CARTESIAN_POINT ( 'NONE',  ( 0.3308579732647030647, -4.812490080619291177, 12.88563776947744088 ) ) ;
#5281=CARTESIAN_POINT ( 'NONE',  ( 16.56782317627811096, 0.003357783021327236019, -0.009228812961909608689 ) ) ;
#5284=ADVANCED_FACE ( 'NONE', ( #8153 ), #10274, .T. ) ;
#5286=EDGE_CURVE ( 'NONE', #15079, #12032, #8864, .T. ) ;
#5295=CARTESIAN_POINT ( 'NONE',  ( 3.353306896162453477, -12.02594772223101494, 7.069984850384768649 ) ) ;
#5296=CARTESIAN_POINT ( 'NONE',  ( 0.4754618798421162973, 8.775436892861113947, 10.80499583390515994 ) ) ;
#5299=EDGE_LOOP ( 'NONE', ( #6978, #9402, #3266, #13239 ) ) ;
#5306=( BOUNDED_SURFACE ( )  B_SPLINE_SURFACE ( 3, 1, ( 
 ( #13466, #13669 ),
 ( #383, #12145 ),
 ( #6207, #9171 ),
 ( #7753, #13562 ) ),
 .UNSPECIFIED., .F., .F., .T. ) 
 B_SPLINE_SURFACE_WITH_KNOTS ( ( 4, 4 ),
 ( 2, 2 ),
 ( 0.000000000000000000, 1.000000000000000000 ),
 ( 0.000000000000000000, 1.000000000000000000 ),
 .UNSPECIFIED. ) 
 GEOMETRIC_REPRESENTATION_ITEM ( )  RATIONAL_B_SPLINE_SURFACE ( (
 ( 1.000000000000000000, 1.000000000000000000),
 ( 0.9933953342250436691, 0.8357391271907733676),
 ( 0.9933953342250436691, 0.8357391271907733676),
 ( 1.000000000000000000, 1.000000000000000000) ) ) 
 REPRESENTATION_ITEM ( '' )  SURFACE ( )  );
#5314=ORIENTED_EDGE ( 'NONE', *, *, #11516, .F. ) ;
#5316=ORIENTED_EDGE ( 'NONE', *, *, #7146, .F. ) ;
#5323=CARTESIAN_POINT ( 'NONE',  ( 0.3170788640506440603, -13.74111462631963398, -0.1533108587037582682 ) ) ;
#5328=CARTESIAN_POINT ( 'NONE',  ( 0.4754618798421162973, 8.775436892861270266, -10.80499583390503382 ) ) ;
#5336=CARTESIAN_POINT ( 'NONE',  ( 16.56679352167444819, 0.006526964904752955397, 0.006618561353599231728 ) ) ;
#5337=CARTESIAN_POINT ( 'NONE',  ( 0.8740764193769091639, -3.609949042658162188, -13.83508774436024957 ) ) ;
#5342=CARTESIAN_POINT ( 'NONE',  ( 0.3058872367615230181, 0.6080468242580958638, 13.72992299905060243 ) ) ;
#5343=ORIENTED_EDGE ( 'NONE', *, *, #2076, .T. ) ;
#5344=CARTESIAN_POINT ( 'NONE',  ( 16.58200780006414732, 0.008650561019685530303, -0.007066318000004736047 ) ) ;
#5346=DIRECTION ( 'NONE',  ( -1.000000000000000000, -0.000000000000000000, -0.000000000000000000 ) ) ;
#5351=DIRECTION ( 'NONE',  ( -0.7635533937278214944, 0.6071939193889607234, -0.2197766120036399873 ) ) ;
#5357=CARTESIAN_POINT ( 'NONE',  ( 3.074695600508759785, 15.30693405987895694, 2.772091048737280072 ) ) ;
#5362=CARTESIAN_POINT ( 'NONE',  ( 0.000000000000000000, 6.799999999999999822, 1.500000000000000000 ) ) ;
#5364=ORIENTED_EDGE ( 'NONE', *, *, #10049, .F. ) ;
#5365=CARTESIAN_POINT ( 'NONE',  ( 2.747332970342022840, -7.289199830147006232, -14.63517873738954655 ) ) ;
#5366=VECTOR ( 'NONE', #3710, 1000.000000000000000 ) ;
#5371=ORIENTED_EDGE ( 'NONE', *, *, #13574, .T. ) ;
#5373=DIRECTION ( 'NONE',  ( -1.000000000000000000, -0.000000000000000000, -0.000000000000000000 ) ) ;
#5374=ORIENTED_EDGE ( 'NONE', *, *, #269, .F. ) ;
#5378=PLANE ( 'NONE',  #4794 ) ;
#5379=UNCERTAINTY_MEASURE_WITH_UNIT (LENGTH_MEASURE( 1.000000000000000082E-05 ), #992, 'distance_accuracy_value', 'NONE');
#5387=CARTESIAN_POINT ( 'NONE',  ( 3.377929128793396796, -1.296196549818846355, -13.92579934231097560 ) ) ;
#5391=CARTESIAN_POINT ( 'NONE',  ( 3.664313757352973600, -12.42002390572631221, 7.012524439851453906 ) ) ;
#5392=PRESENTATION_STYLE_ASSIGNMENT (( #18481 ) ) ;
#5393=ORIENTED_EDGE ( 'NONE', *, *, #15943, .F. ) ;
#5394=ADVANCED_FACE ( 'NONE', ( #9942 ), #6125, .F. ) ;
#5400=CARTESIAN_POINT ( 'NONE',  ( 0.3137051932979757485, 12.91601973349276733, -4.679953077377353665 ) ) ;
#5404=CARTESIAN_POINT ( 'NONE',  ( 3.950837973638676281, 13.10350451991840615, 6.316429227969512894 ) ) ;
#5415=EDGE_CURVE ( 'NONE', #16059, #15061, #7895, .T. ) ;
#5421=CARTESIAN_POINT ( 'NONE',  ( 1.847034903785825577, 9.929438108952146180, 7.498375632854650696 ) ) ;
#5422=CARTESIAN_POINT ( 'NONE',  ( 1.562796894703937678, 6.799999999999999822, 1.500000000000000000 ) ) ;
#5427=DIRECTION ( 'NONE',  ( 0.000000000000000000, 0.000000000000000000, 1.000000000000000000 ) ) ;
#5429=DIRECTION ( 'NONE',  ( 0.000000000000000000, 0.000000000000000000, 1.000000000000000000 ) ) ;
#5432=VERTEX_POINT ( 'NONE', #4120 ) ;
#5436=CARTESIAN_POINT ( 'NONE',  ( 0.3095370825347233956, -10.84046130709064393, 8.444334731363969837 ) ) ;
#5440=EDGE_CURVE ( 'NONE', #1445, #4455, #16775, .T. ) ;
#5442=CARTESIAN_POINT ( 'NONE',  ( 3.950837973638676281, 2.591948120962007884, -14.31366178983250670 ) ) ;
#5446=CARTESIAN_POINT ( 'NONE',  ( 0.4862570985993235340, -13.89016912371016943, -0.7479633556563904939 ) ) ;
#5451=CARTESIAN_POINT ( 'NONE',  ( 2.636624412716902288, 7.605649742760546950, -14.14563173255513995 ) ) ;
#5455=CARTESIAN_POINT ( 'NONE',  ( 0.3308579732647004001, 0.5950689966506276241, -13.74211098745268345 ) ) ;
#5457=ORIENTED_EDGE ( 'NONE', *, *, #11252, .T. ) ;
#5460=ORIENTED_EDGE ( 'NONE', *, *, #13691, .T. ) ;
#5461=CARTESIAN_POINT ( 'NONE',  ( 0.4754618798421167414, 0.7484603771386338922, -13.89949764182681768 ) ) ;
#5464=CARTESIAN_POINT ( 'NONE',  ( 0.3151930723728477157, -11.16020735774772277, 8.013866567350856229 ) ) ;
#5465=CARTESIAN_POINT ( 'NONE',  ( 3.512766787570727356, 6.535475144497194577, -13.55823433651945464 ) ) ;
#5473=CARTESIAN_POINT ( 'NONE',  ( 1.861628059977344263, -0.5393144007391119654, 12.44564375541076728 ) ) ;
#5486=EDGE_CURVE ( 'NONE', #10168, #14610, #4216, .T. ) ;
#5487=EDGE_CURVE ( 'NONE', #16059, #9890, #2345, .T. ) ;
#5490=CARTESIAN_POINT ( 'NONE',  ( 2.123976203522053741, 3.347755036806118856, -15.26039569100256266 ) ) ;
#5491=CARTESIAN_POINT ( 'NONE',  ( 0.3142014840576517476, -13.17932813834297434, 3.879477880151391833 ) ) ;
#5493=ORIENTED_EDGE ( 'NONE', *, *, #3866, .F. ) ;
#5494=B_SPLINE_CURVE_WITH_KNOTS ( 'NONE', 3,
 ( #8716, #5737, #18843, #10147, #14541, #12734, #4132, #8618, #1456, #12915, #4410, #7295, #4033 ),
 .UNSPECIFIED., .F., .F.,
 ( 4, 3, 3, 3, 4 ),
 ( 1.734723475976807094E-18, 0.0002299780670421052245, 0.0004599561239687887651, 0.0006896788984287890393, 0.0009194956271626402800 ),
 .UNSPECIFIED. ) ;
#5496=ORIENTED_EDGE ( 'NONE', *, *, #566, .F. ) ;
#5498=EDGE_CURVE ( 'NONE', #18306, #11651, #5577, .T. ) ;
#5502=CARTESIAN_POINT ( 'NONE',  ( 2.320520222536567090, 11.60169517779319293, 10.64885284334832960 ) ) ;
#5510=CARTESIAN_POINT ( 'NONE',  ( 0.3095370825347224519, -11.38092634279622928, -7.700448427571997989 ) ) ;
#5513=ORIENTED_EDGE ( 'NONE', *, *, #3086, .T. ) ;
#5514=EDGE_CURVE ( 'NONE', #799, #15883, #8701, .T. ) ;
#5516=EDGE_LOOP ( 'NONE', ( #17627, #865, #11953, #1682 ) ) ;
#5517=CARTESIAN_POINT ( 'NONE',  ( 0.3939875929385661668, 4.930599594904554017, 12.90850834464102270 ) ) ;
#5518=VERTEX_POINT ( 'NONE', #7471 ) ;
#5520=CARTESIAN_POINT ( 'NONE',  ( 0.4754618798421162973, -10.80499583390518836, 8.775436892861078420 ) ) ;
#5527=CARTESIAN_POINT ( 'NONE',  ( 1.846613052777652531, -3.520031056876387954, 11.93415846513960332 ) ) ;
#5528=CARTESIAN_POINT ( 'NONE',  ( 0.3145734862173232838, -3.953068532979906458, -13.15783074029282673 ) ) ;
#5529=CARTESIAN_POINT ( 'NONE',  ( 1.846138399168762101, 12.43476674860266584, -0.4167076046095982700 ) ) ;
#5530=CARTESIAN_POINT ( 'NONE',  ( 0.000000000000000000, 0.000000000000000000, -1.500000000000000000 ) ) ;
#5536=CARTESIAN_POINT ( 'NONE',  ( 3.950837973638676281, -14.41405733518061716, 1.958075594453740687 ) ) ;
#5537=EDGE_LOOP ( 'NONE', ( #17841, #16364, #7550, #5084 ) ) ;
#5543=CARTESIAN_POINT ( 'NONE',  ( 0.3151928479966099039, 0.07658992383256929548, -13.73922861026898623 ) ) ;
#5546=CARTESIAN_POINT ( 'NONE',  ( 0.3170788640506441158, -4.100430649998053845, 13.11595226728156405 ) ) ;
#5553=FACE_OUTER_BOUND ( 'NONE', #9062, .T. ) ;
#5554=CARTESIAN_POINT ( 'NONE',  ( 8.438534575730034959, 6.598402093327905504, -1.899950616255119407 ) ) ;
#5560=FILL_AREA_STYLE ('',( #2603 ) ) ;
#5570=EDGE_CURVE ( 'NONE', #1472, #8587, #17607, .T. ) ;
#5577=B_SPLINE_CURVE_WITH_KNOTS ( 'NONE', 3,
 ( #4694, #10523, #16058, #4310 ),
 .UNSPECIFIED., .F., .F.,
 ( 4, 4 ),
 ( 2.359479019930958314E-17, 0.003005512676784853534 ),
 .UNSPECIFIED. ) ;
#5579=CARTESIAN_POINT ( 'NONE',  ( 8.438534575730034959, 3.845978796786037268, 5.688336279099058146 ) ) ;
#5585=EDGE_LOOP ( 'NONE', ( #13903, #12683, #8675, #14963 ) ) ;
#5587=EDGE_CURVE ( 'NONE', #13548, #11500, #18357, .T. ) ;
#5590=CARTESIAN_POINT ( 'NONE',  ( 0.3145734862173252266, 8.321353293018990627, -10.93207848441423913 ) ) ;
#5595=CIRCLE ( 'NONE', #3786, 14.54644660717763927 ) ;
#5604=DIRECTION ( 'NONE',  ( -1.000000000000000000, -0.000000000000000000, -0.000000000000000000 ) ) ;
#5605=CARTESIAN_POINT ( 'NONE',  ( 16.56753206892534891, -0.006760771273036220858, -0.006669401563384898778 ) ) ;
#5611=ORIENTED_EDGE ( 'NONE', *, *, #10206, .F. ) ;
#5612=ADVANCED_FACE ( 'NONE', ( #18072 ), #18444, .F. ) ;
#5616=CARTESIAN_POINT ( 'NONE',  ( 1.845756295923359769, -11.97166802574123423, -3.386818134580184658 ) ) ;
#5625=VECTOR ( 'NONE', #5143, 1000.000000000000114 ) ;
#5628=CARTESIAN_POINT ( 'NONE',  ( 1.847168016377982669, 7.161712042621604546, -10.17509564929251020 ) ) ;
#5629=CARTESIAN_POINT ( 'NONE',  ( 1.861628059977344263, 6.879051339207292948, 10.38573835516714716 ) ) ;
#5631=CARTESIAN_POINT ( 'NONE',  ( 16.56679352167444819, -0.001518074900130714439, 0.009170718284672536857 ) ) ;
#5632=CARTESIAN_POINT ( 'NONE',  ( 0.3151928476913548050, -13.06684726503523919, -4.245457024760359133 ) ) ;
#5633=ORIENTED_EDGE ( 'NONE', *, *, #3300, .T. ) ;
#5635=CARTESIAN_POINT ( 'NONE',  ( 2.002547531651519996, 12.57989064830759496, -0.6781519942172177240 ) ) ;
#5638=CARTESIAN_POINT ( 'NONE',  ( 16.56753206892534891, -0.009369540855502522109, 0.001549402974394259360 ) ) ;
#5642=CARTESIAN_POINT ( 'NONE',  ( 0.3137051932979792457, -11.37800749014136592, 7.698472063774431717 ) ) ;
#5644=( BOUNDED_SURFACE ( )  B_SPLINE_SURFACE ( 3, 1, ( 
 ( #3060, #13019 ),
 ( #7395, #2870 ),
 ( #3161, #10251 ),
 ( #5646, #10153 ) ),
 .UNSPECIFIED., .F., .F., .T. ) 
 B_SPLINE_SURFACE_WITH_KNOTS ( ( 4, 4 ),
 ( 2, 2 ),
 ( 0.000000000000000000, 1.000000000000000000 ),
 ( 0.000000000000000000, 1.000000000000000000 ),
 .UNSPECIFIED. ) 
 GEOMETRIC_REPRESENTATION_ITEM ( )  RATIONAL_B_SPLINE_SURFACE ( (
 ( 1.000000000000000000, 1.000000000000000000),
 ( 0.7792777138730158093, 0.9689936506012928330),
 ( 0.7792777138730158093, 0.9689936506012928330),
 ( 1.000000000000000000, 1.000000000000000000) ) ) 
 REPRESENTATION_ITEM ( '' )  SURFACE ( )  );
#5645=CARTESIAN_POINT ( 'NONE',  ( 2.636624412715137478, -2.862162146983530775, 15.80357026013314048 ) ) ;
#5646=CARTESIAN_POINT ( 'NONE',  ( 16.56872352241294521, -0.007240717549633941472, -0.007512283835804289302 ) ) ;
#5651=CARTESIAN_POINT ( 'NONE',  ( 16.56782317627811096, -0.006045301465876687375, -0.007739510688078416953 ) ) ;
#5653=CARTESIAN_POINT ( 'NONE',  ( 3.353306896162453477, -10.44017738170049903, -9.252610477110389198 ) ) ;
#5654=CARTESIAN_POINT ( 'NONE',  ( 0.3095370825347233956, 8.444334731364008917, 10.84046130709061373 ) ) ;
#5655=ORIENTED_EDGE ( 'NONE', *, *, #8895, .T. ) ;
#5660=ADVANCED_FACE ( 'NONE', ( #16457 ), #18256, .T. ) ;
#5665=CARTESIAN_POINT ( 'NONE',  ( 0.3150692679895968906, 13.11337225490258263, -4.099798979280710576 ) ) ;
#5670=CARTESIAN_POINT ( 'NONE',  ( 16.56679352167444819, -0.006526964904752395082, 0.006618561353600064395 ) ) ;
#5671=CARTESIAN_POINT ( 'NONE',  ( 2.636624412715137034, -11.60464335004055947, 11.10302021257951743 ) ) ;
#5676=ORIENTED_EDGE ( 'NONE', *, *, #3834, .T. ) ;
#5677=AXIS2_PLACEMENT_3D ( 'NONE', #16675, #8173, #13986 ) ;
#5679=ORIENTED_EDGE ( 'NONE', *, *, #7639, .T. ) ;
#5685=CARTESIAN_POINT ( 'NONE',  ( 2.636624412716062515, -6.973567714909003179, -14.46769361191335790 ) ) ;
#5689=CIRCLE ( 'NONE', #16409, 13.42403576283810906 ) ;
#5690=DIRECTION ( 'NONE',  ( -1.000000000000000000, -0.000000000000000000, -0.000000000000000000 ) ) ;
#5695=DIRECTION ( 'NONE',  ( -1.000000000000000000, -0.000000000000000000, -0.000000000000000000 ) ) ;
#5697=B_SPLINE_CURVE_WITH_KNOTS ( 'NONE', 3,
 ( #9640, #13942, #14930, #1847, #12596, #16376, #13401, #7687, #3262, #15025, #3720, #14040, #8040 ),
 .UNSPECIFIED., .F., .F.,
 ( 4, 3, 3, 3, 4 ),
 ( 3.878959614448864246E-18, 0.0002299780670421069050, 0.0004599561239687931019, 0.0006896788984287867625, 0.0009194956271626391958 ),
 .UNSPECIFIED. ) ;
#5700=ORIENTED_EDGE ( 'NONE', *, *, #4312, .F. ) ;
#5702=VERTEX_POINT ( 'NONE', #2996 ) ;
#5703=ORIENTED_EDGE ( 'NONE', *, *, #14176, .T. ) ;
#5708=CARTESIAN_POINT ( 'NONE',  ( 3.074695600507137083, -11.23985886659436773, -10.75417554975720869 ) ) ;
#5709=B_SPLINE_CURVE_WITH_KNOTS ( 'NONE', 3,
 ( #4912, #12178, #13702, #9490, #16573, #3466 ),
 .UNSPECIFIED., .F., .F.,
 ( 4, 2, 4 ),
 ( 0.000000000000000000, 0.001656992708822040920, 0.003313985417644081839 ),
 .UNSPECIFIED. ) ;
#5712=CARTESIAN_POINT ( 'NONE',  ( 16.57778382496167424, -0.01306626476309383916, -0.007244066302947642193 ) ) ;
#5713=VECTOR ( 'NONE', #6370, 1000.000000000000227 ) ;
#5714=CARTESIAN_POINT ( 'NONE',  ( 1.845755665166726844, 3.386720041070728104, 11.97169564665392727 ) ) ;
#5717=B_SPLINE_CURVE_WITH_KNOTS ( 'NONE', 3,
 ( #14082, #9960, #12552, #18566, #6823, #11043 ),
 .UNSPECIFIED., .F., .F.,
 ( 4, 2, 4 ),
 ( 0.000000000000000000, 0.0001828790815886955387, 0.0003657581631773888006 ),
 .UNSPECIFIED. ) ;
#5720=ADVANCED_FACE ( 'NONE', ( #946 ), #873, .F. ) ;
#5729=DIRECTION ( 'NONE',  ( 0.000000000000000000, 0.000000000000000000, 1.000000000000000000 ) ) ;
#5730=CARTESIAN_POINT ( 'NONE',  ( 0.3145729642390373559, -13.15786090015081555, -3.952965287571249764 ) ) ;
#5735=EDGE_LOOP ( 'NONE', ( #12939, #14826, #4462, #12444 ) ) ;
#5736=CARTESIAN_POINT ( 'NONE',  ( 16.56753206892534891, -0.001549402974394225099, -0.009369540855502527313 ) ) ;
#5737=CARTESIAN_POINT ( 'NONE',  ( 0.3142014840576534684, -4.608051180497015231, 12.94260032291127160 ) ) ;
#5738=CARTESIAN_POINT ( 'NONE',  ( 0.3148208552358952028, -10.97826876274317875, 8.260375059853302560 ) ) ;
#5748=ORIENTED_EDGE ( 'NONE', *, *, #15596, .T. ) ;
#5761=ADVANCED_FACE ( 'NONE', ( #1031 ), #11146, .F. ) ;
#5764=CARTESIAN_POINT ( 'NONE',  ( 0.3095370825347234511, -10.84046130709052314, -8.444334731364126156 ) ) ;
#5771=CARTESIAN_POINT ( 'NONE',  ( 2.123976203522053741, 13.47898556379313284, 7.899625852120258251 ) ) ;
#5773=ORIENTED_EDGE ( 'NONE', *, *, #14557, .F. ) ;
#5775=VERTEX_POINT ( 'NONE', #15646 ) ;
#5776=ORIENTED_EDGE ( 'NONE', *, *, #13131, .F. ) ;
#5781=B_SPLINE_CURVE_WITH_KNOTS ( 'NONE', 3,
 ( #15033, #16182, #4720, #4530 ),
 .UNSPECIFIED., .F., .F.,
 ( 4, 4 ),
 ( 1.927807806696441531E-17, 0.003005512676784856570 ),
 .UNSPECIFIED. ) ;
#5782=CARTESIAN_POINT ( 'NONE',  ( 0.8740779401510756497, -5.211551231203870316, -13.31469722824378721 ) ) ;
#5784=VERTEX_POINT ( 'NONE', #8312 ) ;
#5789=CARTESIAN_POINT ( 'NONE',  ( 2.123976203522053297, -3.347755036805797779, -15.26039569100262838 ) ) ;
#5792=CARTESIAN_POINT ( 'NONE',  ( 2.002547531651521773, 9.778737580845699995, 7.942910686618207983 ) ) ;
#5795=CARTESIAN_POINT ( 'NONE',  ( 2.697797270744668463, 4.970631985779762729, -12.33058466479263693 ) ) ;
#5799=ORIENTED_EDGE ( 'NONE', *, *, #3967, .T. ) ;
#5801=VERTEX_POINT ( 'NONE', #1131 ) ;
#5807=CARTESIAN_POINT ( 'NONE',  ( 8.438534575730034959, 5.688336279099100778, -3.845978796785973763 ) ) ;
#5809=ORIENTED_EDGE ( 'NONE', *, *, #12320, .F. ) ;
#5810=CARTESIAN_POINT ( 'NONE',  ( 1.845755665166725290, 0.4784952423730285953, -12.43231320373360660 ) ) ;
#5811=EDGE_CURVE ( 'NONE', #14913, #8937, #9227, .T. ) ;
#5812=CARTESIAN_POINT ( 'NONE',  ( 1.861628059977344263, 3.332996951203627933, 12.00316790821102941 ) ) ;
#5815=CARTESIAN_POINT ( 'NONE',  ( 1.847247051441591070, 11.78111530882023317, 4.004229874809065670 ) ) ;
#5823=ORIENTED_EDGE ( 'NONE', *, *, #9025, .T. ) ;
#5824=CARTESIAN_POINT ( 'NONE',  ( 3.950837973638676281, -6.316429227969562632, 13.10350451991838128 ) ) ;
#5838=FACE_OUTER_BOUND ( 'NONE', #5585, .T. ) ;
#5841=CARTESIAN_POINT ( 'NONE',  ( 0.3132635586635977853, 10.79541209008116454, -8.495712071659280440 ) ) ;
#5843=CARTESIAN_POINT ( 'NONE',  ( 16.56753206892534891, 0.008490833999798002782, -0.004253784598196794220 ) ) ;
#5845=ORIENTED_EDGE ( 'NONE', *, *, #7440, .F. ) ;
#5847=CARTESIAN_POINT ( 'NONE',  ( 0.3095370825347224519, -12.91933430393611282, 4.681152801286110332 ) ) ;
#5855=EDGE_CURVE ( 'NONE', #6897, #15883, #10864, .T. ) ;
#5856=ADVANCED_FACE ( 'NONE', ( #17838 ), #11982, .F. ) ;
#5858=CARTESIAN_POINT ( 'NONE',  ( 3.512766787570836158, 7.127386085302768848, 13.25664064834467837 ) ) ;
#5859=CARTESIAN_POINT ( 'NONE',  ( 2.123976203522053741, 10.37815841598491851, 11.67822624909929452 ) ) ;
#5860=DIRECTION ( 'NONE',  ( 0.7635533937278216055, 0.5095610256143827677, 0.3966532189476653092 ) ) ;
#5864=DIRECTION ( 'NONE',  ( 0.7561779333270775005, -0.6106991889125055195, -0.2350349629540206264 ) ) ;
#5866=CARTESIAN_POINT ( 'NONE',  ( 1.846613052777650976, 0.3401093050881815461, 12.43780859207239864 ) ) ;
#5882=CARTESIAN_POINT ( 'NONE',  ( 0.3058872367615226295, -7.578326039752520060, -11.46514199369366516 ) ) ;
#5884=CARTESIAN_POINT ( 'NONE',  ( 0.3132635586635976188, 0.5277914263193109745, 13.72732610560088773 ) ) ;
#5889=VECTOR ( 'NONE', #9131, 1000.000000000000114 ) ;
#5893=CARTESIAN_POINT ( 'NONE',  ( 1.847034903785822690, 7.126331315909270714, 10.19974412751566994 ) ) ;
#5895=ORIENTED_EDGE ( 'NONE', *, *, #12049, .T. ) ;
#5897=EDGE_CURVE ( 'NONE', #12510, #6753, #6288, .T. ) ;
#5899=CARTESIAN_POINT ( 'NONE',  ( 16.57778382496167424, 0.01466529584256784369, 0.002851818597094051173 ) ) ;
#5901=ORIENTED_EDGE ( 'NONE', *, *, #10540, .T. ) ;
#5903=CIRCLE ( 'NONE', #16610, 16.06066017081991149 ) ;
#5905=EDGE_CURVE ( 'NONE', #5954, #4916, #12861, .T. ) ;
#5907=ORIENTED_EDGE ( 'NONE', *, *, #3459, .T. ) ;
#5910=CARTESIAN_POINT ( 'NONE',  ( 0.3137051932979792457, -3.805684345189695783, -13.20008686438109891 ) ) ;
#5917=CIRCLE ( 'NONE', #12343, 16.06066017081991149 ) ;
#5922=VERTEX_POINT ( 'NONE', #13805 ) ;
#5923=CARTESIAN_POINT ( 'NONE',  ( 16.56679352167444819, 0.001518074900131727951, 0.009170718284672568082 ) ) ;
#5925=DIRECTION ( 'NONE',  ( -0.7635533937278216055, -0.5095610256143884298, 0.3966532189476580372 ) ) ;
#5930=ORIENTED_EDGE ( 'NONE', *, *, #12232, .F. ) ;
#5931=CARTESIAN_POINT ( 'NONE',  ( 0.3170788640506440603, -4.392045232375903829, 13.02120094575826670 ) ) ;
#5933=CARTESIAN_POINT ( 'NONE',  ( 0.4754618798421167414, -7.564402563418384240, -11.68486377711974811 ) ) ;
#5938=CARTESIAN_POINT ( 'NONE',  ( 2.002547531651519996, -10.57595306287287329, -6.845637710436306200 ) ) ;
#5939=CARTESIAN_POINT ( 'NONE',  ( 3.950837973638668288, 0.000000000000000000, 0.000000000000000000 ) ) ;
#5940=CARTESIAN_POINT ( 'NONE',  ( 0.3058872367615230181, -4.821066432589238282, -12.87003593440633331 ) ) ;
#5941=CARTESIAN_POINT ( 'NONE',  ( 0.8740779401507028368, 12.04241618260048696, 7.708543377337672808 ) ) ;
#5942=CARTESIAN_POINT ( 'NONE',  ( 2.123976203522053297, 15.26039569100264082, -3.347755036805743600 ) ) ;
#5954=VERTEX_POINT ( 'NONE', #2422 ) ;
#5956=ORIENTED_EDGE ( 'NONE', *, *, #16056, .F. ) ;
#5959=CARTESIAN_POINT ( 'NONE',  ( 0.3150686449036029235, -13.73846184595214304, 0.1533607327085267646 ) ) ;
#5978=ORIENTED_EDGE ( 'NONE', *, *, #13531, .T. ) ;
#5984=B_SPLINE_CURVE_WITH_KNOTS ( 'NONE', 3,
 ( #9205, #6630, #8068, #7979, #793, #12449 ),
 .UNSPECIFIED., .F., .F.,
 ( 4, 2, 4 ),
 ( 3.436766974507050665E-17, 0.0001825746017570568534, 0.0003651492035140793376 ),
 .UNSPECIFIED. ) ;
#5986=CARTESIAN_POINT ( 'NONE',  ( 1.846138399168762989, 10.30487220521570357, 6.971848976711047641 ) ) ;
#5987=CARTESIAN_POINT ( 'NONE',  ( 16.56753206892534891, 0.009369540855502532517, -0.001549402974394196693 ) ) ;
#5988=ORIENTED_EDGE ( 'NONE', *, *, #6353, .F. ) ;
#5994=CARTESIAN_POINT ( 'NONE',  ( 1.847247051441592625, 11.88474976472817701, -3.685275815977066216 ) ) ;
#5996=CARTESIAN_POINT ( 'NONE',  ( 0.3142014840576500267, -10.88517824918537080, -8.382000553815572630 ) ) ;
#6000=B_SPLINE_CURVE_WITH_KNOTS ( 'NONE', 3,
 ( #15991, #12937, #12493, #17239, #12841, #18766, #18666 ),
 .UNSPECIFIED., .F., .F.,
 ( 4, 3, 4 ),
 ( 3.198396408832238080E-18, 0.0002299780670421062274, 0.0004597478348664300451 ),
 .UNSPECIFIED. ) ;
#6001=( BOUNDED_SURFACE ( )  B_SPLINE_SURFACE ( 3, 1, ( 
 ( #14702, #1525 ),
 ( #14415, #10215 ),
 ( #11750, #12888 ),
 ( #18714, #10197 ) ),
 .UNSPECIFIED., .F., .F., .T. ) 
 B_SPLINE_SURFACE_WITH_KNOTS ( ( 4, 4 ),
 ( 2, 2 ),
 ( 0.000000000000000000, 1.000000000000000000 ),
 ( 0.000000000000000000, 1.000000000000000000 ),
 .UNSPECIFIED. ) 
 GEOMETRIC_REPRESENTATION_ITEM ( )  RATIONAL_B_SPLINE_SURFACE ( (
 ( 1.000000000000000000, 1.000000000000000000),
 ( 0.7792777138730160313, 0.9689936506012927220),
 ( 0.7792777138730160313, 0.9689936506012927220),
 ( 1.000000000000000000, 1.000000000000000000) ) ) 
 REPRESENTATION_ITEM ( '' )  SURFACE ( )  );
#6002=VERTEX_POINT ( 'NONE', #7913 ) ;
#6008=CARTESIAN_POINT ( 'NONE',  ( 16.56872352241294521, -0.007240717549633937135, 0.007512283835805527027 ) ) ;
#6009=EDGE_CURVE ( 'NONE', #16688, #2315, #5126, .T. ) ;
#6012=EDGE_LOOP ( 'NONE', ( #5364, #12185, #4556, #13125 ) ) ;
#6016=CARTESIAN_POINT ( 'NONE',  ( 0.000000000000000000, 0.000000000000000000, 5.000000000000000000 ) ) ;
#6019=EDGE_CURVE ( 'NONE', #4916, #11838, #8762, .T. ) ;
#6031=CARTESIAN_POINT ( 'NONE',  ( 1.254255976357533831, -13.61551404021209777, -5.487601330835152780 ) ) ;
#6036=ADVANCED_FACE ( 'NONE', ( #18855 ), #17848, .F. ) ;
#6037=CARTESIAN_POINT ( 'NONE',  ( 16.56822296793089322, -0.007741272030791128758, -0.006547366384935482571 ) ) ;
#6038=AXIS2_PLACEMENT_3D ( 'NONE', #14785, #13451, #7543 ) ;
#6039=VERTEX_POINT ( 'NONE', #11510 ) ;
#6043=CARTESIAN_POINT ( 'NONE',  ( 1.847461586945732703, 3.813310247068605552, -11.84459954310606378 ) ) ;
#6045=CARTESIAN_POINT ( 'NONE',  ( 0.3137051932979792457, -7.698472063774386420, -11.37800749014139612 ) ) ;
#6050=CARTESIAN_POINT ( 'NONE',  ( 0.3095370825347224519, -7.700448427571790155, -11.38092634279636961 ) ) ;
#6052=CARTESIAN_POINT ( 'NONE',  ( 16.57210152137263393, -0.0006600038696347039187, 0.01453130299868522074 ) ) ;
#6053=CARTESIAN_POINT ( 'NONE',  ( 2.747332970342022840, 2.409922051470680060, 16.17136872824899285 ) ) ;
#6056=DIRECTION ( 'NONE',  ( 0.000000000000000000, 0.000000000000000000, 1.000000000000000000 ) ) ;
#6057=CARTESIAN_POINT ( 'NONE',  ( 16.56679352167444819, 0.008311568981097328460, -0.004162264567719685220 ) ) ;
#6065=EDGE_CURVE ( 'NONE', #1343, #8373, #17231, .T. ) ;
#6066=CARTESIAN_POINT ( 'NONE',  ( 1.847380140988738484, 10.00162556679661741, -7.402792205948994564 ) ) ;
#6070=EDGE_CURVE ( 'NONE', #15029, #18593, #16972, .T. ) ;
#6072=CARTESIAN_POINT ( 'NONE',  ( 3.950837973638676281, -6.316429227969383220, -13.10350451991847009 ) ) ;
#6077=CARTESIAN_POINT ( 'NONE',  ( 2.636624412715137922, 2.161493821597615828, 15.91454522070216093 ) ) ;
#6084=ORIENTED_EDGE ( 'NONE', *, *, #7744, .T. ) ;
#6085=CARTESIAN_POINT ( 'NONE',  ( 2.002547531651519996, 6.845637710436341727, -10.57595306287284842 ) ) ;
#6086=CARTESIAN_POINT ( 'NONE',  ( 16.56822296793089322, -0.01011126603341003585, -0.0007467251401289729364 ) ) ;
#6089=FACE_OUTER_BOUND ( 'NONE', #18388, .T. ) ;
#6100=CARTESIAN_POINT ( 'NONE',  ( 3.512766787570980931, 13.55823433651926280, 6.535475144496921907 ) ) ;
#6104=CARTESIAN_POINT ( 'NONE',  ( 0.3137051932979792457, 4.679953077377670745, -12.91601973349265720 ) ) ;
#6108=ORIENTED_EDGE ( 'NONE', *, *, #11257, .F. ) ;
#6112=LINE ( 'NONE', #9625, #12057 ) ;
#6115=CARTESIAN_POINT ( 'NONE',  ( 2.697797270744668463, 0.9169917281809109033, -13.26309265156976203 ) ) ;
#6117=CARTESIAN_POINT ( 'NONE',  ( 1.847461586945727374, -3.813310247068524284, 11.84459954310609753 ) ) ;
#6119=CARTESIAN_POINT ( 'NONE',  ( 2.002547531651519996, -7.942910686618240845, 9.778737580845669797 ) ) ;
#6121=EDGE_CURVE ( 'NONE', #2897, #4902, #5112, .T. ) ;
#6123=CARTESIAN_POINT ( 'NONE',  ( 0.3137051932979792457, 13.20008686438105983, 3.805684345189833451 ) ) ;
#6124=EDGE_CURVE ( 'NONE', #1472, #10380, #5781, .T. ) ;
#6125=( BOUNDED_SURFACE ( )  B_SPLINE_SURFACE ( 3, 1, ( 
 ( #3933, #12996 ),
 ( #14254, #8419 ),
 ( #6896, #18450 ),
 ( #18548, #18636 ) ),
 .UNSPECIFIED., .F., .F., .T. ) 
 B_SPLINE_SURFACE_WITH_KNOTS ( ( 4, 4 ),
 ( 2, 2 ),
 ( 0.000000000000000000, 1.000000000000000000 ),
 ( 0.000000000000000000, 1.000000000000000000 ),
 .UNSPECIFIED. ) 
 GEOMETRIC_REPRESENTATION_ITEM ( )  RATIONAL_B_SPLINE_SURFACE ( (
 ( 1.000000000000000000, 1.000000000000000000),
 ( 0.7792777138730160313, 0.9689936506012927220),
 ( 0.7792777138730160313, 0.9689936506012927220),
 ( 1.000000000000000000, 1.000000000000000000) ) ) 
 REPRESENTATION_ITEM ( '' )  SURFACE ( )  );
#6127=CARTESIAN_POINT ( 'NONE',  ( 0.3170788640506441158, 11.02668139258453905, -8.200855617524412722 ) ) ;
#6130=CARTESIAN_POINT ( 'NONE',  ( 0.3150686449036074199, 0.1533607327085746430, 13.73846184595213771 ) ) ;
#6135=EDGE_LOOP ( 'NONE', ( #1413, #4514, #15613, #12384 ) ) ;
#6138=VERTEX_POINT ( 'NONE', #14840 ) ;
#6139=CARTESIAN_POINT ( 'NONE',  ( 1.847034903785822246, 4.063013886994871982, -11.76058231742741533 ) ) ;
#6141=LINE ( 'NONE', #11969, #14351 ) ;
#6142=CARTESIAN_POINT ( 'NONE',  ( 1.254255976357772751, -11.25336128106935263, -9.426444230097215993 ) ) ;
#6145=VERTEX_POINT ( 'NONE', #16383 ) ;
#6146=CARTESIAN_POINT ( 'NONE',  ( 1.846524061778018311, -10.27028962889602148, 7.023652644192237560 ) ) ;
#6149=CARTESIAN_POINT ( 'NONE',  ( 16.56679352167444819, 0.006618561353599204840, -0.006526964904752983153 ) ) ;
#6153=CARTESIAN_POINT ( 'NONE',  ( 0.3132635586635977298, -13.72732610560088418, 0.5277914263192632349 ) ) ;
#6154=VERTEX_POINT ( 'NONE', #9115 ) ;
#6157=CARTESIAN_POINT ( 'NONE',  ( 0.3150692679895978343, 11.20465057551037091, -7.951395415074959061 ) ) ;
#6158=EDGE_CURVE ( 'NONE', #3822, #10095, #8311, .T. ) ;
#6159=ORIENTED_EDGE ( 'NONE', *, *, #14290, .T. ) ;
#6167=CARTESIAN_POINT ( 'NONE',  ( 1.342453679581834924, -0.9602753779831757486, 14.76648944001038899 ) ) ;
#6169=CARTESIAN_POINT ( 'NONE',  ( 2.636624412716062960, 6.973567714909310489, -14.46769361191320868 ) ) ;
#6173=B_SPLINE_CURVE_WITH_KNOTS ( 'NONE', 3,
 ( #2430, #16787, #9605, #14093, #1000, #11244, #17059 ),
 .UNSPECIFIED., .F., .F.,
 ( 4, 3, 4 ),
 ( 1.951563910473907981E-18, 0.0002299804304191482840, 0.0004168119862248656667 ),
 .UNSPECIFIED. ) ;
#6174=CARTESIAN_POINT ( 'NONE',  ( 1.847461586945727596, -11.84459954310608332, -3.813310247068566028 ) ) ;
#6175=AXIS2_PLACEMENT_3D ( 'NONE', #12791, #18617, #14129 ) ;
#6176=CARTESIAN_POINT ( 'NONE',  ( 0.8740779401508861346, -14.27348745891575987, 0.8420120399581260129 ) ) ;
#6180=ORIENTED_EDGE ( 'NONE', *, *, #4580, .T. ) ;
#6181=CARTESIAN_POINT ( 'NONE',  ( 0.3151926232592474619, -8.137833541809298410, -11.07013665200804198 ) ) ;
#6182=CARTESIAN_POINT ( 'NONE',  ( 0.3095370825347233956, 10.84046130709070610, -8.444334731363889901 ) ) ;
#6188=CARTESIAN_POINT ( 'NONE',  ( 3.950837973638675393, -2.591948120961912849, 14.31366178983252446 ) ) ;
#6189=CARTESIAN_POINT ( 'NONE',  ( 1.847412631396507798, 11.84727953344288132, -3.804043368582538776 ) ) ;
#6193=CARTESIAN_POINT ( 'NONE',  ( 0.3145729642390374670, 3.952965287571295949, -13.15786090015079957 ) ) ;
#6195=EDGE_LOOP ( 'NONE', ( #4307, #7067, #18702, #17886 ) ) ;
#6196=EDGE_CURVE ( 'NONE', #11775, #15252, #7570, .T. ) ;
#6202=CARTESIAN_POINT ( 'NONE',  ( 16.56753206892534891, 0.001549402974393146101, -0.009369540855502138735 ) ) ;
#6205=CARTESIAN_POINT ( 'NONE',  ( 0.4385251269669950269, -0.7363879510386354132, 13.84299131624729462 ) ) ;
#6207=CARTESIAN_POINT ( 'NONE',  ( 16.56822296793089322, 0.008619100080559776930, 0.005339139727952691740 ) ) ;
#6208=CARTESIAN_POINT ( 'NONE',  ( 16.58200780006414732, 0.004047297414157893791, 0.01041078477703983804 ) ) ;
#6210=B_SPLINE_CURVE_WITH_KNOTS ( 'NONE', 3,
 ( #17514, #4620, #14455, #225, #15891, #4331 ),
 .UNSPECIFIED., .F., .F.,
 ( 4, 2, 4 ),
 ( 0.000000000000000000, 0.001500839035891551789, 0.003001678071783103578 ),
 .UNSPECIFIED. ) ;
#6215=CARTESIAN_POINT ( 'NONE',  ( 0.3308579732647041749, 8.558831104907067555, -10.76782854710817716 ) ) ;
#6216=VERTEX_POINT ( 'NONE', #228 ) ;
#6217=EDGE_LOOP ( 'NONE', ( #8732, #16641, #16798, #3701 ) ) ;
#6219=CARTESIAN_POINT ( 'NONE',  ( 1.847426409206450959, 1.966388007708274189E-11, -12.44303504652081038 ) ) ;
#6222=VECTOR ( 'NONE', #12669, 1000.000000000000114 ) ;
#6226=ORIENTED_EDGE ( 'NONE', *, *, #10681, .T. ) ;
#6229=ADVANCED_BREP_SHAPE_REPRESENTATION ( '', ( #16223, #2030 ), #8454 ) ;
#6231=CARTESIAN_POINT ( 'NONE',  ( 1.847247051441591070, 4.004229874809190903, -11.78111530882019053 ) ) ;
#6233=CARTESIAN_POINT ( 'NONE',  ( 0.4385251269669945273, -7.540955776459655091, -11.63205320541531052 ) ) ;
#6240=CARTESIAN_POINT ( 'NONE',  ( 2.697797270744669795, 12.89731672021094511, -3.226410068829295597 ) ) ;
#6241=DIRECTION ( 'NONE',  ( -1.000000000000000000, -0.000000000000000000, -0.000000000000000000 ) ) ;
#6242=CARTESIAN_POINT ( 'NONE',  ( 2.636624412714236865, 0.000000000000000000, 0.000000000000000000 ) ) ;
#6244=CARTESIAN_POINT ( 'NONE',  ( 1.846138399168762101, -10.30487220521565028, -6.971848976711123136 ) ) ;
#6246=CARTESIAN_POINT ( 'NONE',  ( 1.846138399168762989, 9.815003036200414144, 7.646096044339929954 ) ) ;
#6248=ORIENTED_EDGE ( 'NONE', *, *, #4112, .F. ) ;
#6249=VERTEX_POINT ( 'NONE', #6246 ) ;
#6252=ORIENTED_EDGE ( 'NONE', *, *, #8416, .F. ) ;
#6260=CARTESIAN_POINT ( 'NONE',  ( 16.56679352167444819, -0.001518074900131792136, -0.009170718284672557674 ) ) ;
#6267=AXIS2_PLACEMENT_3D ( 'NONE', #1044, #18542, #12805 ) ;
#6271=LINE ( 'NONE', #10764, #16074 ) ;
#6274=CARTESIAN_POINT ( 'NONE',  ( 0.4862570985993235340, -13.89016912371018186, 0.7479633556561964269 ) ) ;
#6276=ORIENTED_EDGE ( 'NONE', *, *, #14821, .F. ) ;
#6286=CARTESIAN_POINT ( 'NONE',  ( 2.705023505549867036, 0.8488853074252974418, 13.27418276223636440 ) ) ;
#6288=B_SPLINE_CURVE_WITH_KNOTS ( 'NONE', 3,
 ( #5019, #16865, #6654, #5295, #5391, #9509 ),
 .UNSPECIFIED., .F., .F.,
 ( 4, 2, 4 ),
 ( 0.000000000000000000, 0.001500839035891550271, 0.003001678071783100542 ),
 .UNSPECIFIED. ) ;
#6290=CARTESIAN_POINT ( 'NONE',  ( 16.56872352241294521, -0.007240717549633937135, 0.007512283835805527027 ) ) ;
#6291=CARTESIAN_POINT ( 'NONE',  ( 0.3095370825347234511, -8.444334731364085300, 10.84046130709055333 ) ) ;
#6293=DIRECTION ( 'NONE',  ( 0.7071067818211348444, 0.000000000000000000, -0.7071067805519601901 ) ) ;
#6295=CARTESIAN_POINT ( 'NONE',  ( 3.950837973638675393, 10.05648675950126325, 10.51028938476221342 ) ) ;
#6296=CARTESIAN_POINT ( 'NONE',  ( 0.3142014840576516921, 4.608051180497103161, -12.94260032291123785 ) ) ;
#6297=EDGE_LOOP ( 'NONE', ( #2163, #11717, #8210, #11462 ) ) ;
#6300=ORIENTED_EDGE ( 'NONE', *, *, #16341, .F. ) ;
#6302=CARTESIAN_POINT ( 'NONE',  ( 1.847247051441588184, -7.177495230324629105, -10.16425585218608951 ) ) ;
#6306=B_SPLINE_CURVE_WITH_KNOTS ( 'NONE', 3,
 ( #13157, #17851, #10297, #14496, #1405, #169 ),
 .UNSPECIFIED., .F., .F.,
 ( 4, 2, 4 ),
 ( 3.337089043155729788E-17, 0.0001825746017570573684, 0.0003651492035140813976 ),
 .UNSPECIFIED. ) ;
#6307=CARTESIAN_POINT ( 'NONE',  ( 2.320521194582547242, 1.795798718313595055, 15.64520804578271118 ) ) ;
#6308=ORIENTED_EDGE ( 'NONE', *, *, #12102, .T. ) ;
#6312=FACE_OUTER_BOUND ( 'NONE', #3892, .T. ) ;
#6315=EDGE_CURVE ( 'NONE', #4723, #78, #1992, .T. ) ;
#6321=CARTESIAN_POINT ( 'NONE',  ( 3.950837973638668288, 0.000000000000000000, 0.000000000000000000 ) ) ;
#6328=AXIS2_PLACEMENT_3D ( 'NONE', #12823, #15882, #18649 ) ;
#6333=ORIENTED_EDGE ( 'NONE', *, *, #2128, .F. ) ;
#6335=CARTESIAN_POINT ( 'NONE',  ( 16.58200780006414732, -0.006043560077721639792, -0.009393638146079824613 ) ) ;
#6342=ADVANCED_FACE ( 'NONE', ( #9573 ), #11972, .T. ) ;
#6343=EDGE_LOOP ( 'NONE', ( #1786, #9715, #1010, #8655, #5901, #8474, #15691, #13381, #7239, #18533, #2145, #3273, #10553, #11161, #4625, #10740, #296, #17379, #1754, #13240, #7044, #6903, #15472, #11839, #11143, #3021, #11539, #676, #3492, #17503, #3435, #6180, #17010, #17910, #14961, #13072, #17257, #9511, #12697, #17489, #1349, #15225, #1947, #5457, #7890, #10580, #2251, #4129, #3874, #11421, #7586, #13474, #8224, #2191, #7916, #4267, #6787, #13685, #9781, #8752, #4675, #11092, #16039, #18482 ) ) ;
#6345=CARTESIAN_POINT ( 'NONE',  ( 1.847412631396506022, -10.09191835241968427, 7.278870946904215877 ) ) ;
#6347=CARTESIAN_POINT ( 'NONE',  ( 1.846138399168762101, 6.971848976711011225, 10.30487220521572667 ) ) ;
#6348=VERTEX_POINT ( 'NONE', #6808 ) ;
#6350=ORIENTED_EDGE ( 'NONE', *, *, #6552, .F. ) ;
#6353=EDGE_CURVE ( 'NONE', #678, #16918, #4002, .T. ) ;
#6356=CARTESIAN_POINT ( 'NONE',  ( 1.847034903785822690, -0.2299360331935046409, 12.44051878787773013 ) ) ;
#6366=DIRECTION ( 'NONE',  ( 0.000000000000000000, 0.000000000000000000, -1.000000000000000000 ) ) ;
#6370=DIRECTION ( 'NONE',  ( 0.7635533937278214944, 0.5347026451755962917, -0.3620487483322465949 ) ) ;
#6374=CARTESIAN_POINT ( 'NONE',  ( 0.3170788640506441158, 13.02120094575834131, -4.392045232375677344 ) ) ;
#6380=ORIENTED_EDGE ( 'NONE', *, *, #11319, .T. ) ;
#6381=CARTESIAN_POINT ( 'NONE',  ( 0.4754618798421162973, 10.80499583390525586, -8.775436892860994931 ) ) ;
#6382=CARTESIAN_POINT ( 'NONE',  ( 0.3058872367615226295, -12.87003593440624982, -4.821066432589462103 ) ) ;
#6390=CARTESIAN_POINT ( 'NONE',  ( 2.002547531651519996, 7.942910686618173344, 9.778737580845726640 ) ) ;
#6394=VERTEX_POINT ( 'NONE', #13000 ) ;
#6398=EDGE_CURVE ( 'NONE', #18880, #11465, #2867, .T. ) ;
#6406=CARTESIAN_POINT ( 'NONE',  ( 1.847247051441598176, -4.004229874809106526, 11.78111530882021185 ) ) ;
#6414=CARTESIAN_POINT ( 'NONE',  ( 2.002547531651519996, -7.942910686618100513, -9.778737580845787036 ) ) ;
#6421=B_SPLINE_CURVE_WITH_KNOTS ( 'NONE', 3,
 ( #12558, #13722, #9423, #4842, #15248, #725 ),
 .UNSPECIFIED., .F., .F.,
 ( 4, 2, 4 ),
 ( 1.951563910473907981E-18, 0.0002017457492448081235, 0.0004034914984896142954 ),
 .UNSPECIFIED. ) ;
#6422=EDGE_CURVE ( 'NONE', #15496, #5049, #7232, .T. ) ;
#6431=ORIENTED_EDGE ( 'NONE', *, *, #9764, .T. ) ;
#6436=CARTESIAN_POINT ( 'NONE',  ( 0.4754618798421162973, 10.80499583390512974, 8.775436892861156579 ) ) ;
#6438=ORIENTED_EDGE ( 'NONE', *, *, #14874, .F. ) ;
#6440=( BOUNDED_SURFACE ( )  B_SPLINE_SURFACE ( 3, 1, ( 
 ( #5605, #18704 ),
 ( #11024, #3744 ),
 ( #13972, #12531 ),
 ( #3464, #9298 ) ),
 .UNSPECIFIED., .F., .F., .T. ) 
 B_SPLINE_SURFACE_WITH_KNOTS ( ( 4, 4 ),
 ( 2, 2 ),
 ( 0.000000000000000000, 1.000000000000000000 ),
 ( 0.000000000000000000, 1.000000000000000000 ),
 .UNSPECIFIED. ) 
 GEOMETRIC_REPRESENTATION_ITEM ( )  RATIONAL_B_SPLINE_SURFACE ( (
 ( 1.000000000000000000, 1.000000000000000000),
 ( 0.9933953342250436691, 0.8357391271907733676),
 ( 0.9933953342250436691, 0.8357391271907733676),
 ( 1.000000000000000000, 1.000000000000000000) ) ) 
 REPRESENTATION_ITEM ( '' )  SURFACE ( )  );
#6444=EDGE_CURVE ( 'NONE', #799, #16688, #16582, .T. ) ;
#6445=ORIENTED_EDGE ( 'NONE', *, *, #9378, .T. ) ;
#6447=ORIENTED_EDGE ( 'NONE', *, *, #9553, .T. ) ;
#6449=ORIENTED_EDGE ( 'NONE', *, *, #9481, .T. ) ;
#6451=CARTESIAN_POINT ( 'NONE',  ( 16.56753206892534891, 0.004253784598196176658, -0.008490833999798941267 ) ) ;
#6459=CARTESIAN_POINT ( 'NONE',  ( 2.353870697619111052, 12.05847592522643907, 4.720869121224175124 ) ) ;
#6468=ORIENTED_EDGE ( 'NONE', *, *, #16293, .F. ) ;
#6470=EDGE_LOOP ( 'NONE', ( #4005, #8505, #8800, #9232 ) ) ;
#6471=ORIENTED_EDGE ( 'NONE', *, *, #18338, .F. ) ;
#6478=CARTESIAN_POINT ( 'NONE',  ( 3.950837973638668288, 0.000000000000000000, 0.000000000000000000 ) ) ;
#6481=DIRECTION ( 'NONE',  ( -0.7561779333270775005, 0.5081796452863305280, -0.4122479608995649469 ) ) ;
#6482=VERTEX_POINT ( 'NONE', #18453 ) ;
#6484=ORIENTED_EDGE ( 'NONE', *, *, #9822, .T. ) ;
#6487=ORIENTED_EDGE ( 'NONE', *, *, #14431, .F. ) ;
#6493=CARTESIAN_POINT ( 'NONE',  ( 8.522092701127531811, 6.722964936702122252, -1.786985377231962380 ) ) ;
#6496=DIRECTION ( 'NONE',  ( 0.000000000000000000, 0.000000000000000000, -1.000000000000000000 ) ) ;
#6498=CARTESIAN_POINT ( 'NONE',  ( 1.977228804421385933, 15.33060379559031539, -1.488378900181928532 ) ) ;
#6499=CARTESIAN_POINT ( 'NONE',  ( 1.861706995891675653, 0.5394761475745838419, 12.44571539481144207 ) ) ;
#6503=CARTESIAN_POINT ( 'NONE',  ( 3.950837973638676281, -1.958075594453890789, 14.41405733518059940 ) ) ;
#6509=CARTESIAN_POINT ( 'NONE',  ( 0.000000000000000000, 0.000000000000000000, 0.000000000000000000 ) ) ;
#6512=ADVANCED_FACE ( 'NONE', ( #1931 ), #11756, .F. ) ;
#6521=CARTESIAN_POINT ( 'NONE',  ( 3.512766787570769100, 13.55823433651956833, -6.535475144496838418 ) ) ;
#6524=CONICAL_SURFACE ( 'NONE', #11108, 14.54644660717763927, 0.8559913436420816257 ) ;
#6535=CARTESIAN_POINT ( 'NONE',  ( 0.3137051932979757485, 8.442169467526850823, 10.83767969834806166 ) ) ;
#6536=CARTESIAN_POINT ( 'NONE',  ( 3.950837973638675393, -13.10350451991845055, 6.316429227969417859 ) ) ;
#6538=ORIENTED_EDGE ( 'NONE', *, *, #17902, .T. ) ;
#6544=VECTOR ( 'NONE', #3007, 1000.000000000000114 ) ;
#6546=CARTESIAN_POINT ( 'NONE',  ( 0.3137051932979775248, 10.83767969834815581, -8.442169467526731808 ) ) ;
#6547=CARTESIAN_POINT ( 'NONE',  ( 2.123976203522053741, 14.31368049382978569, -6.261444813538409981 ) ) ;
#6551=CARTESIAN_POINT ( 'NONE',  ( 1.959283090834841090, -10.53516775895155000, -6.829027319138364582 ) ) ;
#6552=EDGE_CURVE ( 'NONE', #15452, #4150, #7580, .T. ) ;
#6553=CARTESIAN_POINT ( 'NONE',  ( 0.8740764193769881008, 5.211550415969331773, -13.31469591265785901 ) ) ;
#6556=FACE_OUTER_BOUND ( 'NONE', #1688, .T. ) ;
#6561=ORIENTED_EDGE ( 'NONE', *, *, #12750, .T. ) ;
#6563=ORIENTED_EDGE ( 'NONE', *, *, #6065, .T. ) ;
#6566=CARTESIAN_POINT ( 'NONE',  ( 1.254255976357841584, 1.011593778944668731, -14.64488542023482331 ) ) ;
#6574=EDGE_CURVE ( 'NONE', #3683, #15961, #395, .T. ) ;
#6577=B_SPLINE_CURVE_WITH_KNOTS ( 'NONE', 3,
 ( #9656, #2560, #13959, #870, #5258, #6711 ),
 .UNSPECIFIED., .F., .F.,
 ( 4, 2, 4 ),
 ( 2.622335209753013447E-18, 0.0002017457492448088824, 0.0004034914984896151085 ),
 .UNSPECIFIED. ) ;
#6580=ORIENTED_EDGE ( 'NONE', *, *, #16070, .F. ) ;
#6587=CARTESIAN_POINT ( 'NONE',  ( 2.636624412716045196, 11.10302021257998994, -11.60464335004042447 ) ) ;
#6589=ORIENTED_EDGE ( 'NONE', *, *, #14493, .F. ) ;
#6591=CARTESIAN_POINT ( 'NONE',  ( 1.562796894703937678, 4.769696007084728073, -1.500000000000000000 ) ) ;
#6594=CARTESIAN_POINT ( 'NONE',  ( 0.4754618798421162973, 3.583352865732857495, -13.45049478164055756 ) ) ;
#6599=CARTESIAN_POINT ( 'NONE',  ( 1.977436885026506497, -3.321781585408274839, -15.04044112860335147 ) ) ;
#6625=CARTESIAN_POINT ( 'NONE',  ( 0.3720661004400040439, -0.7231997263363842965, -13.79610186261031046 ) ) ;
#6626=ORIENTED_EDGE ( 'NONE', *, *, #14384, .F. ) ;
#6630=CARTESIAN_POINT ( 'NONE',  ( 1.959283090834841090, 11.71721539537261414, -4.509128209890848282 ) ) ;
#6632=( BOUNDED_SURFACE ( )  B_SPLINE_SURFACE ( 3, 1, ( 
 ( #2790, #7027 ),
 ( #11422, #4342 ),
 ( #7115, #18236 ),
 ( #9533, #7220 ) ),
 .UNSPECIFIED., .F., .F., .T. ) 
 B_SPLINE_SURFACE_WITH_KNOTS ( ( 4, 4 ),
 ( 2, 2 ),
 ( 0.000000000000000000, 1.000000000000000000 ),
 ( 0.000000000000000000, 1.000000000000000000 ),
 .UNSPECIFIED. ) 
 GEOMETRIC_REPRESENTATION_ITEM ( )  RATIONAL_B_SPLINE_SURFACE ( (
 ( 1.000000000000000000, 1.000000000000000000),
 ( 0.9933953342250436691, 0.8357391271907733676),
 ( 0.9933953342250436691, 0.8357391271907733676),
 ( 1.000000000000000000, 1.000000000000000000) ) ) 
 REPRESENTATION_ITEM ( '' )  SURFACE ( )  );
#6633=ORIENTED_EDGE ( 'NONE', *, *, #11806, .F. ) ;
#6634=ORIENTED_EDGE ( 'NONE', *, *, #8643, .F. ) ;
#6635=CARTESIAN_POINT ( 'NONE',  ( 0.3137051932979792457, -0.4596302728640728752, 13.73004976592201842 ) ) ;
#6637=CARTESIAN_POINT ( 'NONE',  ( 2.636624412714237309, 14.14563173255211126, 7.605649742762011556 ) ) ;
#6640=CARTESIAN_POINT ( 'NONE',  ( 0.3150686449036049219, 4.391272911157320991, 13.01866258978838609 ) ) ;
#6645=CARTESIAN_POINT ( 'NONE',  ( 16.57778382496167424, -0.002851818597093308278, -0.01466529584256674387 ) ) ;
#6650=CARTESIAN_POINT ( 'NONE',  ( 16.57605080000000086, 0.000000000000000000, 5.000000000000000000 ) ) ;
#6651=CARTESIAN_POINT ( 'NONE',  ( 2.636624412714292376, 11.60464335004048309, 11.10302021257707850 ) ) ;
#6652=CARTESIAN_POINT ( 'NONE',  ( 16.56753206892534891, 0.001421777558676785977, 0.009389754735541558373 ) ) ;
#6654=CARTESIAN_POINT ( 'NONE',  ( 2.697797270744666243, -11.26906156738832188, 7.053988368581824986 ) ) ;
#6657=ADVANCED_FACE ( 'NONE', ( #14046 ), #1035, .F. ) ;
#6662=EDGE_CURVE ( 'NONE', #14073, #16368, #12275, .T. ) ;
#6670=CARTESIAN_POINT ( 'NONE',  ( 1.845756295923373758, 7.694561132136944259, 9.776763338604617104 ) ) ;
#6672=CONICAL_SURFACE ( 'NONE', #17648, 14.54644660717763927, 0.8559913436420816257 ) ;
#6677=CARTESIAN_POINT ( 'NONE',  ( 2.636624412715093513, -14.14563173255330142, 7.605649742761597665 ) ) ;
#6678=ADVANCED_FACE ( 'NONE', ( #6702 ), #14536, .F. ) ;
#6679=ADVANCED_FACE ( 'NONE', ( #12601 ), #14424, .F. ) ;
#6682=DIRECTION ( 'NONE',  ( -1.000000000000000000, -0.000000000000000000, -0.000000000000000000 ) ) ;
#6683=CARTESIAN_POINT ( 'NONE',  ( 16.56753206892534891, 0.008432171035096382855, 0.004368917149004273269 ) ) ;
#6685=ORIENTED_EDGE ( 'NONE', *, *, #2443, .T. ) ;
#6686=CARTESIAN_POINT ( 'NONE',  ( 0.4754618798421167414, -10.80499583390506402, -8.775436892861231186 ) ) ;
#6687=CARTESIAN_POINT ( 'NONE',  ( 1.959283090834855745, 0.6676170829052219258, 12.53713130127477982 ) ) ;
#6689=CARTESIAN_POINT ( 'NONE',  ( 1.959212340397943120, -7.909199412631233272, 9.750290364083607386 ) ) ;
#6697=ORIENTED_EDGE ( 'NONE', *, *, #18691, .T. ) ;
#6702=FACE_OUTER_BOUND ( 'NONE', #5537, .T. ) ;
#6704=EDGE_CURVE ( 'NONE', #18610, #421, #13492, .T. ) ;
#6711=CARTESIAN_POINT ( 'NONE',  ( 0.4862570985993235340, 13.89016912371017476, -0.7479633556562934604 ) ) ;
#6713=CARTESIAN_POINT ( 'NONE',  ( 3.950837973638676281, 14.31366178983253512, 2.591948120961855118 ) ) ;
#6715=DIRECTION ( 'NONE',  ( 0.000000000000000000, -1.000000000000000000, -0.000000000000000000 ) ) ;
#6718=CARTESIAN_POINT ( 'NONE',  ( 16.56753206892534891, -0.001421777558676017277, 0.009389754735542238384 ) ) ;
#6722=FACE_OUTER_BOUND ( 'NONE', #7108, .T. ) ;
#6723=CARTESIAN_POINT ( 'NONE',  ( 0.3307726912345205772, 8.558645027434268471, 10.76786801061209964 ) ) ;
#6727=CARTESIAN_POINT ( 'NONE',  ( 0.3137051932979792457, 8.442169467527008919, -10.83767969834794087 ) ) ;
#6730=CARTESIAN_POINT ( 'NONE',  ( 0.3137051932979809665, -4.679953077377580151, 12.91601973349268917 ) ) ;
#6734=CARTESIAN_POINT ( 'NONE',  ( 1.847461586945727152, -10.08650590720931284, -7.286856109515166047 ) ) ;
#6736=CARTESIAN_POINT ( 'NONE',  ( 3.950837973638668288, 14.41405733518061538, -1.958075594453841273 ) ) ;
#6738=DIRECTION ( 'NONE',  ( -0.7635533937278216055, -0.5347026451755912957, -0.3620487483322542555 ) ) ;
#6742=DIRECTION ( 'NONE',  ( 0.7635533937278214944, -0.6204116510013502062, 0.1790966170213858510 ) ) ;
#6743=( BOUNDED_SURFACE ( )  B_SPLINE_SURFACE ( 3, 1, ( 
 ( #16281, #6053 ),
 ( #4814, #8908 ),
 ( #11881, #7491 ),
 ( #10546, #123 ) ),
 .UNSPECIFIED., .F., .F., .T. ) 
 B_SPLINE_SURFACE_WITH_KNOTS ( ( 4, 4 ),
 ( 2, 2 ),
 ( 0.000000000000000000, 1.000000000000000000 ),
 ( 0.000000000000000000, 1.000000000000000000 ),
 .UNSPECIFIED. ) 
 GEOMETRIC_REPRESENTATION_ITEM ( )  RATIONAL_B_SPLINE_SURFACE ( (
 ( 1.000000000000000000, 1.000000000000000000),
 ( 0.7792777138730158093, 0.9689936506012928330),
 ( 0.7792777138730158093, 0.9689936506012928330),
 ( 1.000000000000000000, 1.000000000000000000) ) ) 
 REPRESENTATION_ITEM ( '' )  SURFACE ( )  );
#6746=CARTESIAN_POINT ( 'NONE',  ( 0.3137051932979792457, -8.442169467526928983, 10.83767969834800127 ) ) ;
#6749=DIRECTION ( 'NONE',  ( -0.7635533937278214944, 0.5347026451755939602, 0.3620487483322503142 ) ) ;
#6753=VERTEX_POINT ( 'NONE', #11556 ) ;
#6758=ADVANCED_FACE ( 'NONE', ( #4484 ), #4163, .F. ) ;
#6759=CARTESIAN_POINT ( 'NONE',  ( 1.342453679581834924, 11.38190519890867236, -9.456403821038676938 ) ) ;
#6762=CARTESIAN_POINT ( 'NONE',  ( 16.57210152137263393, -0.01214401161737629908, -0.008007331252333388036 ) ) ;
#6763=CARTESIAN_POINT ( 'NONE',  ( 0.3939822652208159193, 8.678192463540325363, -10.75310269629511950 ) ) ;
#6764=CARTESIAN_POINT ( 'NONE',  ( 1.562796894703937678, 0.000000000000000000, -1.500000000000000000 ) ) ;
#6769=ORIENTED_EDGE ( 'NONE', *, *, #14325, .F. ) ;
#6773=CARTESIAN_POINT ( 'NONE',  ( 2.123976203522053741, -14.31368049382974483, 6.261444813538503240 ) ) ;
#6776=ORIENTED_EDGE ( 'NONE', *, *, #10570, .T. ) ;
#6777=CARTESIAN_POINT ( 'NONE',  ( 1.846955891736115740, 10.21904526726846640, 7.098901504650394934 ) ) ;
#6778=CARTESIAN_POINT ( 'NONE',  ( 0.4862570985993235340, 13.44146924561385958, -3.580942890621532371 ) ) ;
#6780=CARTESIAN_POINT ( 'NONE',  ( 2.002547531651519996, -6.845637710436110801, -10.57595306287299763 ) ) ;
#6782=CARTESIAN_POINT ( 'NONE',  ( 1.959212340397943786, -10.53510106265286517, 6.829000156128149257 ) ) ;
#6783=CARTESIAN_POINT ( 'NONE',  ( 1.959212340397946006, -4.509090217468600947, 11.71715421693496673 ) ) ;
#6784=ADVANCED_FACE ( 'NONE', ( #16138 ), #11360, .T. ) ;
#6785=ORIENTED_EDGE ( 'NONE', *, *, #17934, .F. ) ;
#6786=CARTESIAN_POINT ( 'NONE',  ( 16.57210152137263393, -0.009075239946108286035, 0.01136813053532071717 ) ) ;
#6787=ORIENTED_EDGE ( 'NONE', *, *, #12311, .T. ) ;
#6789=CARTESIAN_POINT ( 'NONE',  ( 0.3058872367615230181, -13.24582953854922529, -3.664492643742902178 ) ) ;
#6792=CARTESIAN_POINT ( 'NONE',  ( 1.562796894703937678, 0.000000000000000000, -12.15840553252917289 ) ) ;
#6795=CARTESIAN_POINT ( 'NONE',  ( 2.320520222537543198, -15.43440824796705613, 3.126729907239071959 ) ) ;
#6799=ADVANCED_FACE ( 'NONE', ( #4579 ), #1486, .F. ) ;
#6807=ORIENTED_EDGE ( 'NONE', *, *, #13273, .T. ) ;
#6808=CARTESIAN_POINT ( 'NONE',  ( 2.002547531651519996, 7.942910686618173344, 9.778737580845726640 ) ) ;
#6811=CARTESIAN_POINT ( 'NONE',  ( 3.512766787570699822, -13.55823433651950616, -6.535475144497160827 ) ) ;
#6812=CARTESIAN_POINT ( 'NONE',  ( 0.3137051932979809665, 10.83767969834803324, 8.442169467526891680 ) ) ;
#6814=CARTESIAN_POINT ( 'NONE',  ( 0.3148208552358936485, 4.463611911212218786, 12.99355031785207260 ) ) ;
#6816=CARTESIAN_POINT ( 'NONE',  ( 16.56872352241294521, 0.001442253899401220278, -0.01033355228142500415 ) ) ;
#6823=CARTESIAN_POINT ( 'NONE',  ( 1.959212340397946450, 7.909199412631302550, -9.750290364083546990 ) ) ;
#6825=CARTESIAN_POINT ( 'NONE',  ( 1.846524061778019199, -3.506196582971023545, -11.93805390544204670 ) ) ;
#6827=CARTESIAN_POINT ( 'NONE',  ( 0.3095370825347233956, 13.20347358821914519, 3.806662003783457315 ) ) ;
#6830=EDGE_CURVE ( 'NONE', #12767, #15590, #5159, .T. ) ;
#6840=CARTESIAN_POINT ( 'NONE',  ( 3.353306896162455697, 7.069984850384810393, 12.02594772223098651 ) ) ;
#6845=CARTESIAN_POINT ( 'NONE',  ( 0.3151928478948589074, -0.0001388664988634735829, -13.73922860964089487 ) ) ;
#6848=LINE ( 'NONE', #6764, #7863 ) ;
#6849=ORIENTED_EDGE ( 'NONE', *, *, #2512, .F. ) ;
#6853=VERTEX_POINT ( 'NONE', #13661 ) ;
#6857=CARTESIAN_POINT ( 'NONE',  ( 1.918918678667048683, -11.69059232068581800, 4.466049546133867842 ) ) ;
#6858=LINE ( 'NONE', #3985, #10252 ) ;
#6860=CARTESIAN_POINT ( 'NONE',  ( 1.847380140988739594, 10.13114603776196887, 7.224522571381366554 ) ) ;
#6862=EDGE_CURVE ( 'NONE', #9401, #7021, #15416, .T. ) ;
#6866=CARTESIAN_POINT ( 'NONE',  ( 1.562796894703937678, 6.799999999999999822, 0.000000000000000000 ) ) ;
#6869=CARTESIAN_POINT ( 'NONE',  ( 16.56782317627811096, 0.009228812961908652857, -0.003357783021327854014 ) ) ;
#6875=CARTESIAN_POINT ( 'NONE',  ( 0.3137051932979792457, 4.679953077377485116, 12.91601973349272114 ) ) ;
#6877=CARTESIAN_POINT ( 'NONE',  ( 0.4754618798421162973, -13.45049478164057177, -3.583352865732810866 ) ) ;
#6878=ORIENTED_EDGE ( 'NONE', *, *, #18749, .T. ) ;
#6881=CARTESIAN_POINT ( 'NONE',  ( 1.847168016377981559, -12.44137401948661648, 0.1868244120189130053 ) ) ;
#6882=CARTESIAN_POINT ( 'NONE',  ( 2.636624412716062960, 2.862162146982868194, -15.80357026013419564 ) ) ;
#6886=CARTESIAN_POINT ( 'NONE',  ( 1.254255976357440572, -14.24071337840763363, 3.563435620217590749 ) ) ;
#6888=CARTESIAN_POINT ( 'NONE',  ( 1.847247051441591514, 12.44188156437794390, 0.1676840720645733362 ) ) ;
#6891=B_SPLINE_CURVE_WITH_KNOTS ( 'NONE', 3,
 ( #17563, #7253, #10592, #4665, #16429, #3311 ),
 .UNSPECIFIED., .F., .F.,
 ( 4, 2, 4 ),
 ( 8.131516293641283255E-19, 0.001657017934709845109, 0.003314035869419688484 ),
 .UNSPECIFIED. ) ;
#6892=CARTESIAN_POINT ( 'NONE',  ( 1.846138399168762989, 11.95493567637850774, 3.446241763653039580 ) ) ;
#6896=CARTESIAN_POINT ( 'NONE',  ( 16.57778382496167424, -0.01354073047775889056, 0.006312874906844006574 ) ) ;
#6897=VERTEX_POINT ( 'NONE', #13366 ) ;
#6900=CARTESIAN_POINT ( 'NONE',  ( 3.950837973638676281, -12.81214529934970336, -6.888253895133431115 ) ) ;
#6903=ORIENTED_EDGE ( 'NONE', *, *, #10629, .T. ) ;
#6904=CARTESIAN_POINT ( 'NONE',  ( 1.562796894703937678, 0.000000000000000000, 0.000000000000000000 ) ) ;
#6908=EDGE_CURVE ( 'NONE', #6039, #2050, #18053, .T. ) ;
#6909=EDGE_CURVE ( 'NONE', #7024, #7279, #15612, .T. ) ;
#6910=EDGE_CURVE ( 'NONE', #12290, #5702, #3936, .T. ) ;
#6911=FACE_OUTER_BOUND ( 'NONE', #16390, .T. ) ;
#6912=DIRECTION ( 'NONE',  ( 0.7635533937278214944, 0.2197766120036505344, -0.6071939193889570596 ) ) ;
#6913=CARTESIAN_POINT ( 'NONE',  ( 0.3142014840576535795, -11.33546131209467767, 7.762239086932820165 ) ) ;
#6914=CARTESIAN_POINT ( 'NONE',  ( 3.074695600507182824, 6.754521329825023734, -14.01296402267889007 ) ) ;
#6919=DIRECTION ( 'NONE',  ( -1.000000000000000000, -0.000000000000000000, -0.000000000000000000 ) ) ;
#6920=EDGE_CURVE ( 'NONE', #7741, #2927, #9067, .T. ) ;
#6921=CARTESIAN_POINT ( 'NONE',  ( 2.002547531651519996, -0.6781519942170860515, -12.57989064830760206 ) ) ;
#6932=ORIENTED_EDGE ( 'NONE', *, *, #13490, .F. ) ;
#6935=B_SPLINE_CURVE_WITH_KNOTS ( 'NONE', 3,
 ( #959, #3922, #1041, #18173, #15483, #10923 ),
 .UNSPECIFIED., .F., .F.,
 ( 4, 2, 4 ),
 ( 0.000000000000000000, 0.001656992708822831520, 0.003313985417645663040 ),
 .UNSPECIFIED. ) ;
#6940=CARTESIAN_POINT ( 'NONE',  ( 16.56782317627811096, 0.009814734722107082768, 0.0003415813796006631126 ) ) ;
#6946=AXIS2_PLACEMENT_3D ( 'NONE', #13286, #17595, #5729 ) ;
#6949=CARTESIAN_POINT ( 'NONE',  ( 16.58200780006414732, -0.01080144354108990290, 0.002844973367390998473 ) ) ;
#6950=CARTESIAN_POINT ( 'NONE',  ( 0.3151930723728423867, -13.09040889075573411, 4.172946285306520231 ) ) ;
#6960=CARTESIAN_POINT ( 'NONE',  ( 2.002547531651519996, -11.75462648437098601, -4.532360870844453160 ) ) ;
#6961=CARTESIAN_POINT ( 'NONE',  ( 1.846955891736115518, 9.909315188408152508, -7.525208385419853485 ) ) ;
#6962=LINE ( 'NONE', #11079, #5366 ) ;
#6970=CARTESIAN_POINT ( 'NONE',  ( 0.3939875929385628361, -8.678227324501040840, -10.75308190953752785 ) ) ;
#6978=ORIENTED_EDGE ( 'NONE', *, *, #17310, .F. ) ;
#6980=EDGE_CURVE ( 'NONE', #15773, #678, #13185, .T. ) ;
#6981=CARTESIAN_POINT ( 'NONE',  ( 16.56872352241294521, 0.004564908236400220913, 0.009382111268606271176 ) ) ;
#6990=CARTESIAN_POINT ( 'NONE',  ( 0.3308579732647025651, -13.74211098745268522, -0.5950689966505779971 ) ) ;
#6993=EDGE_CURVE ( 'NONE', #12620, #11032, #12403, .T. ) ;
#6997=VERTEX_POINT ( 'NONE', #6677 ) ;
#6999=CARTESIAN_POINT ( 'NONE',  ( 2.705023505549866591, -11.23800170568051371, -7.115606223895292182 ) ) ;
#7003=VERTEX_POINT ( 'NONE', #2607 ) ;
#7004=CARTESIAN_POINT ( 'NONE',  ( 0.3142011359265368120, 4.608101617236774139, 12.94258167753013922 ) ) ;
#7006=DIRECTION ( 'NONE',  ( 0.7635533937278216055, 0.1790966170213880715, 0.6204116510013496510 ) ) ;
#7007=CARTESIAN_POINT ( 'NONE',  ( 0.3148213771069364175, -11.24846294176317407, 7.888490156175182122 ) ) ;
#7013=( BOUNDED_SURFACE ( )  B_SPLINE_SURFACE ( 3, 1, ( 
 ( #3437, #9272 ),
 ( #15104, #7438 ),
 ( #2913, #5789 ),
 ( #3204, #1506 ) ),
 .UNSPECIFIED., .F., .F., .T. ) 
 B_SPLINE_SURFACE_WITH_KNOTS ( ( 4, 4 ),
 ( 2, 2 ),
 ( 0.000000000000000000, 1.000000000000000000 ),
 ( 0.000000000000000000, 1.000000000000000000 ),
 .UNSPECIFIED. ) 
 GEOMETRIC_REPRESENTATION_ITEM ( )  RATIONAL_B_SPLINE_SURFACE ( (
 ( 1.000000000000000000, 1.000000000000000000),
 ( 0.7792777138730160313, 0.9689936506012927220),
 ( 0.7792777138730160313, 0.9689936506012927220),
 ( 1.000000000000000000, 1.000000000000000000) ) ) 
 REPRESENTATION_ITEM ( '' )  SURFACE ( )  );
#7018=CARTESIAN_POINT ( 'NONE',  ( 3.950837973638676281, -14.41405733518059229, -1.958075594453940971 ) ) ;
#7021=VERTEX_POINT ( 'NONE', #842 ) ;
#7023=DIRECTION ( 'NONE',  ( 0.7071067818211358436, 0.000000000000000000, -0.7071067805519591909 ) ) ;
#7024=VERTEX_POINT ( 'NONE', #17433 ) ;
#7027=CARTESIAN_POINT ( 'NONE',  ( 0.3095370825347234511, -13.73357284481724427, -0.4597470195091644674 ) ) ;
#7028=EDGE_LOOP ( 'NONE', ( #5166, #743, #18234, #16314 ) ) ;
#7031=LINE ( 'NONE', #9786, #1062 ) ;
#7034=CARTESIAN_POINT ( 'NONE',  ( 16.56679352167444819, -0.009170718284672554205, 0.001518074900131824228 ) ) ;
#7035=CARTESIAN_POINT ( 'NONE',  ( 0.3151926232592480726, -0.07678256780548071980, -13.73922722301401578 ) ) ;
#7036=CARTESIAN_POINT ( 'NONE',  ( 0.4754618798421162973, -12.98792082933648118, 5.007009103465200894 ) ) ;
#7037=ADVANCED_FACE ( 'NONE', ( #14464 ), #6632, .F. ) ;
#7038=CARTESIAN_POINT ( 'NONE',  ( 8.438534575730034959, 2.341351102130369011, -6.454982381540262715 ) ) ;
#7040=EDGE_LOOP ( 'NONE', ( #4316, #945, #13433, #18455 ) ) ;
#7041=EDGE_CURVE ( 'NONE', #415, #1445, #6000, .T. ) ;
#7043=ORIENTED_EDGE ( 'NONE', *, *, #5286, .T. ) ;
#7044=ORIENTED_EDGE ( 'NONE', *, *, #11516, .T. ) ;
#7047=( BOUNDED_SURFACE ( )  B_SPLINE_SURFACE ( 3, 1, ( 
 ( #9147, #3400 ),
 ( #13640, #5882 ),
 ( #2344, #7921 ),
 ( #15167, #8097 ) ),
 .UNSPECIFIED., .F., .F., .T. ) 
 B_SPLINE_SURFACE_WITH_KNOTS ( ( 4, 4 ),
 ( 2, 2 ),
 ( 0.000000000000000000, 1.000000000000000000 ),
 ( 0.000000000000000000, 1.000000000000000000 ),
 .UNSPECIFIED. ) 
 GEOMETRIC_REPRESENTATION_ITEM ( )  RATIONAL_B_SPLINE_SURFACE ( (
 ( 1.000000000000000000, 1.000000000000000000),
 ( 0.9933953342250436691, 0.8357391271907733676),
 ( 0.9933953342250436691, 0.8357391271907733676),
 ( 1.000000000000000000, 1.000000000000000000) ) ) 
 REPRESENTATION_ITEM ( '' )  SURFACE ( )  );
#7052=ORIENTED_EDGE ( 'NONE', *, *, #3302, .F. ) ;
#7053=CARTESIAN_POINT ( 'NONE',  ( 0.8740779401507798863, 5.211551231203803702, 13.31469722824348878 ) ) ;
#7055=VECTOR ( 'NONE', #16229, 1000.000000000000000 ) ;
#7060=CARTESIAN_POINT ( 'NONE',  ( 3.950837973638668288, 0.000000000000000000, 0.000000000000000000 ) ) ;
#7061=VERTEX_POINT ( 'NONE', #13032 ) ;
#7063=CARTESIAN_POINT ( 'NONE',  ( 2.636624412715137922, -15.91454522070252153, 2.161493821597598508 ) ) ;
#7067=ORIENTED_EDGE ( 'NONE', *, *, #2000, .F. ) ;
#7069=ORIENTED_EDGE ( 'NONE', *, *, #8589, .T. ) ;
#7072=DIRECTION ( 'NONE',  ( 0.7635533937278216055, -0.5347026451755990673, 0.3620487483322425981 ) ) ;
#7075=CARTESIAN_POINT ( 'NONE',  ( 16.56872352241294521, -0.001821578298044716857, -0.01027347319884440967 ) ) ;
#7076=CARTESIAN_POINT ( 'NONE',  ( 2.697797270744671128, 10.19107313879056953, 8.537712152180894520 ) ) ;
#7078=CARTESIAN_POINT ( 'NONE',  ( 2.636624412714237309, 7.605649742761960042, 14.14563173255213613 ) ) ;
#7091=ORIENTED_EDGE ( 'NONE', *, *, #18860, .F. ) ;
#7096=CARTESIAN_POINT ( 'NONE',  ( 0.4384471787762814210, -3.577367180593642892, 13.39294437382617353 ) ) ;
#7104=CARTESIAN_POINT ( 'NONE',  ( 3.664313757352971823, -13.97913389346635427, 2.831308606787193316 ) ) ;
#7106=CARTESIAN_POINT ( 'NONE',  ( 1.342453679581834924, 11.38190519890853558, 9.456403821038842139 ) ) ;
#7108=EDGE_LOOP ( 'NONE', ( #14104, #10012, #15317, #15968 ) ) ;
#7115=CARTESIAN_POINT ( 'NONE',  ( 16.56822296793089322, 0.007741272030791174728, -0.006547366384936662183 ) ) ;
#7118=AXIS2_PLACEMENT_3D ( 'NONE', #1643, #10250, #2966 ) ;
#7121=( BOUNDED_SURFACE ( )  B_SPLINE_SURFACE ( 3, 1, ( 
 ( #13117, #11682 ),
 ( #3162, #13306 ),
 ( #6052, #14836 ),
 ( #4526, #10155 ) ),
 .UNSPECIFIED., .F., .F., .T. ) 
 B_SPLINE_SURFACE_WITH_KNOTS ( ( 4, 4 ),
 ( 2, 2 ),
 ( 0.000000000000000000, 1.000000000000000000 ),
 ( 0.000000000000000000, 1.000000000000000000 ),
 .UNSPECIFIED. ) 
 GEOMETRIC_REPRESENTATION_ITEM ( )  RATIONAL_B_SPLINE_SURFACE ( (
 ( 1.000000000000000000, 1.000000000000000000),
 ( 0.7792777138730158093, 0.9689936506012928330),
 ( 0.7792777138730158093, 0.9689936506012928330),
 ( 1.000000000000000000, 1.000000000000000000) ) ) 
 REPRESENTATION_ITEM ( '' )  SURFACE ( )  );
#7122=CARTESIAN_POINT ( 'NONE',  ( 0.3150686449036065317, 13.01866258978842694, -4.391272911157185099 ) ) ;
#7123=ADVANCED_FACE ( 'NONE', ( #5140 ), #13927, .F. ) ;
#7127=CARTESIAN_POINT ( 'NONE',  ( 0.3939875929385618369, 7.545068896001375869, -11.57636969881026801 ) ) ;
#7130=CARTESIAN_POINT ( 'NONE',  ( 16.56822296793089322, -0.009385634690642031749, 0.003834730849371980905 ) ) ;
#7139=CARTESIAN_POINT ( 'NONE',  ( 1.254009781011992342, -5.487405433548717681, -13.61532727684465982 ) ) ;
#7142=CARTESIAN_POINT ( 'NONE',  ( 3.377929128793398128, -13.64476897106782083, -3.070552481925011179 ) ) ;
#7146=EDGE_CURVE ( 'NONE', #10284, #7547, #11929, .T. ) ;
#7148=CIRCLE ( 'NONE', #740, 13.42403576283810906 ) ;
#7155=EDGE_LOOP ( 'NONE', ( #2144, #6580, #9094, #12337 ) ) ;
#7156=B_SPLINE_CURVE_WITH_KNOTS ( 'NONE', 3,
 ( #16463, #14721, #11866, #8992 ),
 .UNSPECIFIED., .F., .F.,
 ( 4, 4 ),
 ( 1.974081779422029518E-17, 0.003005512676784849631 ),
 .UNSPECIFIED. ) ;
#7157=( BOUNDED_SURFACE ( )  B_SPLINE_SURFACE ( 3, 1, ( 
 ( #3657, #9488 ),
 ( #8157, #16842 ),
 ( #15310, #3560 ),
 ( #614, #4098 ) ),
 .UNSPECIFIED., .F., .F., .T. ) 
 B_SPLINE_SURFACE_WITH_KNOTS ( ( 4, 4 ),
 ( 2, 2 ),
 ( 0.000000000000000000, 1.000000000000000000 ),
 ( 0.000000000000000000, 1.000000000000000000 ),
 .UNSPECIFIED. ) 
 GEOMETRIC_REPRESENTATION_ITEM ( )  RATIONAL_B_SPLINE_SURFACE ( (
 ( 1.000000000000000000, 1.000000000000000000),
 ( 0.9593108457356467333, 0.9995965569486454649),
 ( 0.9593108457356467333, 0.9995965569486454649),
 ( 1.000000000000000000, 1.000000000000000000) ) ) 
 REPRESENTATION_ITEM ( '' )  SURFACE ( )  );
#7161=ORIENTED_EDGE ( 'NONE', *, *, #18031, .T. ) ;
#7171=CARTESIAN_POINT ( 'NONE',  ( 2.747332970342022840, -11.45495994260726214, 11.66639548242803492 ) ) ;
#7180=CONICAL_SURFACE ( 'NONE', #2586, 14.54644660717763927, 0.8559913436420816257 ) ;
#7189=CARTESIAN_POINT ( 'NONE',  ( 0.4862570985993235340, -12.97920246947883172, 5.003653737315437944 ) ) ;
#7192=VECTOR ( 'NONE', #213, 1000.000000000000114 ) ;
#7196=CARTESIAN_POINT ( 'NONE',  ( 3.074695600507258320, -7.366518011946037170, 13.70113613813197873 ) ) ;
#7197=CARTESIAN_POINT ( 'NONE',  ( 8.438534575730034959, -1.899950616255142277, -6.598402093327899287 ) ) ;
#7203=CARTESIAN_POINT ( 'NONE',  ( 16.56679352167444819, 0.006618561353600086947, 0.006526964904752371663 ) ) ;
#7204=DIRECTION ( 'NONE',  ( -1.000000000000000000, -0.000000000000000000, -0.000000000000000000 ) ) ;
#7205=B_SPLINE_CURVE_WITH_KNOTS ( 'NONE', 3,
 ( #18743, #5465, #6914, #1260 ),
 .UNSPECIFIED., .F., .F.,
 ( 4, 4 ),
 ( 0.000000000000000000, 0.002004993803842804005 ),
 .UNSPECIFIED. ) ;
#7213=CARTESIAN_POINT ( 'NONE',  ( 0.3720661004400040439, -3.575426119359279564, 13.34435358167251984 ) ) ;
#7217=ORIENTED_EDGE ( 'NONE', *, *, #8387, .T. ) ;
#7218=CARTESIAN_POINT ( 'NONE',  ( 16.57778382496167424, 0.007244066302946777433, 0.01306626476309292149 ) ) ;
#7219=EDGE_LOOP ( 'NONE', ( #7789, #16574, #6350, #16982 ) ) ;
#7220=CARTESIAN_POINT ( 'NONE',  ( 0.4754618798421162973, -13.89949764182682124, -0.7484603771385882620 ) ) ;
#7229=CARTESIAN_POINT ( 'NONE',  ( 0.4862570985993252548, 10.79774104611373353, 8.769551628660776643 ) ) ;
#7232=B_SPLINE_CURVE_WITH_KNOTS ( 'NONE', 3,
 ( #7189, #11391, #17209, #2483, #14345, #9946 ),
 .UNSPECIFIED., .F., .F.,
 ( 4, 2, 4 ),
 ( 1.305552300251627978E-18, 0.001657017934710633541, 0.003314035869421265781 ),
 .UNSPECIFIED. ) ;
#7238=ORIENTED_EDGE ( 'NONE', *, *, #6908, .F. ) ;
#7239=ORIENTED_EDGE ( 'NONE', *, *, #1979, .T. ) ;
#7244=EDGE_LOOP ( 'NONE', ( #13551, #11769, #15161, #8726 ) ) ;
#7252=CARTESIAN_POINT ( 'NONE',  ( 2.002547531651519996, 12.17374746633582561, -3.242439124566524278 ) ) ;
#7253=CARTESIAN_POINT ( 'NONE',  ( 0.8740779401506997282, 9.070947476926598085, 11.05257166392028267 ) ) ;
#7255=CARTESIAN_POINT ( 'NONE',  ( 3.512766787570778870, -6.535475144496882827, -13.55823433651953636 ) ) ;
#7259=EDGE_CURVE ( 'NONE', #16918, #1375, #2147, .T. ) ;
#7265=CARTESIAN_POINT ( 'NONE',  ( 1.861706995891666105, 3.332865258614144732, -12.00328602385076593 ) ) ;
#7267=CARTESIAN_POINT ( 'NONE',  ( 0.3720661004400040439, 7.524064345033631973, -11.58636699658207370 ) ) ;
#7275=CARTESIAN_POINT ( 'NONE',  ( 1.846955891736117517, 11.91257079808168839, 3.593597880662386945 ) ) ;
#7278=DIRECTION ( 'NONE',  ( -1.000000000000000000, -0.000000000000000000, -0.000000000000000000 ) ) ;
#7279=VERTEX_POINT ( 'NONE', #13979 ) ;
#7280=CARTESIAN_POINT ( 'NONE',  ( 1.847421816787903071, 0.02876707915197697710, -12.44300551404155364 ) ) ;
#7282=EDGE_CURVE ( 'NONE', #1657, #767, #4174, .T. ) ;
#7287=EDGE_CURVE ( 'NONE', #7021, #4376, #9005, .T. ) ;
#7288=ORIENTED_EDGE ( 'NONE', *, *, #17295, .F. ) ;
#7295=CARTESIAN_POINT ( 'NONE',  ( 0.3142011359265320380, -3.879426116491784260, 13.17934269988456819 ) ) ;
#7296=CARTESIAN_POINT ( 'NONE',  ( 0.3939822652208137543, 11.57634296752778802, -7.545099438011897419 ) ) ;
#7300=CARTESIAN_POINT ( 'NONE',  ( 0.3137051932979809665, -13.20008686438108647, 3.805684345189735307 ) ) ;
#7302=CARTESIAN_POINT ( 'NONE',  ( 16.56679352167444819, 0.004162264567718796174, -0.008311568981097996328 ) ) ;
#7305=DIRECTION ( 'NONE',  ( 0.000000000000000000, 0.000000000000000000, 1.000000000000000000 ) ) ;
#7308=ADVANCED_FACE ( 'NONE', ( #15039 ), #17110, .F. ) ;
#7316=ORIENTED_EDGE ( 'NONE', *, *, #14797, .F. ) ;
#7317=CARTESIAN_POINT ( 'NONE',  ( 1.846613052777650976, 9.862487290071108248, -7.585914669018062106 ) ) ;
#7320=AXIS2_PLACEMENT_3D ( 'NONE', #16023, #14590, #70 ) ;
#7323=CARTESIAN_POINT ( 'NONE',  ( 2.320520222536938348, -1.795797593768547085, 15.64520721754664123 ) ) ;
#7327=FACE_OUTER_BOUND ( 'NONE', #9673, .T. ) ;
#7328=CARTESIAN_POINT ( 'NONE',  ( 16.57210152137263393, 0.008007331252333427934, -0.01214401161737626612 ) ) ;
#7329=ORIENTED_EDGE ( 'NONE', *, *, #12794, .T. ) ;
#7339=CARTESIAN_POINT ( 'NONE',  ( 8.522092701127531811, -2.505958102592667824, 6.489356537178181838 ) ) ;
#7342=ORIENTED_EDGE ( 'NONE', *, *, #18030, .F. ) ;
#7344=DIRECTION ( 'NONE',  ( 0.7561779333270775005, -0.5491072561318390832, 0.3559159372837255031 ) ) ;
#7347=CARTESIAN_POINT ( 'NONE',  ( 8.522092701127531811, 0.3779863304872196350, -6.946128462138591253 ) ) ;
#7348=EDGE_CURVE ( 'NONE', #348, #14985, #16578, .T. ) ;
#7352=CARTESIAN_POINT ( 'NONE',  ( 0.3148213771069373057, 4.463459503829174224, -12.99360322443197724 ) ) ;
#7356=ORIENTED_EDGE ( 'NONE', *, *, #12769, .T. ) ;
#7358=ORIENTED_EDGE ( 'NONE', *, *, #12308, .T. ) ;
#7361=CARTESIAN_POINT ( 'NONE',  ( 1.845756295923353996, 3.386818134580228179, -11.97166802574122890 ) ) ;
#7363=CARTESIAN_POINT ( 'NONE',  ( 8.438534575730034959, -3.845978796786076348, 5.688336279099031501 ) ) ;
#7367=CARTESIAN_POINT ( 'NONE',  ( 0.3148213771069355293, -4.026433757158891957, -13.13560149728604998 ) ) ;
#7368=B_SPLINE_CURVE_WITH_KNOTS ( 'NONE', 3,
 ( #14441, #11394, #9949, #15503, #12911, #6812 ),
 .UNSPECIFIED., .F., .F.,
 ( 4, 2, 4 ),
 ( 4.192373019364431701E-17, 0.0002014099069817294621, 0.0004028198139634169657 ),
 .UNSPECIFIED. ) ;
#7373=CARTESIAN_POINT ( 'NONE',  ( 0.3142014840576536350, 12.94260032291128759, 4.608051180496968158 ) ) ;
#7376=CARTESIAN_POINT ( 'NONE',  ( 1.847380140988740260, 7.224522571381473135, -10.13114603776188893 ) ) ;
#7380=CARTESIAN_POINT ( 'NONE',  ( 0.4754618798421162973, 13.89949764182682657, -0.7484603771384912285 ) ) ;
#7381=VERTEX_POINT ( 'NONE', #17309 ) ;
#7382=CARTESIAN_POINT ( 'NONE',  ( 0.3939875929385642239, -0.7003304234512184312, -13.80036004410494854 ) ) ;
#7389=EDGE_CURVE ( 'NONE', #14913, #1370, #7368, .T. ) ;
#7390=EDGE_CURVE ( 'NONE', #11620, #8960, #1433, .T. ) ;
#7395=CARTESIAN_POINT ( 'NONE',  ( 16.57778382496167424, 0.001819584982831899374, -0.01482878558584570412 ) ) ;
#7397=CARTESIAN_POINT ( 'NONE',  ( 0.3170788640506441158, -7.952793437297652090, 11.20690911610900997 ) ) ;
#7399=ORIENTED_EDGE ( 'NONE', *, *, #11488, .F. ) ;
#7400=CARTESIAN_POINT ( 'NONE',  ( 1.845756295923359547, 4.296776483139476355, 11.67600463554274626 ) ) ;
#7404=ORIENTED_EDGE ( 'NONE', *, *, #5570, .T. ) ;
#7423=CARTESIAN_POINT ( 'NONE',  ( 16.56872352241294521, 0.009207754980064196751, -0.004907101719995712874 ) ) ;
#7433=CARTESIAN_POINT ( 'NONE',  ( 16.56872352241294521, 0.009207754980064196751, -0.004907101719995712874 ) ) ;
#7434=ORIENTED_EDGE ( 'NONE', *, *, #6830, .F. ) ;
#7437=CARTESIAN_POINT ( 'NONE',  ( 0.4862570985993235340, 8.769551628660890330, -10.79774104611363761 ) ) ;
#7438=CARTESIAN_POINT ( 'NONE',  ( 1.342453679581834924, -3.649820028552632767, -14.34050741580210619 ) ) ;
#7439=CARTESIAN_POINT ( 'NONE',  ( 0.3142014840576498047, 7.762239086932858356, 11.33546131209465102 ) ) ;
#7440=EDGE_CURVE ( 'NONE', #12470, #11533, #14660, .T. ) ;
#7442=CARTESIAN_POINT ( 'NONE',  ( 1.846138399168762101, 11.95493567637855392, -3.446241763652874379 ) ) ;
#7443=CARTESIAN_POINT ( 'NONE',  ( 1.846138399168762989, 9.815003036200414144, 7.646096044339929954 ) ) ;
#7444=ADVANCED_FACE ( 'NONE', ( #18458 ), #4739, .T. ) ;
#7449=EDGE_LOOP ( 'NONE', ( #10499, #15432, #2165, #912 ) ) ;
#7454=VERTEX_POINT ( 'NONE', #18556 ) ;
#7456=VECTOR ( 'NONE', #7344, 1000.000000000000114 ) ;
#7461=ORIENTED_EDGE ( 'NONE', *, *, #11992, .T. ) ;
#7471=CARTESIAN_POINT ( 'NONE',  ( 2.636624412716045196, 11.10302021257998994, -11.60464335004042447 ) ) ;
#7483=CARTESIAN_POINT ( 'NONE',  ( 2.002547531651519996, 11.75462648437101976, 4.532360870844369671 ) ) ;
#7486=VECTOR ( 'NONE', #621, 1000.000000000000227 ) ;
#7488=CARTESIAN_POINT ( 'NONE',  ( 0.3095370825347224519, -8.444334731363925428, -10.84046130709067768 ) ) ;
#7491=CARTESIAN_POINT ( 'NONE',  ( 1.342453679581834924, 0.9602753779830727199, 14.76648944001039787 ) ) ;
#7492=CARTESIAN_POINT ( 'NONE',  ( 0.4754618798421167414, 13.45049478164064638, -3.583352865732531534 ) ) ;
#7496=CARTESIAN_POINT ( 'NONE',  ( 0.3137051932979792457, -13.73004976592202375, 0.4596302728639276580 ) ) ;
#7501=EDGE_CURVE ( 'NONE', #16313, #7003, #8680, .T. ) ;
#7503=CARTESIAN_POINT ( 'NONE',  ( 1.846822687350018866, -0.2922081769261017925, 12.43915556955403723 ) ) ;
#7507=CARTESIAN_POINT ( 'NONE',  ( 1.847372867223022519, 10.12831093686732586, -7.228345833872643844 ) ) ;
#7510=CARTESIAN_POINT ( 'NONE',  ( 0.3132642857406529591, -8.495623922778147374, 10.79548167658031588 ) ) ;
#7513=CARTESIAN_POINT ( 'NONE',  ( 0.3137051932979757485, -7.698472063774552510, 11.37800749014128421 ) ) ;
#7521=CARTESIAN_POINT ( 'NONE',  ( 1.846138399168762101, -11.69739621335919111, -4.238866729160527314 ) ) ;
#7526=VECTOR ( 'NONE', #5860, 1000.000000000000114 ) ;
#7527=VERTEX_POINT ( 'NONE', #6792 ) ;
#7530=EDGE_CURVE ( 'NONE', #14742, #10307, #12175, .T. ) ;
#7532=CARTESIAN_POINT ( 'NONE',  ( 0.3720661004400037664, -12.89739157014188997, -4.951033743989776248 ) ) ;
#7534=DIRECTION ( 'NONE',  ( 0.7635533937278214944, -0.6071939193889578368, -0.2197766120036483140 ) ) ;
#7539=CARTESIAN_POINT ( 'NONE',  ( 3.377929128793395908, -3.070552481924963217, 13.64476897106782971 ) ) ;
#7543=DIRECTION ( 'NONE',  ( 0.000000000000000000, 0.000000000000000000, 1.000000000000000000 ) ) ;
#7547=VERTEX_POINT ( 'NONE', #12605 ) ;
#7548=ORIENTED_EDGE ( 'NONE', *, *, #10715, .F. ) ;
#7550=ORIENTED_EDGE ( 'NONE', *, *, #17793, .F. ) ;
#7554=ORIENTED_EDGE ( 'NONE', *, *, #11935, .T. ) ;
#7559=B_SPLINE_CURVE_WITH_KNOTS ( 'NONE', 3,
 ( #5446, #11292, #17108, #6990, #12804, #4110 ),
 .UNSPECIFIED., .F., .F.,
 ( 4, 2, 4 ),
 ( 4.276569467073304015E-17, 0.0002014099069817285948, 0.0004028198139634144178 ),
 .UNSPECIFIED. ) ;
#7567=CARTESIAN_POINT ( 'NONE',  ( 1.342453679581834924, 7.902645620902629453, -12.51077660954457293 ) ) ;
#7569=CARTESIAN_POINT ( 'NONE',  ( 2.002547531651519996, -12.57989064830759141, -0.6781519942173057647 ) ) ;
#7570=CIRCLE ( 'NONE', #1438, 14.54644660717763927 ) ;
#7574=CARTESIAN_POINT ( 'NONE',  ( 16.56679352167444819, 0.004277682826583292797, 0.008252760440870202802 ) ) ;
#7575=ORIENTED_EDGE ( 'NONE', *, *, #16940, .T. ) ;
#7579=CARTESIAN_POINT ( 'NONE',  ( 1.846138399168762101, -11.69739621335919111, -4.238866729160527314 ) ) ;
#7580=LINE ( 'NONE', #17891, #379 ) ;
#7581=B_SPLINE_CURVE_WITH_KNOTS ( 'NONE', 3,
 ( #2953, #8801, #14624, #2119, #3635, #7671 ),
 .UNSPECIFIED., .F., .F.,
 ( 4, 2, 4 ),
 ( 3.522439207679730663E-17, 0.0001825746017570583171, 0.0003651492035140813976 ),
 .UNSPECIFIED. ) ;
#7584=FACE_OUTER_BOUND ( 'NONE', #16017, .T. ) ;
#7586=ORIENTED_EDGE ( 'NONE', *, *, #6910, .T. ) ;
#7588=CARTESIAN_POINT ( 'NONE',  ( 0.4862570985993235340, -10.79774104611366781, -8.769551628660854803 ) ) ;
#7606=ORIENTED_EDGE ( 'NONE', *, *, #7390, .F. ) ;
#7610=CARTESIAN_POINT ( 'NONE',  ( 0.3095370825347224519, -0.4597470195091133416, 13.73357284481724605 ) ) ;
#7613=FACE_OUTER_BOUND ( 'NONE', #15130, .T. ) ;
#7619=DIRECTION ( 'NONE',  ( -1.000000000000000000, 0.000000000000000000, 0.000000000000000000 ) ) ;
#7620=CARTESIAN_POINT ( 'NONE',  ( 16.56872352241294521, 0.004907101719994633009, -0.009207754980063766539 ) ) ;
#7623=CARTESIAN_POINT ( 'NONE',  ( 0.3720661004400037664, 11.58636699658225844, -7.524064345033335321 ) ) ;
#7630=CARTESIAN_POINT ( 'NONE',  ( 0.3151928476913555821, -8.075884471919669849, -11.11514699826559571 ) ) ;
#7631=DIRECTION ( 'NONE',  ( -0.7635533937278214944, 0.2197766120036462600, 0.6071939193889586139 ) ) ;
#7639=EDGE_CURVE ( 'NONE', #6997, #13145, #1665, .T. ) ;
#7645=( BOUNDED_SURFACE ( )  B_SPLINE_SURFACE ( 3, 1, ( 
 ( #12621, #5365 ),
 ( #16934, #1247 ),
 ( #12445, #11301 ),
 ( #14256, #18277 ) ),
 .UNSPECIFIED., .F., .F., .T. ) 
 B_SPLINE_SURFACE_WITH_KNOTS ( ( 4, 4 ),
 ( 2, 2 ),
 ( 0.000000000000000000, 1.000000000000000000 ),
 ( 0.000000000000000000, 1.000000000000000000 ),
 .UNSPECIFIED. ) 
 GEOMETRIC_REPRESENTATION_ITEM ( )  RATIONAL_B_SPLINE_SURFACE ( (
 ( 1.000000000000000000, 1.000000000000000000),
 ( 0.7792777138730158093, 0.9689936506012928330),
 ( 0.7792777138730158093, 0.9689936506012928330),
 ( 1.000000000000000000, 1.000000000000000000) ) ) 
 REPRESENTATION_ITEM ( '' )  SURFACE ( )  );
#7647=ORIENTED_EDGE ( 'NONE', *, *, #14005, .T. ) ;
#7649=EDGE_LOOP ( 'NONE', ( #6563, #639, #17574, #12901 ) ) ;
#7671=CARTESIAN_POINT ( 'NONE',  ( 1.846138399168762989, 11.95493567637850774, 3.446241763653039580 ) ) ;
#7672=CARTESIAN_POINT ( 'NONE',  ( 8.438534575730034959, -5.415535776177550886, 4.221456476902647914 ) ) ;
#7673=ORIENTED_EDGE ( 'NONE', *, *, #16056, .T. ) ;
#7674=CARTESIAN_POINT ( 'NONE',  ( 3.512766787570801519, 6.535475144496956545, 13.55823433651946175 ) ) ;
#7676=( BOUNDED_SURFACE ( )  B_SPLINE_SURFACE ( 3, 1, ( 
 ( #7852, #6594 ),
 ( #15098, #16631 ),
 ( #13672, #2372 ),
 ( #16728, #12420 ) ),
 .UNSPECIFIED., .F., .F., .T. ) 
 B_SPLINE_SURFACE_WITH_KNOTS ( ( 4, 4 ),
 ( 2, 2 ),
 ( 0.000000000000000000, 1.000000000000000000 ),
 ( 0.000000000000000000, 1.000000000000000000 ),
 .UNSPECIFIED. ) 
 GEOMETRIC_REPRESENTATION_ITEM ( )  RATIONAL_B_SPLINE_SURFACE ( (
 ( 1.000000000000000000, 1.000000000000000000),
 ( 0.9933953342250438912, 0.8357391271907739227),
 ( 0.9933953342250438912, 0.8357391271907739227),
 ( 1.000000000000000000, 1.000000000000000000) ) ) 
 REPRESENTATION_ITEM ( '' )  SURFACE ( )  );
#7678=CARTESIAN_POINT ( 'NONE',  ( 8.522092701127531811, -5.841710761610158009, 3.777034505568503064 ) ) ;
#7687=CARTESIAN_POINT ( 'NONE',  ( 0.3151926232592466848, 11.16039997398654116, 8.013596737356428079 ) ) ;
#7690=FACE_OUTER_BOUND ( 'NONE', #9446, .T. ) ;
#7699=CARTESIAN_POINT ( 'NONE',  ( 1.846524061778019199, -0.3544704288993353880, 12.43723828841088341 ) ) ;
#7700=EDGE_LOOP ( 'NONE', ( #15549, #5162, #3099, #5314 ) ) ;
#7706=FACE_OUTER_BOUND ( 'NONE', #58, .T. ) ;
#7709=CARTESIAN_POINT ( 'NONE',  ( 3.950837973638668288, 0.000000000000000000, 0.000000000000000000 ) ) ;
#7715=CARTESIAN_POINT ( 'NONE',  ( 2.002547531651519996, 11.75462648437101976, 4.532360870844369671 ) ) ;
#7718=VERTEX_POINT ( 'NONE', #10214 ) ;
#7724=CARTESIAN_POINT ( 'NONE',  ( 0.3137051932979809665, 10.83767969834803324, 8.442169467526891680 ) ) ;
#7731=CARTESIAN_POINT ( 'NONE',  ( 0.3145729642390364678, 8.321438378985256179, 10.93201268464375353 ) ) ;
#7736=CARTESIAN_POINT ( 'NONE',  ( 1.847247051441591292, 7.177495230324704600, 10.16425585218603267 ) ) ;
#7741=VERTEX_POINT ( 'NONE', #14898 ) ;
#7743=EDGE_CURVE ( 'NONE', #3320, #10843, #1629, .T. ) ;
#7744=EDGE_CURVE ( 'NONE', #10843, #4344, #16230, .T. ) ;
#7745=EDGE_CURVE ( 'NONE', #15231, #16174, #10702, .T. ) ;
#7753=CARTESIAN_POINT ( 'NONE',  ( 16.56872352241294521, 0.009382111268607367521, 0.004564908236399998868 ) ) ;
#7754=CARTESIAN_POINT ( 'NONE',  ( 1.342453679581834924, -7.902645620902536194, 12.51077660954462978 ) ) ;
#7780=CARTESIAN_POINT ( 'NONE',  ( 2.636624412715138366, -15.91454522070249311, -2.161493821597819665 ) ) ;
#7789=ORIENTED_EDGE ( 'NONE', *, *, #15765, .T. ) ;
#7790=VECTOR ( 'NONE', #8007, 1000.000000000000000 ) ;
#7816=VERTEX_POINT ( 'NONE', #377 ) ;
#7821=VECTOR ( 'NONE', #5864, 1000.000000000000114 ) ;
#7839=ORIENTED_EDGE ( 'NONE', *, *, #1120, .T. ) ;
#7840=ORIENTED_EDGE ( 'NONE', *, *, #16070, .T. ) ;
#7841=CARTESIAN_POINT ( 'NONE',  ( 2.636624412716061627, -7.605649742761058540, -14.14563173255469408 ) ) ;
#7845=CARTESIAN_POINT ( 'NONE',  ( 0.4862570985993235340, 0.7479633556562450547, 13.89016912371017831 ) ) ;
#7852=CARTESIAN_POINT ( 'NONE',  ( 16.56872352241294521, -0.009382111268606286789, 0.004564908236400187953 ) ) ;
#7861=ORIENTED_EDGE ( 'NONE', *, *, #17410, .F. ) ;
#7863=VECTOR ( 'NONE', #4168, 1000.000000000000000 ) ;
#7864=VECTOR ( 'NONE', #7023, 1000.000000000000000 ) ;
#7865=CIRCLE ( 'NONE', #6328, 16.06066017081991149 ) ;
#7871=( BOUNDED_SURFACE ( )  B_SPLINE_SURFACE ( 3, 1, ( 
 ( #12013, #6381 ),
 ( #6086, #353 ),
 ( #11916, #14877 ),
 ( #4654, #6182 ) ),
 .UNSPECIFIED., .F., .F., .T. ) 
 B_SPLINE_SURFACE_WITH_KNOTS ( ( 4, 4 ),
 ( 2, 2 ),
 ( 0.000000000000000000, 1.000000000000000000 ),
 ( 0.000000000000000000, 1.000000000000000000 ),
 .UNSPECIFIED. ) 
 GEOMETRIC_REPRESENTATION_ITEM ( )  RATIONAL_B_SPLINE_SURFACE ( (
 ( 1.000000000000000000, 1.000000000000000000),
 ( 0.9933953342250438912, 0.8357391271907739227),
 ( 0.9933953342250438912, 0.8357391271907739227),
 ( 1.000000000000000000, 1.000000000000000000) ) ) 
 REPRESENTATION_ITEM ( '' )  SURFACE ( )  );
#7874=CARTESIAN_POINT ( 'NONE',  ( 8.522092701127531811, 4.388629235579577070, 5.397361180353158261 ) ) ;
#7875=AXIS2_PLACEMENT_3D ( 'NONE', #15799, #4148, #7305 ) ;
#7877=CARTESIAN_POINT ( 'NONE',  ( 2.320520222536476496, 15.64520721754621491, 1.795797593768047262 ) ) ;
#7878=B_SPLINE_CURVE_WITH_KNOTS ( 'NONE', 3,
 ( #17089, #9809, #2542, #8391, #14222, #1122 ),
 .UNSPECIFIED., .F., .F.,
 ( 4, 2, 4 ),
 ( 0.000000000000000000, 0.001657017934709840989, 0.003314035869419681979 ),
 .UNSPECIFIED. ) ;
#7883=CARTESIAN_POINT ( 'NONE',  ( 2.002547531651519996, -4.532360870844247991, -11.75462648437106417 ) ) ;
#7890=ORIENTED_EDGE ( 'NONE', *, *, #16782, .T. ) ;
#7893=ORIENTED_EDGE ( 'NONE', *, *, #13574, .F. ) ;
#7895=B_SPLINE_CURVE_WITH_KNOTS ( 'NONE', 3,
 ( #5536, #11482, #11577, #9838 ),
 .UNSPECIFIED., .F., .F.,
 ( 4, 4 ),
 ( 1.464275143509529362E-17, 0.003005512676784844427 ),
 .UNSPECIFIED. ) ;
#7896=CARTESIAN_POINT ( 'NONE',  ( 0.3137051932979792457, 11.37800749014142276, -7.698472063774345564 ) ) ;
#7897=ORIENTED_EDGE ( 'NONE', *, *, #17714, .F. ) ;
#7898=CARTESIAN_POINT ( 'NONE',  ( 0.3720661004400040439, 11.58636699658215541, 7.524064345033506740 ) ) ;
#7899=ORIENTED_EDGE ( 'NONE', *, *, #11190, .T. ) ;
#7900=CARTESIAN_POINT ( 'NONE',  ( 3.074695600508088322, 15.41438262616131283, 2.093687500611883578 ) ) ;
#7901=CARTESIAN_POINT ( 'NONE',  ( 0.3151926232592509591, -13.73922722301401400, 0.07678256780552859817 ) ) ;
#7910=CARTESIAN_POINT ( 'NONE',  ( 0.3058872367615230181, -8.562166468153638021, -10.75034008168925226 ) ) ;
#7911=CARTESIAN_POINT ( 'NONE',  ( 3.377929128793386138, 13.92579934231094718, -1.296196549818984911 ) ) ;
#7913=CARTESIAN_POINT ( 'NONE',  ( 0.3137051932979775248, 3.805684345189972895, -13.20008686438101719 ) ) ;
#7916=ORIENTED_EDGE ( 'NONE', *, *, #10047, .T. ) ;
#7918=ORIENTED_EDGE ( 'NONE', *, *, #5587, .F. ) ;
#7920=CARTESIAN_POINT ( 'NONE',  ( 0.4862570985993235340, 12.97920246947886191, -5.003653737315353567 ) ) ;
#7921=CARTESIAN_POINT ( 'NONE',  ( 0.3720661004400037664, -7.524064345033377954, -11.58636699658223179 ) ) ;
#7924=FACE_OUTER_BOUND ( 'NONE', #9519, .T. ) ;
#7926=CARTESIAN_POINT ( 'NONE',  ( 0.4754618798421171855, 10.80499583390525764, -8.775436892860993154 ) ) ;
#7928=CARTESIAN_POINT ( 'NONE',  ( 2.636624412716061627, -7.605649742761058540, -14.14563173255469408 ) ) ;
#7931=CARTESIAN_POINT ( 'NONE',  ( 8.522092701127531811, -2.505958102592576342, -6.489356537178215589 ) ) ;
#7933=ADVANCED_FACE ( 'NONE', ( #16892 ), #7180, .T. ) ;
#7934=ORIENTED_EDGE ( 'NONE', *, *, #11937, .T. ) ;
#7948=EDGE_CURVE ( 'NONE', #9927, #7816, #16709, .T. ) ;
#7949=CARTESIAN_POINT ( 'NONE',  ( 1.342453679581834924, -14.34050741580209198, 3.649820028552675844 ) ) ;
#7951=CARTESIAN_POINT ( 'NONE',  ( 0.3058872367615230181, 12.87003593440634930, -4.821066432589193873 ) ) ;
#7955=CARTESIAN_POINT ( 'NONE',  ( 3.950837973638668288, 0.000000000000000000, 0.000000000000000000 ) ) ;
#7959=ORIENTED_EDGE ( 'NONE', *, *, #18629, .T. ) ;
#7961=ORIENTED_EDGE ( 'NONE', *, *, #3153, .F. ) ;
#7965=CARTESIAN_POINT ( 'NONE',  ( 1.846613052777651198, 3.520031056876471887, -11.93415846513958023 ) ) ;
#7967=CARTESIAN_POINT ( 'NONE',  ( 3.377929128793398128, 7.136734442941011558, -12.02809354424093691 ) ) ;
#7975=CARTESIAN_POINT ( 'NONE',  ( 2.002547531651520885, -4.532360870844412304, 11.75462648437100377 ) ) ;
#7976=B_SPLINE_CURVE_WITH_KNOTS ( 'NONE', 3,
 ( #13079, #15755, #5708, #4105 ),
 .UNSPECIFIED., .F., .F.,
 ( 4, 4 ),
 ( 0.000000000000000000, 0.002004993803842769744 ),
 .UNSPECIFIED. ) ;
#7977=EDGE_LOOP ( 'NONE', ( #15297, #14017, #1367, #13082 ) ) ;
#7978=CARTESIAN_POINT ( 'NONE',  ( 2.320520222537280297, -15.64520721754692190, -1.795797593768913236 ) ) ;
#7979=CARTESIAN_POINT ( 'NONE',  ( 1.861706995891668326, 11.66987142852990189, -4.359009869687124450 ) ) ;
#7980=( BOUNDED_SURFACE ( )  B_SPLINE_SURFACE ( 3, 1, ( 
 ( #15044, #10461 ),
 ( #13614, #16103 ),
 ( #6260, #9029 ),
 ( #1766, #7610 ) ),
 .UNSPECIFIED., .F., .F., .T. ) 
 B_SPLINE_SURFACE_WITH_KNOTS ( ( 4, 4 ),
 ( 2, 2 ),
 ( 0.000000000000000000, 1.000000000000000000 ),
 ( 0.000000000000000000, 1.000000000000000000 ),
 .UNSPECIFIED. ) 
 GEOMETRIC_REPRESENTATION_ITEM ( )  RATIONAL_B_SPLINE_SURFACE ( (
 ( 1.000000000000000000, 1.000000000000000000),
 ( 0.9593108457356467333, 0.9995965569486454649),
 ( 0.9593108457356467333, 0.9995965569486454649),
 ( 1.000000000000000000, 1.000000000000000000) ) ) 
 REPRESENTATION_ITEM ( '' )  SURFACE ( )  );
#7984=CARTESIAN_POINT ( 'NONE',  ( 8.522092701127531811, -6.946128462138593029, -0.3779863304871954321 ) ) ;
#7995=CARTESIAN_POINT ( 'NONE',  ( 3.353306896162455697, 13.88482890973696726, 1.348936822032873240 ) ) ;
#7996=CARTESIAN_POINT ( 'NONE',  ( 2.320520222538103638, 6.542539914241700671, -14.32454429810417906 ) ) ;
#7998=CARTESIAN_POINT ( 'NONE',  ( 2.002547531651519996, -6.845637710436110801, -10.57595306287299763 ) ) ;
#8003=EDGE_LOOP ( 'NONE', ( #8569, #5988, #18525, #8850 ) ) ;
#8004=VERTEX_POINT ( 'NONE', #5986 ) ;
#8007=DIRECTION ( 'NONE',  ( -1.000000000000000000, 0.000000000000000000, 0.000000000000000000 ) ) ;
#8008=ADVANCED_FACE ( 'NONE', ( #18882 ), #8564, .F. ) ;
#8009=CARTESIAN_POINT ( 'NONE',  ( 1.342453679581834924, 7.902645620902447376, 12.51077660954468662 ) ) ;
#8010=CARTESIAN_POINT ( 'NONE',  ( 1.847247051441591514, -11.88474976472815214, 3.685275815977142599 ) ) ;
#8026=CARTESIAN_POINT ( 'NONE',  ( 16.57210152137263393, -0.005118120558002011225, -0.01361613799508959964 ) ) ;
#8027=AXIS2_PLACEMENT_3D ( 'NONE', #15903, #14286, #9974 ) ;
#8030=EDGE_LOOP ( 'NONE', ( #4057, #13435, #16445, #17946 ) ) ;
#8031=CARTESIAN_POINT ( 'NONE',  ( 2.123976203522053297, -11.67822624909917550, -10.37815841598504107 ) ) ;
#8032=DIRECTION ( 'NONE',  ( -0.7561779333270775005, 0.5491072561318340872, 0.3559159372837335522 ) ) ;
#8033=EDGE_CURVE ( 'NONE', #617, #15501, #14627, .T. ) ;
#8038=CARTESIAN_POINT ( 'NONE',  ( 1.846138399168762989, 11.95493567637850774, 3.446241763653039580 ) ) ;
#8040=CARTESIAN_POINT ( 'NONE',  ( 0.3137051932979792457, 11.37800749014131263, 7.698472063774513430 ) ) ;
#8050=B_SPLINE_CURVE_WITH_KNOTS ( 'NONE', 3,
 ( #7845, #13666, #9167, #14900, #6307, #15193 ),
 .UNSPECIFIED., .F., .F.,
 ( 4, 2, 4 ),
 ( 5.421010862427522170E-20, 0.001657017934710529891, 0.003314035869421059783 ),
 .UNSPECIFIED. ) ;
#8057=B_SPLINE_CURVE_WITH_KNOTS ( 'NONE', 3,
 ( #4971, #8220, #13674, #10806, #16632, #6503 ),
 .UNSPECIFIED., .F., .F.,
 ( 4, 2, 4 ),
 ( 9.263427422397552964E-19, 0.001500839035891552656, 0.003001678071783104446 ),
 .UNSPECIFIED. ) ;
#8060=CARTESIAN_POINT ( 'NONE',  ( 0.3137051932979809665, 13.20008686438111312, -3.805684345189650042 ) ) ;
#8065=EDGE_CURVE ( 'NONE', #14465, #16063, #4137, .T. ) ;
#8068=CARTESIAN_POINT ( 'NONE',  ( 1.918918678667046240, 11.69059232068584819, -4.466049546133788795 ) ) ;
#8070=B_SPLINE_CURVE_WITH_KNOTS ( 'NONE', 3,
 ( #16882, #10885, #6763, #6215, #13824, #9443 ),
 .UNSPECIFIED., .F., .F.,
 ( 4, 2, 4 ),
 ( 4.027530160694267299E-17, 0.0002014099069817290014, 0.0004028198139634177246 ),
 .UNSPECIFIED. ) ;
#8072=CARTESIAN_POINT ( 'NONE',  ( 1.861706995891668104, -9.751699138048492088, 7.751853334747282886 ) ) ;
#8073=CARTESIAN_POINT ( 'NONE',  ( 16.56872352241294521, -0.001442253899401880124, -0.01033355228142401362 ) ) ;
#8074=VERTEX_POINT ( 'NONE', #61 ) ;
#8076=CIRCLE ( 'NONE', #2261, 12.15840553252917289 ) ;
#8079=CARTESIAN_POINT ( 'NONE',  ( 0.4754618798421171855, 12.98792082933651493, -5.007009103465112076 ) ) ;
#8085=EDGE_CURVE ( 'NONE', #10095, #14563, #8853, .T. ) ;
#8089=CARTESIAN_POINT ( 'NONE',  ( 0.3939875929385656117, -13.34133634968952720, -3.598491969338368346 ) ) ;
#8097=CARTESIAN_POINT ( 'NONE',  ( 0.4754618798421162973, -7.564402563418381575, -11.68486377711974811 ) ) ;
#8099=VERTEX_POINT ( 'NONE', #16512 ) ;
#8101=LINE ( 'NONE', #12301, #16206 ) ;
#8108=CARTESIAN_POINT ( 'NONE',  ( 0.3095370825347224519, -3.806662003783324089, -13.20347358821918249 ) ) ;
#8109=CARTESIAN_POINT ( 'NONE',  ( 3.512766787570764215, -6.535475144497081779, 13.55823433651946175 ) ) ;
#8111=ADVANCED_FACE ( 'NONE', ( #16317 ), #11760, .F. ) ;
#8116=VERTEX_POINT ( 'NONE', #10584 ) ;
#8124=CARTESIAN_POINT ( 'NONE',  ( 16.56872352241294521, 0.001821578298044641397, 0.01027347319884442528 ) ) ;
#8129=DIRECTION ( 'NONE',  ( 0.000000000000000000, 0.000000000000000000, 1.000000000000000000 ) ) ;
#8132=CARTESIAN_POINT ( 'NONE',  ( 1.918921323896325193, -4.466082741316288462, 11.69058285425789201 ) ) ;
#8136=ADVANCED_FACE ( 'NONE', ( #9047 ), #7871, .F. ) ;
#8140=CIRCLE ( 'NONE', #806, 14.54644660717763927 ) ;
#8143=VERTEX_POINT ( 'NONE', #14966 ) ;
#8145=CARTESIAN_POINT ( 'NONE',  ( 0.4862570985993235340, 3.580942890621860109, -13.44146924561377254 ) ) ;
#8146=DIRECTION ( 'NONE',  ( 0.7635533937278216055, 0.6453904417649386493, 0.02138673900302558509 ) ) ;
#8148=ADVANCED_FACE ( 'NONE', ( #1886 ), #6001, .F. ) ;
#8152=CARTESIAN_POINT ( 'NONE',  ( 0.3170788640506440603, 8.200855617524691610, -11.02668139258432944 ) ) ;
#8153=FACE_OUTER_BOUND ( 'NONE', #17141, .T. ) ;
#8157=CARTESIAN_POINT ( 'NONE',  ( 16.56679352167444819, -0.004277682826582317882, 0.008252760440870482092 ) ) ;
#8161=ORIENTED_EDGE ( 'NONE', *, *, #5261, .T. ) ;
#8167=CARTESIAN_POINT ( 'NONE',  ( 0.4754618798421171855, -0.7484603771383426807, -13.89949764182683545 ) ) ;
#8168=EDGE_CURVE ( 'NONE', #9866, #6897, #10303, .T. ) ;
#8170=CARTESIAN_POINT ( 'NONE',  ( 1.847168016377985111, -10.17509564929253507, -7.161712042621569019 ) ) ;
#8173=DIRECTION ( 'NONE',  ( -1.000000000000000000, -0.000000000000000000, -0.000000000000000000 ) ) ;
#8177=DIRECTION ( 'NONE',  ( -1.000000000000000000, -0.000000000000000000, -0.000000000000000000 ) ) ;
#8178=CARTESIAN_POINT ( 'NONE',  ( 0.3307726912345191894, -4.812300915532890855, -12.88561780039863436 ) ) ;
#8179=CARTESIAN_POINT ( 'NONE',  ( 16.56679352167444819, -0.001390132774595520624, -0.009190982326619362083 ) ) ;
#8180=CARTESIAN_POINT ( 'NONE',  ( 2.636624412716062071, -14.14563173255412742, -7.605649742760987486 ) ) ;
#8192=CARTESIAN_POINT ( 'NONE',  ( 2.002547531651519996, 6.845637710436190737, 10.57595306287294612 ) ) ;
#8194=CARTESIAN_POINT ( 'NONE',  ( 16.58200780006414732, -0.0006320991582339893951, -0.01115192838421470191 ) ) ;
#8196=CARTESIAN_POINT ( 'NONE',  ( 3.950837973638677170, 1.958075594453790869, 14.41405733518061538 ) ) ;
#8197=FACE_OUTER_BOUND ( 'NONE', #7028, .T. ) ;
#8199=ORIENTED_EDGE ( 'NONE', *, *, #3890, .T. ) ;
#8201=B_SPLINE_CURVE_WITH_KNOTS ( 'NONE', 3,
 ( #13968, #5083, #18001, #10934 ),
 .UNSPECIFIED., .F., .F.,
 ( 4, 4 ),
 ( 1.514782153580211930E-17, 0.003005512676784846161 ),
 .UNSPECIFIED. ) ;
#8207=CARTESIAN_POINT ( 'NONE',  ( 3.512766787570810845, 10.40533104696146083, -10.87507422923874856 ) ) ;
#8209=CARTESIAN_POINT ( 'NONE',  ( 1.342453679581834924, 9.456403821038797730, 11.38190519890856933 ) ) ;
#8210=ORIENTED_EDGE ( 'NONE', *, *, #14686, .F. ) ;
#8211=CARTESIAN_POINT ( 'NONE',  ( 1.846822687350021974, 9.891732594446578375, 7.547953575784160485 ) ) ;
#8217=CARTESIAN_POINT ( 'NONE',  ( 0.3137051932979792457, 13.73004976592202198, 0.4596302728640249136 ) ) ;
#8220=CARTESIAN_POINT ( 'NONE',  ( 2.353870697619111496, -0.7635393531607235218, 12.92712089195302561 ) ) ;
#8222=B_SPLINE_CURVE_WITH_KNOTS ( 'NONE', 3,
 ( #7896, #15232, #328, #13505, #6157, #13411, #13315, #9305, #3170, #12269, #10744, #4822, #13706 ),
 .UNSPECIFIED., .F., .F.,
 ( 4, 3, 3, 3, 4 ),
 ( 8.673617379884034509E-19, 0.0002299780670421053329, 0.0004599561239687884940, 0.0006896788984287899067, 0.0009194956271626421231 ),
 .UNSPECIFIED. ) ;
#8224=ORIENTED_EDGE ( 'NONE', *, *, #15343, .T. ) ;
#8225=CARTESIAN_POINT ( 'NONE',  ( 16.58200780006414732, -0.01115192838421470017, 0.0006320991582340292937 ) ) ;
#8226=VERTEX_POINT ( 'NONE', #6016 ) ;
#8233=DIRECTION ( 'NONE',  ( 0.000000000000000000, 8.881784197001252323E-16, 1.000000000000000000 ) ) ;
#8243=FILL_AREA_STYLE_COLOUR ( '', #13014 ) ;
#8245=B_SPLINE_CURVE_WITH_KNOTS ( 'NONE', 3,
 ( #7496, #6153, #17622, #9117, #11981, #15984 ),
 .UNSPECIFIED., .F., .F.,
 ( 4, 2, 4 ),
 ( 2.017461075144244397E-18, 0.0002017457492448097769, 0.0004034914984896175480 ),
 .UNSPECIFIED. ) ;
#8267=CARTESIAN_POINT ( 'NONE',  ( 0.3720661004400037664, 0.7231997263366731765, -13.79610186261028559 ) ) ;
#8269=CARTESIAN_POINT ( 'NONE',  ( 1.847372867223029846, -3.744745203533896394, -11.86627781945711924 ) ) ;
#8270=CARTESIAN_POINT ( 'NONE',  ( 16.56753206892534891, -0.006669401563385243120, -0.006760771273035091553 ) ) ;
#8274=EDGE_CURVE ( 'NONE', #15252, #14131, #10994, .T. ) ;
#8277=EDGE_LOOP ( 'NONE', ( #6276, #3929, #2225, #11118, #10414, #1704 ) ) ;
#8278=CARTESIAN_POINT ( 'NONE',  ( 0.4384471787762840855, 12.93784327393180433, -4.978024343488911541 ) ) ;
#8280=CARTESIAN_POINT ( 'NONE',  ( 2.353870697619111940, 6.980654702310842730, 10.90705766126222187 ) ) ;
#8287=DIRECTION ( 'NONE',  ( 0.7635533937278216055, -0.3620487483322484823, -0.5347026451755951815 ) ) ;
#8288=ORIENTED_EDGE ( 'NONE', *, *, #15650, .T. ) ;
#8293=B_SPLINE_CURVE_WITH_KNOTS ( 'NONE', 3,
 ( #13897, #18115, #5015, #16592, #13719, #15244 ),
 .UNSPECIFIED., .F., .F.,
 ( 4, 2, 4 ),
 ( 8.673617379884035472E-19, 0.001500839035891551789, 0.003001678071783102711 ),
 .UNSPECIFIED. ) ;
#8299=ORIENTED_EDGE ( 'NONE', *, *, #7501, .T. ) ;
#8300=CARTESIAN_POINT ( 'NONE',  ( 16.56872352241294521, 0.01027347319884441834, -0.001821578298044677175 ) ) ;
#8306=CARTESIAN_POINT ( 'NONE',  ( 1.846524061778020531, 3.506196582971103926, 11.93805390544202361 ) ) ;
#8310=VERTEX_POINT ( 'NONE', #10509 ) ;
#8311=B_SPLINE_CURVE_WITH_KNOTS ( 'NONE', 3,
 ( #10258, #10351, #16090, #2974, #7400, #126 ),
 .UNSPECIFIED., .F., .F.,
 ( 4, 2, 4 ),
 ( 3.332294980281255979E-17, 0.0001825746017570583984, 0.0003651492035140835118 ),
 .UNSPECIFIED. ) ;
#8312=CARTESIAN_POINT ( 'NONE',  ( 0.3137051932979792457, 12.91601973349270871, 4.679953077377533965 ) ) ;
#8315=EDGE_CURVE ( 'NONE', #8587, #4376, #15775, .T. ) ;
#8316=EDGE_CURVE ( 'NONE', #7381, #14945, #8050, .T. ) ;
#8324=VERTEX_POINT ( 'NONE', #4873 ) ;
#8326=CARTESIAN_POINT ( 'NONE',  ( 2.002547531651519996, 7.942910686618313676, -9.778737580845612953 ) ) ;
#8333=CARTESIAN_POINT ( 'NONE',  ( 1.254009781012255020, 7.789615163754674221, -12.44229282923133262 ) ) ;
#8336=EDGE_LOOP ( 'NONE', ( #6248, #9207, #7434, #12132 ) ) ;
#8345=CARTESIAN_POINT ( 'NONE',  ( 0.3137051932979809665, 3.805684345189785933, 13.20008686438107581 ) ) ;
#8346=CARTESIAN_POINT ( 'NONE',  ( 16.56782317627811096, 0.008141063682853404496, 0.005492611183757338013 ) ) ;
#8347=CARTESIAN_POINT ( 'NONE',  ( 0.3132642857406501280, 11.41580579227788128, -7.641821025099742926 ) ) ;
#8355=CARTESIAN_POINT ( 'NONE',  ( 1.847168016377986000, -4.022276579849877187, -11.77471791462002670 ) ) ;
#8360=CARTESIAN_POINT ( 'NONE',  ( 1.861706995891668104, 6.878962591851903063, -10.38589138506418408 ) ) ;
#8361=VERTEX_POINT ( 'NONE', #4586 ) ;
#8368=ADVANCED_FACE ( 'NONE', ( #14802 ), #17270, .F. ) ;
#8372=LINE ( 'NONE', #13331, #5889 ) ;
#8373=VERTEX_POINT ( 'NONE', #10798 ) ;
#8374=ORIENTED_EDGE ( 'NONE', *, *, #10047, .F. ) ;
#8378=( BOUNDED_SURFACE ( )  B_SPLINE_SURFACE ( 3, 1, ( 
 ( #13837, #2446 ),
 ( #8026, #3897 ),
 ( #10987, #14028 ),
 ( #12406, #2104 ) ),
 .UNSPECIFIED., .F., .F., .T. ) 
 B_SPLINE_SURFACE_WITH_KNOTS ( ( 4, 4 ),
 ( 2, 2 ),
 ( 0.000000000000000000, 1.000000000000000000 ),
 ( 0.000000000000000000, 1.000000000000000000 ),
 .UNSPECIFIED. ) 
 GEOMETRIC_REPRESENTATION_ITEM ( )  RATIONAL_B_SPLINE_SURFACE ( (
 ( 1.000000000000000000, 1.000000000000000000),
 ( 0.7792777138730160313, 0.9689936506012927220),
 ( 0.7792777138730160313, 0.9689936506012927220),
 ( 1.000000000000000000, 1.000000000000000000) ) ) 
 REPRESENTATION_ITEM ( '' )  SURFACE ( )  );
#8387=EDGE_CURVE ( 'NONE', #9890, #421, #17369, .T. ) ;
#8388=CARTESIAN_POINT ( 'NONE',  ( 1.959212340397940899, -12.12975361829678178, 3.239239832448982170 ) ) ;
#8391=CARTESIAN_POINT ( 'NONE',  ( 1.977228804421385044, 15.04020501276069588, 3.321884655132254505 ) ) ;
#8392=EDGE_CURVE ( 'NONE', #8961, #8612, #12101, .T. ) ;
#8398=CONICAL_SURFACE ( 'NONE', #5043, 14.54644660717763927, 0.8559913436420816257 ) ;
#8407=CARTESIAN_POINT ( 'NONE',  ( 0.4862570985993235340, 10.79774104611385965, -8.769551628660616771 ) ) ;
#8408=ORIENTED_EDGE ( 'NONE', *, *, #6121, .T. ) ;
#8409=LINE ( 'NONE', #14417, #9303 ) ;
#8410=DIRECTION ( 'NONE',  ( 0.000000000000000000, 0.000000000000000000, 1.000000000000000000 ) ) ;
#8416=EDGE_CURVE ( 'NONE', #885, #3195, #6858, .T. ) ;
#8419=CARTESIAN_POINT ( 'NONE',  ( 1.342453679581834924, 3.649820028552730022, 14.34050741580208133 ) ) ;
#8421=CARTESIAN_POINT ( 'NONE',  ( 0.3137051932979792457, 0.4596302728641686874, -13.73004976592201487 ) ) ;
#8428=CARTESIAN_POINT ( 'NONE',  ( 0.3145734862173267810, 3.953068532979994831, 13.15783074029279831 ) ) ;
#8429=CARTESIAN_POINT ( 'NONE',  ( 1.846138399168762101, -9.815003036200465658, 7.646096044339859787 ) ) ;
#8432=CARTESIAN_POINT ( 'NONE',  ( 0.4862570985993235340, 12.97920246947886191, -5.003653737315353567 ) ) ;
#8440=CARTESIAN_POINT ( 'NONE',  ( 1.918921323896325193, -0.6349083173281016013, 12.49850046818174043 ) ) ;
#8446=CARTESIAN_POINT ( 'NONE',  ( 2.697797270744666687, -10.19107313879051269, -8.537712152180978009 ) ) ;
#8447=CARTESIAN_POINT ( 'NONE',  ( 16.56872352241294521, 0.001821578298043785094, -0.01027347319884367241 ) ) ;
#8448=ORIENTED_EDGE ( 'NONE', *, *, #2407, .T. ) ;
#8454=( GEOMETRIC_REPRESENTATION_CONTEXT ( 3 ) GLOBAL_UNCERTAINTY_ASSIGNED_CONTEXT ( ( #13228 ) ) GLOBAL_UNIT_ASSIGNED_CONTEXT ( ( #17202, #18446, #9835 ) ) REPRESENTATION_CONTEXT ( 'NONE', 'WORKASPACE' ) );
#8455=ORIENTED_EDGE ( 'NONE', *, *, #18860, .T. ) ;
#8459=( BOUNDED_SURFACE ( )  B_SPLINE_SURFACE ( 3, 1, ( 
 ( #11385, #16838 ),
 ( #11111, #11298 ),
 ( #2479, #8152 ),
 ( #6718, #12718 ) ),
 .UNSPECIFIED., .F., .F., .T. ) 
 B_SPLINE_SURFACE_WITH_KNOTS ( ( 4, 4 ),
 ( 2, 2 ),
 ( 0.000000000000000000, 1.000000000000000000 ),
 ( 0.000000000000000000, 1.000000000000000000 ),
 .UNSPECIFIED. ) 
 GEOMETRIC_REPRESENTATION_ITEM ( )  RATIONAL_B_SPLINE_SURFACE ( (
 ( 1.000000000000000000, 1.000000000000000000),
 ( 0.9593108457356467333, 0.9995965569486454649),
 ( 0.9593108457356467333, 0.9995965569486454649),
 ( 1.000000000000000000, 1.000000000000000000) ) ) 
 REPRESENTATION_ITEM ( '' )  SURFACE ( )  );
#8474=ORIENTED_EDGE ( 'NONE', *, *, #8544, .F. ) ;
#8475=ORIENTED_EDGE ( 'NONE', *, *, #11297, .T. ) ;
#8479=CARTESIAN_POINT ( 'NONE',  ( 0.3151928476913555821, 8.075547435847115096, -11.11539186930577827 ) ) ;
#8482=CARTESIAN_POINT ( 'NONE',  ( 0.3307726912345187453, 0.5948952607472642873, 13.74203354050372461 ) ) ;
#8491=FACE_OUTER_BOUND ( 'NONE', #17022, .T. ) ;
#8492=CARTESIAN_POINT ( 'NONE',  ( 0.4862570985993235340, -5.003653737315397976, -12.97920246947884770 ) ) ;
#8496=ORIENTED_EDGE ( 'NONE', *, *, #7743, .T. ) ;
#8498=DIRECTION ( 'NONE',  ( 0.000000000000000000, 0.000000000000000000, 1.000000000000000000 ) ) ;
#8502=CARTESIAN_POINT ( 'NONE',  ( 1.562796894703937678, 0.000000000000000000, 0.000000000000000000 ) ) ;
#8503=CARTESIAN_POINT ( 'NONE',  ( 0.4754618798421162973, 7.564402563418637371, -11.68486377711958468 ) ) ;
#8505=ORIENTED_EDGE ( 'NONE', *, *, #8895, .F. ) ;
#8507=EDGE_CURVE ( 'NONE', #617, #10695, #6962, .T. ) ;
#8510=LINE ( 'NONE', #5530, #3535 ) ;
#8514=VECTOR ( 'NONE', #6912, 999.9999999999998863 ) ;
#8518=CARTESIAN_POINT ( 'NONE',  ( 3.353306896162455697, -5.573563251762193360, 12.78841260990236428 ) ) ;
#8529=CARTESIAN_POINT ( 'NONE',  ( 2.636624412714236865, 0.000000000000000000, 0.000000000000000000 ) ) ;
#8535=CARTESIAN_POINT ( 'NONE',  ( 2.002547531651519996, -0.6781519942172617998, 12.57989064830759318 ) ) ;
#8537=CARTESIAN_POINT ( 'NONE',  ( 16.57210152137263393, -0.01136813053532154116, 0.009075239946109162070 ) ) ;
#8544=EDGE_CURVE ( 'NONE', #15569, #5801, #8140, .T. ) ;
#8551=CARTESIAN_POINT ( 'NONE',  ( 0.3145729642390390768, 12.96842777670212676, -4.535980493004950986 ) ) ;
#8555=CARTESIAN_POINT ( 'NONE',  ( 0.3137051932979792457, -13.73004976592202375, 0.4596302728639276580 ) ) ;
#8556=CARTESIAN_POINT ( 'NONE',  ( 16.57778382496167424, -0.01466529584256786797, -0.002851818597093949692 ) ) ;
#8557=CARTESIAN_POINT ( 'NONE',  ( 0.3148213771069329203, -13.13560149728604109, 4.026433757158931925 ) ) ;
#8563=VERTEX_POINT ( 'NONE', #4274 ) ;
#8564=( BOUNDED_SURFACE ( )  B_SPLINE_SURFACE ( 3, 1, ( 
 ( #9996, #17356 ),
 ( #18788, #15829 ),
 ( #11822, #16014 ),
 ( #16216, #11627 ) ),
 .UNSPECIFIED., .F., .F., .T. ) 
 B_SPLINE_SURFACE_WITH_KNOTS ( ( 4, 4 ),
 ( 2, 2 ),
 ( 0.000000000000000000, 1.000000000000000000 ),
 ( 0.000000000000000000, 1.000000000000000000 ),
 .UNSPECIFIED. ) 
 GEOMETRIC_REPRESENTATION_ITEM ( )  RATIONAL_B_SPLINE_SURFACE ( (
 ( 1.000000000000000000, 1.000000000000000000),
 ( 0.9593108457356467333, 0.9995965569486454649),
 ( 0.9593108457356467333, 0.9995965569486454649),
 ( 1.000000000000000000, 1.000000000000000000) ) ) 
 REPRESENTATION_ITEM ( '' )  SURFACE ( )  );
#8567=CARTESIAN_POINT ( 'NONE',  ( 1.861706995891673433, -0.5394761475744983548, -12.44571539481144562 ) ) ;
#8568=CARTESIAN_POINT ( 'NONE',  ( 0.3137051932979757485, 7.698472063774634222, -11.37800749014122736 ) ) ;
#8569=ORIENTED_EDGE ( 'NONE', *, *, #7259, .F. ) ;
#8570=CARTESIAN_POINT ( 'NONE',  ( 0.4862570985993252548, 5.003653737315486794, 12.97920246947881395 ) ) ;
#8572=CIRCLE ( 'NONE', #6038, 14.54644660717763927 ) ;
#8577=CARTESIAN_POINT ( 'NONE',  ( 16.58200780006414732, 0.002844973367391037070, 0.01080144354108989249 ) ) ;
#8579=DIRECTION ( 'NONE',  ( 0.000000000000000000, 0.000000000000000000, 1.000000000000000000 ) ) ;
#8582=FACE_OUTER_BOUND ( 'NONE', #14177, .T. ) ;
#8587=VERTEX_POINT ( 'NONE', #10289 ) ;
#8589=EDGE_CURVE ( 'NONE', #15501, #1561, #4181, .T. ) ;
#8592=CARTESIAN_POINT ( 'NONE',  ( 16.56822296793089322, -0.009847136207495329335, 0.002414375228568802195 ) ) ;
#8596=LINE ( 'NONE', #9929, #1022 ) ;
#8597=CARTESIAN_POINT ( 'NONE',  ( 1.847380140988738262, 12.44273713935591097, -0.1101766933249076624 ) ) ;
#8599=EDGE_CURVE ( 'NONE', #14131, #14913, #2964, .T. ) ;
#8602=EDGE_CURVE ( 'NONE', #9114, #3538, #16187, .T. ) ;
#8607=CARTESIAN_POINT ( 'NONE',  ( 3.074695600507274307, 11.23985886659449029, -10.75417554975685341 ) ) ;
#8608=CARTESIAN_POINT ( 'NONE',  ( 1.959212340397939123, 6.829000156128186561, 10.53510106265284563 ) ) ;
#8611=CARTESIAN_POINT ( 'NONE',  ( 0.3148208552358935930, -13.13564827777586785, -4.026279359288564841 ) ) ;
#8612=VERTEX_POINT ( 'NONE', #18687 ) ;
#8616=CARTESIAN_POINT ( 'NONE',  ( 0.3095370825347234511, 7.700448427571873644, 11.38092634279631277 ) ) ;
#8618=CARTESIAN_POINT ( 'NONE',  ( 0.3151926232592506816, -4.172630140040890723, 13.09050869763091107 ) ) ;
#8619=CARTESIAN_POINT ( 'NONE',  ( 0.4862570985993235340, 11.67702470553376060, -7.559321496869298329 ) ) ;
#8625=CARTESIAN_POINT ( 'NONE',  ( 2.353870697619111940, -12.53036919722786813, 3.268530966681581607 ) ) ;
#8632=CARTESIAN_POINT ( 'NONE',  ( 2.002547531651519996, 6.845637710436341727, -10.57595306287284842 ) ) ;
#8639=CARTESIAN_POINT ( 'NONE',  ( 2.002547531651521773, 9.778737580845699995, 7.942910686618207983 ) ) ;
#8641=CARTESIAN_POINT ( 'NONE',  ( 0.3142011359265323156, -7.762194356530850214, 11.33549115679420538 ) ) ;
#8643=EDGE_CURVE ( 'NONE', #348, #8116, #12994, .T. ) ;
#8647=CARTESIAN_POINT ( 'NONE',  ( 1.845756295923359769, 10.33914852636104875, 6.920504327368230513 ) ) ;
#8648=CARTESIAN_POINT ( 'NONE',  ( 0.3150686449036028680, -13.01866258978840030, 4.391272911157273029 ) ) ;
#8650=CIRCLE ( 'NONE', #3142, 12.15840553252917289 ) ;
#8655=ORIENTED_EDGE ( 'NONE', *, *, #14180, .T. ) ;
#8666=CARTESIAN_POINT ( 'NONE',  ( 1.918921323896323194, 12.08297777410669482, -3.258415356426395793 ) ) ;
#8667=CARTESIAN_POINT ( 'NONE',  ( 1.846955891736119293, 4.094751675596701723, 11.74973605926565767 ) ) ;
#8670=B_SPLINE_CURVE_WITH_KNOTS ( 'NONE', 3,
 ( #14664, #7323, #1577, #9035, #14472, #4640 ),
 .UNSPECIFIED., .F., .F.,
 ( 4, 2, 4 ),
 ( 0.000000000000000000, 0.001656992708822505175, 0.003313985417645010350 ),
 .UNSPECIFIED. ) ;
#8674=( BOUNDED_SURFACE ( )  B_SPLINE_SURFACE ( 3, 1, ( 
 ( #787, #9295 ),
 ( #878, #6625 ),
 ( #697, #18275 ),
 ( #15400, #15129 ) ),
 .UNSPECIFIED., .F., .F., .T. ) 
 B_SPLINE_SURFACE_WITH_KNOTS ( ( 4, 4 ),
 ( 2, 2 ),
 ( 0.000000000000000000, 1.000000000000000000 ),
 ( 0.000000000000000000, 1.000000000000000000 ),
 .UNSPECIFIED. ) 
 GEOMETRIC_REPRESENTATION_ITEM ( )  RATIONAL_B_SPLINE_SURFACE ( (
 ( 1.000000000000000000, 1.000000000000000000),
 ( 0.9933953342250438912, 0.8357391271907739227),
 ( 0.9933953342250438912, 0.8357391271907739227),
 ( 1.000000000000000000, 1.000000000000000000) ) ) 
 REPRESENTATION_ITEM ( '' )  SURFACE ( )  );
#8675=ORIENTED_EDGE ( 'NONE', *, *, #18654, .T. ) ;
#8676=ORIENTED_EDGE ( 'NONE', *, *, #17028, .F. ) ;
#8677=ORIENTED_EDGE ( 'NONE', *, *, #12308, .F. ) ;
#8678=CARTESIAN_POINT ( 'NONE',  ( 0.3720661004400037664, 13.79610186261029625, 0.7231997263365286255 ) ) ;
#8680=CIRCLE ( 'NONE', #18166, 5.000000000000000000 ) ;
#8697=LINE ( 'NONE', #18827, #15973 ) ;
#8701=LINE ( 'NONE', #10422, #11203 ) ;
#8702=EDGE_LOOP ( 'NONE', ( #2768, #11372, #17647, #18808 ) ) ;
#8707=FACE_OUTER_BOUND ( 'NONE', #10265, .T. ) ;
#8708=CONICAL_SURFACE ( 'NONE', #2889, 14.54644660717763927, 0.8559913436420816257 ) ;
#8711=B_SPLINE_CURVE_WITH_KNOTS ( 'NONE', 3,
 ( #11274, #18698, #17090, #11450, #6782, #14400 ),
 .UNSPECIFIED., .F., .F.,
 ( 4, 2, 4 ),
 ( 0.000000000000000000, 0.0001828790815886944003, 0.0003657581631773888006 ),
 .UNSPECIFIED. ) ;
#8714=FACE_OUTER_BOUND ( 'NONE', #8336, .T. ) ;
#8716=CARTESIAN_POINT ( 'NONE',  ( 0.3137051932979809665, -4.679953077377580151, 12.91601973349268917 ) ) ;
#8717=CARTESIAN_POINT ( 'NONE',  ( 0.3150692679895978898, -11.20465057551030874, 7.951395415075045214 ) ) ;
#8719=CARTESIAN_POINT ( 'NONE',  ( 16.56679352167444819, 0.004162264567719650525, 0.008311568981097349276 ) ) ;
#8726=ORIENTED_EDGE ( 'NONE', *, *, #4981, .T. ) ;
#8727=CARTESIAN_POINT ( 'NONE',  ( 3.950837973638675393, -10.51028938476210328, -10.05648675950137871 ) ) ;
#8728=CARTESIAN_POINT ( 'NONE',  ( 3.377929128793385249, 13.64476897106782971, 3.070552481924919253 ) ) ;
#8732=ORIENTED_EDGE ( 'NONE', *, *, #2351, .F. ) ;
#8734=ORIENTED_EDGE ( 'NONE', *, *, #428, .F. ) ;
#8738=CARTESIAN_POINT ( 'NONE',  ( 1.847247051441596621, -7.448813758297236909, 9.967131402978164800 ) ) ;
#8742=ADVANCED_FACE ( 'NONE', ( #3102 ), #11261, .F. ) ;
#8743=B_SPLINE_CURVE_WITH_KNOTS ( 'NONE', 3,
 ( #4404, #13003, #12816, #7382, #13192, #9185 ),
 .UNSPECIFIED., .F., .F.,
 ( 4, 2, 4 ),
 ( 2.185279341460844539E-18, 0.0002017457492448067953, 0.0004034914984896113680 ),
 .UNSPECIFIED. ) ;
#8752=ORIENTED_EDGE ( 'NONE', *, *, #10473, .F. ) ;
#8757=ORIENTED_EDGE ( 'NONE', *, *, #13691, .F. ) ;
#8762=CIRCLE ( 'NONE', #7875, 16.06066017081991149 ) ;
#8764=B_SPLINE_CURVE_WITH_KNOTS ( 'NONE', 3,
 ( #13356, #6100, #16130, #3012 ),
 .UNSPECIFIED., .F., .F.,
 ( 4, 4 ),
 ( 0.000000000000000000, 0.002004993803842603211 ),
 .UNSPECIFIED. ) ;
#8767=CARTESIAN_POINT ( 'NONE',  ( 1.254009781011409919, 5.487405433548389055, 13.61532727684416955 ) ) ;
#8773=DIRECTION ( 'NONE',  ( 0.7071067818211358436, 8.659560554583467185E-17, 0.7071067805519591909 ) ) ;
#8775=CARTESIAN_POINT ( 'NONE',  ( 2.320521194582657376, -3.126729093671833937, 15.43440938317077915 ) ) ;
#8777=ORIENTED_EDGE ( 'NONE', *, *, #1372, .T. ) ;
#8778=ORIENTED_EDGE ( 'NONE', *, *, #10675, .T. ) ;
#8779=ORIENTED_EDGE ( 'NONE', *, *, #1423, .T. ) ;
#8787=CARTESIAN_POINT ( 'NONE',  ( 3.950837973638668288, 0.000000000000000000, 0.000000000000000000 ) ) ;
#8788=CARTESIAN_POINT ( 'NONE',  ( 1.959283090834841090, -12.12982544407802799, -3.239245055717093091 ) ) ;
#8791=AXIS2_PLACEMENT_3D ( 'NONE', #12465, #6919, #16861 ) ;
#8792=CARTESIAN_POINT ( 'NONE',  ( 3.950837973638675393, 10.51028938476217967, 10.05648675950130233 ) ) ;
#8794=CARTESIAN_POINT ( 'NONE',  ( 0.3137051932979792457, 4.679953077377670745, -12.91601973349265720 ) ) ;
#8795=CARTESIAN_POINT ( 'NONE',  ( 2.002547531651519996, 11.75462648437108015, -4.532360870844206246 ) ) ;
#8797=ORIENTED_EDGE ( 'NONE', *, *, #2290, .T. ) ;
#8800=ORIENTED_EDGE ( 'NONE', *, *, #18240, .F. ) ;
#8801=CARTESIAN_POINT ( 'NONE',  ( 1.959283090834842644, 12.12982544407805108, 3.239245055717007826 ) ) ;
#8807=CARTESIAN_POINT ( 'NONE',  ( 0.3170788640506441158, 13.11595226728158003, 4.100430649998006771 ) ) ;
#8808=CARTESIAN_POINT ( 'NONE',  ( 3.950837973638675393, -6.888253895133384930, 12.81214529934972823 ) ) ;
#8810=CARTESIAN_POINT ( 'NONE',  ( 1.846138399168762101, 4.238866729160568170, -11.69739621335917690 ) ) ;
#8811=CARTESIAN_POINT ( 'NONE',  ( 0.3132642857406524040, 3.740125687984731773, 13.21852905223340535 ) ) ;
#8815=CARTESIAN_POINT ( 'NONE',  ( 0.3058872367615226295, 13.24582953854930345, -3.664492643742625511 ) ) ;
#8816=CARTESIAN_POINT ( 'NONE',  ( 0.4384471787762801442, 10.76632603192799742, -8.732395932355569101 ) ) ;
#8818=CARTESIAN_POINT ( 'NONE',  ( 3.353306896162454809, 12.02594772223106645, -7.069984850384678055 ) ) ;
#8822=CARTESIAN_POINT ( 'NONE',  ( 3.950837973638675393, 6.888253895133292559, 12.81214529934977797 ) ) ;
#8824=ORIENTED_EDGE ( 'NONE', *, *, #3042, .F. ) ;
#8826=ORIENTED_EDGE ( 'NONE', *, *, #6019, .F. ) ;
#8833=EDGE_CURVE ( 'NONE', #6154, #9401, #18484, .T. ) ;
#8835=CARTESIAN_POINT ( 'NONE',  ( 1.846822687350024417, -7.547953575784189795, 9.891732594446548177 ) ) ;
#8839=CARTESIAN_POINT ( 'NONE',  ( 1.918918678667045352, 9.738328798462491775, -7.860057224348732774 ) ) ;
#8841=CARTESIAN_POINT ( 'NONE',  ( 1.342453679581834924, -14.76648944001040142, 0.9602753779830212055 ) ) ;
#8847=CARTESIAN_POINT ( 'NONE',  ( 0.4754618798421162973, 0.7484603771384427118, 13.89949764182683012 ) ) ;
#8848=EDGE_LOOP ( 'NONE', ( #4914, #10747, #1802, #7893 ) ) ;
#8849=ORIENTED_EDGE ( 'NONE', *, *, #16965, .F. ) ;
#8850=ORIENTED_EDGE ( 'NONE', *, *, #10375, .F. ) ;
#8853=LINE ( 'NONE', #1588, #18462 ) ;
#8854=CARTESIAN_POINT ( 'NONE',  ( 1.977436885025011470, 11.52792723756289206, 10.21547824869447219 ) ) ;
#8857=CARTESIAN_POINT ( 'NONE',  ( 0.3132635586635977853, -11.41586812343484070, -7.641727604904016147 ) ) ;
#8858=CARTESIAN_POINT ( 'NONE',  ( 2.320520222538116961, 10.64885284335071169, -11.60169517779341852 ) ) ;
#8863=CARTESIAN_POINT ( 'NONE',  ( 0.4862570985993252548, -12.97920246947875889, -5.003653737315625349 ) ) ;
#8864=B_SPLINE_CURVE_WITH_KNOTS ( 'NONE', 3,
 ( #6347, #15028, #5629, #2480, #8608, #15869 ),
 .UNSPECIFIED., .F., .F.,
 ( 4, 2, 4 ),
 ( 0.000000000000000000, 0.0001828790815886947255, 0.0003657581631773894511 ),
 .UNSPECIFIED. ) ;
#8865=CARTESIAN_POINT ( 'NONE',  ( 1.846955891736116184, 7.525208385419960067, 9.909315188408065467 ) ) ;
#8868=ORIENTED_EDGE ( 'NONE', *, *, #16502, .T. ) ;
#8871=CARTESIAN_POINT ( 'NONE',  ( 2.747332970342022840, 7.289199830147313541, -14.63517873738939379 ) ) ;
#8872=ORIENTED_EDGE ( 'NONE', *, *, #10675, .F. ) ;
#8876=CARTESIAN_POINT ( 'NONE',  ( 1.846138399168762101, -11.95493567637848109, -3.446241763653124401 ) ) ;
#8879=CARTESIAN_POINT ( 'NONE',  ( 0.3142011359265305392, -4.608101617236689762, -12.94258167753017297 ) ) ;
#8880=CARTESIAN_POINT ( 'NONE',  ( 16.57210152137263393, 0.01361613799508855013, 0.005118120558001428358 ) ) ;
#8884=EDGE_CURVE ( 'NONE', #15501, #10168, #6173, .T. ) ;
#8886=VERTEX_POINT ( 'NONE', #18669 ) ;
#8887=CARTESIAN_POINT ( 'NONE',  ( 3.074695600507311610, 2.772091048739249164, 15.30693405987785916 ) ) ;
#8890=CARTESIAN_POINT ( 'NONE',  ( 16.56753206892534891, 0.004368917149005333185, 0.008432171035096464387 ) ) ;
#8892=VERTEX_POINT ( 'NONE', #2703 ) ;
#8895=EDGE_CURVE ( 'NONE', #12474, #11305, #13236, .T. ) ;
#8897=CARTESIAN_POINT ( 'NONE',  ( 16.56753206892534891, -0.006669401563385243120, -0.006760771273035091553 ) ) ;
#8901=ORIENTED_EDGE ( 'NONE', *, *, #546, .T. ) ;
#8904=CARTESIAN_POINT ( 'NONE',  ( 3.950837973638675393, -14.31366178983251380, -2.591948120961955926 ) ) ;
#8905=CARTESIAN_POINT ( 'NONE',  ( 3.950837973638677170, -14.31366178983255466, 2.591948120961746760 ) ) ;
#8908=CARTESIAN_POINT ( 'NONE',  ( 2.123976203522053741, 1.531817366691752502, 15.54801196254787676 ) ) ;
#8913=FACE_OUTER_BOUND ( 'NONE', #16164, .T. ) ;
#8922=CARTESIAN_POINT ( 'NONE',  ( 1.847247051441589960, 10.16425585218611083, -7.177495230324590025 ) ) ;
#8930=CARTESIAN_POINT ( 'NONE',  ( 3.950837973638675393, -10.05648675950118509, -10.51028938476228980 ) ) ;
#8934=CARTESIAN_POINT ( 'NONE',  ( 0.3095370825347234511, -0.4597470195091165057, 13.73357284481724605 ) ) ;
#8937=VERTEX_POINT ( 'NONE', #8639 ) ;
#8946=ORIENTED_EDGE ( 'NONE', *, *, #1979, .F. ) ;
#8953=CARTESIAN_POINT ( 'NONE',  ( 0.8740779401510758717, -0.8420120399581221271, -14.27348745891595172 ) ) ;
#8956=CARTESIAN_POINT ( 'NONE',  ( 1.847034903785823579, 11.90269060117939048, -3.625649561595184700 ) ) ;
#8960=VERTEX_POINT ( 'NONE', #1279 ) ;
#8961=VERTEX_POINT ( 'NONE', #15708 ) ;
#8962=ORIENTED_EDGE ( 'NONE', *, *, #3412, .F. ) ;
#8963=EDGE_LOOP ( 'NONE', ( #10870, #6484, #7839, #10014 ) ) ;
#8964=CARTESIAN_POINT ( 'NONE',  ( 0.4754618798421167414, 5.007009103465430044, -12.98792082933639058 ) ) ;
#8971=CARTESIAN_POINT ( 'NONE',  ( 2.320521194583479829, -10.64885423995220393, -11.60169518685964363 ) ) ;
#8977=CARTESIAN_POINT ( 'NONE',  ( 2.123976203522053741, -7.899625852120303549, 13.47898556379310087 ) ) ;
#8980=CARTESIAN_POINT ( 'NONE',  ( 0.3151926232592501265, 13.09050869763092884, 4.172630140040843649 ) ) ;
#8982=CARTESIAN_POINT ( 'NONE',  ( 1.846138399168762101, 7.646096044339892650, 9.815003036200437236 ) ) ;
#8983=ORIENTED_EDGE ( 'NONE', *, *, #8884, .F. ) ;
#8985=CARTESIAN_POINT ( 'NONE',  ( 2.636624412715137478, -2.862162146983530775, 15.80357026013314048 ) ) ;
#8990=B_SPLINE_CURVE_WITH_KNOTS ( 'NONE', 3,
 ( #16168, #3052, #2124, #3547, #16466, #12063 ),
 .UNSPECIFIED., .F., .F.,
 ( 4, 2, 4 ),
 ( 0.000000000000000000, 0.001500839035891550705, 0.003001678071783101410 ),
 .UNSPECIFIED. ) ;
#8992=CARTESIAN_POINT ( 'NONE',  ( 2.002547531651519996, -6.845637710436264456, 10.57595306287289638 ) ) ;
#8997=ORIENTED_EDGE ( 'NONE', *, *, #14048, .F. ) ;
#9000=CARTESIAN_POINT ( 'NONE',  ( 0.3148208552358917611, 13.73693263646118723, -0.2299193288887949882 ) ) ;
#9005=CIRCLE ( 'NONE', #16340, 16.06066017081991149 ) ;
#9008=CARTESIAN_POINT ( 'NONE',  ( 2.636624412715435462, -15.80357026013316712, -2.862162146983298516 ) ) ;
#9010=CARTESIAN_POINT ( 'NONE',  ( 16.56822296793089322, -0.003834730849370904075, 0.009385634690641608477 ) ) ;
#9015=DIRECTION ( 'NONE',  ( -1.000000000000000000, -0.000000000000000000, -0.000000000000000000 ) ) ;
#9019=VERTEX_POINT ( 'NONE', #14188 ) ;
#9020=CARTESIAN_POINT ( 'NONE',  ( 3.512766787570793969, 2.025881399556391127, 14.91422000116820179 ) ) ;
#9022=CARTESIAN_POINT ( 'NONE',  ( 3.512766787570692273, -2.682019731918297012, -14.81029789862167867 ) ) ;
#9023=ORIENTED_EDGE ( 'NONE', *, *, #18552, .F. ) ;
#9025=EDGE_CURVE ( 'NONE', #15958, #6394, #12754, .T. ) ;
#9027=CARTESIAN_POINT ( 'NONE',  ( 2.636624412714237309, 7.605649742761960042, 14.14563173255213613 ) ) ;
#9028=CARTESIAN_POINT ( 'NONE',  ( 0.3150692679895994996, -13.73846569174796883, -0.1531143455845980217 ) ) ;
#9029=CARTESIAN_POINT ( 'NONE',  ( 0.3170788640506440603, -0.1533108587037102788, 13.74111462631963576 ) ) ;
#9031=CIRCLE ( 'NONE', #11164, 16.06066017081991149 ) ;
#9035=CARTESIAN_POINT ( 'NONE',  ( 1.254255976357524505, -1.011593778944422262, 14.64488542023450535 ) ) ;
#9043=ORIENTED_EDGE ( 'NONE', *, *, #16867, .F. ) ;
#9047=FACE_OUTER_BOUND ( 'NONE', #9994, .T. ) ;
#9050=CARTESIAN_POINT ( 'NONE',  ( 0.3307726912345205217, -11.46720933246392882, -7.596084275799019458 ) ) ;
#9055=AXIS2_PLACEMENT_3D ( 'NONE', #12006, #5604, #9137 ) ;
#9057=CARTESIAN_POINT ( 'NONE',  ( 0.000000000000000000, 1.805416924949539152E-15, 13.42403576283810906 ) ) ;
#9058=CARTESIAN_POINT ( 'NONE',  ( 0.3151926232592488497, -11.16039997398647365, -8.013596737356504462 ) ) ;
#9060=CARTESIAN_POINT ( 'NONE',  ( 0.3151928476913556376, 4.245457024760402653, -13.06684726503522320 ) ) ;
#9062=EDGE_LOOP ( 'NONE', ( #3297, #18098, #11692, #1246 ) ) ;
#9063=VERTEX_POINT ( 'NONE', #9878 ) ;
#9064=VERTEX_POINT ( 'NONE', #2612 ) ;
#9066=VERTEX_POINT ( 'NONE', #17243 ) ;
#9067=LINE ( 'NONE', #2005, #4343 ) ;
#9072=CARTESIAN_POINT ( 'NONE',  ( 3.950837973638676281, -10.05648675950133963, 10.51028938476214059 ) ) ;
#9073=EDGE_CURVE ( 'NONE', #415, #209, #4159, .T. ) ;
#9074=CARTESIAN_POINT ( 'NONE',  ( 3.074695600507584281, 13.70113613813179043, -7.366518011945612621 ) ) ;
#9081=( BOUNDED_SURFACE ( )  B_SPLINE_SURFACE ( 3, 1, ( 
 ( #3186, #248 ),
 ( #13140, #5771 ),
 ( #17447, #11710 ),
 ( #149, #1673 ) ),
 .UNSPECIFIED., .F., .F., .T. ) 
 B_SPLINE_SURFACE_WITH_KNOTS ( ( 4, 4 ),
 ( 2, 2 ),
 ( 0.000000000000000000, 1.000000000000000000 ),
 ( 0.000000000000000000, 1.000000000000000000 ),
 .UNSPECIFIED. ) 
 GEOMETRIC_REPRESENTATION_ITEM ( )  RATIONAL_B_SPLINE_SURFACE ( (
 ( 1.000000000000000000, 1.000000000000000000),
 ( 0.7792777138730158093, 0.9689936506012928330),
 ( 0.7792777138730158093, 0.9689936506012928330),
 ( 1.000000000000000000, 1.000000000000000000) ) ) 
 REPRESENTATION_ITEM ( '' )  SURFACE ( )  );
#9082=CARTESIAN_POINT ( 'NONE',  ( 0.4862570985993252548, 3.580942890621670482, 13.44146924561382583 ) ) ;
#9083=CARTESIAN_POINT ( 'NONE',  ( 8.522092701127531811, -6.946128462138598358, 0.3779863304870977325 ) ) ;
#9084=CARTESIAN_POINT ( 'NONE',  ( 0.3095370825347224519, -4.681152801286072140, -12.91933430393612703 ) ) ;
#9088=ORIENTED_EDGE ( 'NONE', *, *, #17310, .T. ) ;
#9091=ADVANCED_FACE ( 'NONE', ( #7706 ), #7980, .F. ) ;
#9093=VECTOR ( 'NONE', #11157, 1000.000000000000227 ) ;
#9094=ORIENTED_EDGE ( 'NONE', *, *, #10451, .F. ) ;
#9097=ORIENTED_EDGE ( 'NONE', *, *, #7745, .T. ) ;
#9100=DIRECTION ( 'NONE',  ( -1.000000000000000000, 0.000000000000000000, 0.000000000000000000 ) ) ;
#9101=CARTESIAN_POINT ( 'NONE',  ( 0.8740764193768466583, -11.05257066464528748, -9.070946295054149289 ) ) ;
#9111=B_SPLINE_CURVE_WITH_KNOTS ( 'NONE', 3,
 ( #11942, #3125, #3325, #10316, #8971, #14801 ),
 .UNSPECIFIED., .F., .F.,
 ( 4, 2, 4 ),
 ( 4.878909776184769953E-19, 0.001657017934711441055, 0.003314035869422881676 ),
 .UNSPECIFIED. ) ;
#9114=VERTEX_POINT ( 'NONE', #4542 ) ;
#9115=CARTESIAN_POINT ( 'NONE',  ( 0.3137051932979757485, 12.91601973349276733, -4.679953077377353665 ) ) ;
#9116=( BOUNDED_SURFACE ( )  B_SPLINE_SURFACE ( 3, 1, ( 
 ( #12455, #16946 ),
 ( #11033, #16849 ),
 ( #9581, #15413 ),
 ( #2320, #8167 ) ),
 .UNSPECIFIED., .F., .F., .T. ) 
 B_SPLINE_SURFACE_WITH_KNOTS ( ( 4, 4 ),
 ( 2, 2 ),
 ( 0.000000000000000000, 1.000000000000000000 ),
 ( 0.000000000000000000, 1.000000000000000000 ),
 .UNSPECIFIED. ) 
 GEOMETRIC_REPRESENTATION_ITEM ( )  RATIONAL_B_SPLINE_SURFACE ( (
 ( 1.000000000000000000, 1.000000000000000000),
 ( 0.7792777138730158093, 0.9689936506012928330),
 ( 0.7792777138730158093, 0.9689936506012928330),
 ( 1.000000000000000000, 1.000000000000000000) ) ) 
 REPRESENTATION_ITEM ( '' )  SURFACE ( )  );
#9117=CARTESIAN_POINT ( 'NONE',  ( 0.3939875929385656117, -13.80036004410495210, 0.7003304234512695015 ) ) ;
#9120=CARTESIAN_POINT ( 'NONE',  ( 0.4862570985993235340, -8.769551628660812170, 10.79774104611370333 ) ) ;
#9127=CARTESIAN_POINT ( 'NONE',  ( 16.57605080000000086, 6.799999999999999822, 1.500000000000000000 ) ) ;
#9128=CARTESIAN_POINT ( 'NONE',  ( 3.950837973638668288, 0.000000000000000000, 0.000000000000000000 ) ) ;
#9131=DIRECTION ( 'NONE',  ( 0.7561779333270775005, 0.5081796452863215352, 0.4122479608995760492 ) ) ;
#9134=EDGE_CURVE ( 'NONE', #8612, #17983, #4100, .T. ) ;
#9136=CARTESIAN_POINT ( 'NONE',  ( 1.846613052777650310, -11.93415846513959444, -3.520031056876430142 ) ) ;
#9137=DIRECTION ( 'NONE',  ( 0.000000000000000000, 0.000000000000000000, 1.000000000000000000 ) ) ;
#9141=VERTEX_POINT ( 'NONE', #16397 ) ;
#9145=DIRECTION ( 'NONE',  ( 0.000000000000000000, 0.000000000000000000, -1.000000000000000000 ) ) ;
#9147=CARTESIAN_POINT ( 'NONE',  ( 16.56753206892534891, 0.008490833999798923920, 0.004253784598196209618 ) ) ;
#9151=CARTESIAN_POINT ( 'NONE',  ( 0.3148213771069364175, 7.888490156175222090, 11.24846294176314387 ) ) ;
#9152=CARTESIAN_POINT ( 'NONE',  ( 1.846613052777651420, 11.72395935470504291, -4.166957398589727468 ) ) ;
#9156=CARTESIAN_POINT ( 'NONE',  ( 0.3150686449036048109, 4.099563462784836965, -13.11344473514184372 ) ) ;
#9160=ORIENTED_EDGE ( 'NONE', *, *, #8507, .T. ) ;
#9163=CARTESIAN_POINT ( 'NONE',  ( 3.512766787570702043, -7.127386085302744867, -13.25664064834487021 ) ) ;
#9167=CARTESIAN_POINT ( 'NONE',  ( 1.254009781011571567, 1.011465182608068503, 14.64464726212582590 ) ) ;
#9168=ORIENTED_EDGE ( 'NONE', *, *, #8643, .T. ) ;
#9171=CARTESIAN_POINT ( 'NONE',  ( 0.3720661004400037664, -3.575426119359092159, -13.34435358167256247 ) ) ;
#9174=CARTESIAN_POINT ( 'NONE',  ( 3.950837973638676281, 10.05648675950141602, -10.51028938476206953 ) ) ;
#9175=CARTESIAN_POINT ( 'NONE',  ( 1.845756295923360657, -6.920504327368265152, 10.33914852636102033 ) ) ;
#9177=ORIENTED_EDGE ( 'NONE', *, *, #17597, .F. ) ;
#9179=CARTESIAN_POINT ( 'NONE',  ( 16.56679352167444819, -0.006526964904753006572, -0.006618561353599182288 ) ) ;
#9185=CARTESIAN_POINT ( 'NONE',  ( 0.4862570985993235340, -0.7479633556561480212, -13.89016912371018186 ) ) ;
#9191=CARTESIAN_POINT ( 'NONE',  ( 0.3137051932979792457, -10.83767969834796929, -8.442169467526971616 ) ) ;
#9193=CARTESIAN_POINT ( 'NONE',  ( 0.3137051932979809665, 3.805684345189785933, 13.20008686438107581 ) ) ;
#9194=B_SPLINE_CURVE_WITH_KNOTS ( 'NONE', 3,
 ( #16633, #588, #9637, #15467, #9466, #2198 ),
 .UNSPECIFIED., .F., .F.,
 ( 4, 2, 4 ),
 ( 0.000000000000000000, 0.001656992708824380845, 0.003313985417648761689 ),
 .UNSPECIFIED. ) ;
#9200=CARTESIAN_POINT ( 'NONE',  ( 16.56753206892534891, 0.001421777558675947238, -0.009389754735542250527 ) ) ;
#9203=VERTEX_POINT ( 'NONE', #18106 ) ;
#9205=CARTESIAN_POINT ( 'NONE',  ( 2.002547531651519996, 11.75462648437108015, -4.532360870844206246 ) ) ;
#9207=ORIENTED_EDGE ( 'NONE', *, *, #13647, .F. ) ;
#9208=AXIS2_PLACEMENT_3D ( 'NONE', #13869, #18000, #10644 ) ;
#9211=CARTESIAN_POINT ( 'NONE',  ( 3.074695600508143833, 13.70113613813285269, 7.366518011945069055 ) ) ;
#9212=VERTEX_POINT ( 'NONE', #4922 ) ;
#9214=CARTESIAN_POINT ( 'NONE',  ( 0.4754618798421162973, -13.89949764182683190, 0.7484603771383941950 ) ) ;
#9215=DIRECTION ( 'NONE',  ( 0.7635533937278216055, 0.02138673900302332995, -0.6453904417649386493 ) ) ;
#9219=CARTESIAN_POINT ( 'NONE',  ( 3.512766787570770433, -2.025881399556492823, 14.91422000116819113 ) ) ;
#9226=CARTESIAN_POINT ( 'NONE',  ( 2.002547531651519996, 12.57989064830759496, -0.6781519942172177240 ) ) ;
#9227=LINE ( 'NONE', #17645, #10926 ) ;
#9232=ORIENTED_EDGE ( 'NONE', *, *, #15792, .F. ) ;
#9245=CARTESIAN_POINT ( 'NONE',  ( 16.56753206892534891, 0.001421777558675943985, -0.009389754735542252262 ) ) ;
#9250=ORIENTED_EDGE ( 'NONE', *, *, #8589, .F. ) ;
#9252=VERTEX_POINT ( 'NONE', #6546 ) ;
#9254=CARTESIAN_POINT ( 'NONE',  ( 1.847380140988736708, -7.402792205949027426, -10.00162556679659076 ) ) ;
#9271=ORIENTED_EDGE ( 'NONE', *, *, #4630, .F. ) ;
#9272=CARTESIAN_POINT ( 'NONE',  ( 0.4754618798421167414, -3.583352865732579051, -13.45049478164063217 ) ) ;
#9273=CARTESIAN_POINT ( 'NONE',  ( 16.57605080000000086, 6.799999999999999822, -1.500000000000000000 ) ) ;
#9275=CARTESIAN_POINT ( 'NONE',  ( 3.950837973638675393, -10.51028938476224894, 10.05648675950122595 ) ) ;
#9284=CARTESIAN_POINT ( 'NONE',  ( 0.3151928476913591903, 13.73922860838471749, -0.0002082997484259338093 ) ) ;
#9293=ORIENTED_EDGE ( 'NONE', *, *, #14599, .T. ) ;
#9295=CARTESIAN_POINT ( 'NONE',  ( 0.4754618798421162973, -0.7484603771383456783, -13.89949764182683545 ) ) ;
#9298=CARTESIAN_POINT ( 'NONE',  ( 0.4754618798421162973, 3.583352865732667425, 13.45049478164061441 ) ) ;
#9303=VECTOR ( 'NONE', #2748, 1000.000000000000000 ) ;
#9305=CARTESIAN_POINT ( 'NONE',  ( 0.3151926232592440202, 11.07013665200807395, -8.137833541809259330 ) ) ;
#9317=EDGE_CURVE ( 'NONE', #2137, #9780, #5041, .T. ) ;
#9320=CARTESIAN_POINT ( 'NONE',  ( 1.861706995891666105, -10.38589138506421072, -6.878962591851865760 ) ) ;
#9322=B_SPLINE_CURVE_WITH_KNOTS ( 'NONE', 3,
 ( #6882, #15568, #17195, #5442 ),
 .UNSPECIFIED., .F., .F.,
 ( 4, 4 ),
 ( 1.779952243785056044E-16, 0.002004993803842976610 ),
 .UNSPECIFIED. ) ;
#9337=EDGE_CURVE ( 'NONE', #698, #15961, #10958, .T. ) ;
#9343=CARTESIAN_POINT ( 'NONE',  ( 1.846138399168762101, -3.446241763652916124, -11.95493567637853971 ) ) ;
#9345=CARTESIAN_POINT ( 'NONE',  ( 16.56872352241294521, 0.009382111268606257298, -0.004564908236400254740 ) ) ;
#9346=CARTESIAN_POINT ( 'NONE',  ( 2.636624412714236865, 1.966863607038798701E-15, 16.06066017081991149 ) ) ;
#9350=VECTOR ( 'NONE', #4461, 1000.000000000000114 ) ;
#9360=DIRECTION ( 'NONE',  ( 0.7561779333270775005, -0.6322161072786965930, 0.1688126975276491026 ) ) ;
#9361=CARTESIAN_POINT ( 'NONE',  ( 2.636624412715362631, -15.80357026013197519, 2.862162146984090327 ) ) ;
#9363=CARTESIAN_POINT ( 'NONE',  ( 1.846613052777651198, 10.26230975746759810, 7.035606253495352291 ) ) ;
#9369=DIRECTION ( 'NONE',  ( 0.000000000000000000, 0.000000000000000000, 1.000000000000000000 ) ) ;
#9377=ADVANCED_FACE ( 'NONE', ( #1457, #10054 ), #11228, .F. ) ;
#9378=EDGE_CURVE ( 'NONE', #6482, #9203, #3632, .T. ) ;
#9380=STYLED_ITEM ( 'NONE', ( #965 ), #6229 ) ;
#9384=PRODUCT_DEFINITION_SHAPE ( 'NONE', 'NONE',  #16076 ) ;
#9401=VERTEX_POINT ( 'NONE', #8432 ) ;
#9402=ORIENTED_EDGE ( 'NONE', *, *, #17099, .T. ) ;
#9403=CARTESIAN_POINT ( 'NONE',  ( 2.636624412715137922, 2.161493821597615828, 15.91454522070216093 ) ) ;
#9409=CARTESIAN_POINT ( 'NONE',  ( 2.636624412714236865, 15.91454522070173638, 2.161493821596668585 ) ) ;
#9413=EDGE_CURVE ( 'NONE', #859, #2427, #18676, .T. ) ;
#9414=CARTESIAN_POINT ( 'NONE',  ( 0.4754618798421167414, -0.7484603771385368587, 13.89949764182682301 ) ) ;
#9416=CARTESIAN_POINT ( 'NONE',  ( 1.918921323896323639, 10.48468902844562578, -6.832782632379261756 ) ) ;
#9420=CARTESIAN_POINT ( 'NONE',  ( 0.3137051932979775248, 3.805684345189972895, -13.20008686438101719 ) ) ;
#9421=CARTESIAN_POINT ( 'NONE',  ( 3.950837973638676281, 13.10350451991840615, 6.316429227969512894 ) ) ;
#9423=CARTESIAN_POINT ( 'NONE',  ( 0.3307726912345200776, -7.596084275798974161, 11.46720933246395369 ) ) ;
#9427=EDGE_CURVE ( 'NONE', #2319, #13310, #13488, .T. ) ;
#9433=B_SPLINE_CURVE_WITH_KNOTS ( 'NONE', 3,
 ( #4286, #17092, #5795, #3997, #9912, #15745 ),
 .UNSPECIFIED., .F., .F.,
 ( 4, 2, 4 ),
 ( 0.000000000000000000, 0.001500839035891551355, 0.003001678071783102711 ),
 .UNSPECIFIED. ) ;
#9435=CARTESIAN_POINT ( 'NONE',  ( 16.57605080000000086, 6.799999999999999822, -1.500000000000000000 ) ) ;
#9436=CARTESIAN_POINT ( 'NONE',  ( 1.845755665166724846, -3.386720041070645948, -11.97169564665394681 ) ) ;
#9437=CARTESIAN_POINT ( 'NONE',  ( 2.320521194582656488, -7.743190876766163022, 13.71278319228045284 ) ) ;
#9439=CARTESIAN_POINT ( 'NONE',  ( 0.4862570985993252548, -5.003653737315580052, 12.97920246947877665 ) ) ;
#9443=CARTESIAN_POINT ( 'NONE',  ( 0.3137051932979792457, 8.442169467527008919, -10.83767969834794087 ) ) ;
#9444=CARTESIAN_POINT ( 'NONE',  ( 0.3058872367615230181, -11.46514199369352482, -7.578326039752732335 ) ) ;
#9445=ORIENTED_EDGE ( 'NONE', *, *, #9317, .T. ) ;
#9446=EDGE_LOOP ( 'NONE', ( #15338, #6785, #9097, #2243 ) ) ;
#9447=EDGE_LOOP ( 'NONE', ( #9846, #8872, #9754, #7052 ) ) ;
#9453=CARTESIAN_POINT ( 'NONE',  ( 16.57210152137263393, 0.008007331252332874558, 0.01214401161737521141 ) ) ;
#9457=VECTOR ( 'NONE', #13394, 1000.000000000000000 ) ;
#9458=CARTESIAN_POINT ( 'NONE',  ( 0.8740779401507015045, 14.27348745891557158, -0.8420120399581809689 ) ) ;
#9460=CARTESIAN_POINT ( 'NONE',  ( 16.57778382496167424, -0.006312874906843954532, -0.01354073047775891311 ) ) ;
#9462=CARTESIAN_POINT ( 'NONE',  ( 2.636624412716062071, -11.10302021258080352, -11.60464335004061454 ) ) ;
#9466=CARTESIAN_POINT ( 'NONE',  ( 0.8740764193771586310, 12.04241474978035420, -7.708542792189425619 ) ) ;
#9467=EDGE_LOOP ( 'NONE', ( #7342, #8824, #4862, #13285 ) ) ;
#9473=B_SPLINE_CURVE_WITH_KNOTS ( 'NONE', 3,
 ( #18507, #5858, #14751, #9027 ),
 .UNSPECIFIED., .F., .F.,
 ( 4, 4 ),
 ( 0.000000000000000000, 0.002004993803842618390 ),
 .UNSPECIFIED. ) ;
#9477=CARTESIAN_POINT ( 'NONE',  ( 3.377929128793398572, 3.070552481925057364, -13.64476897106781017 ) ) ;
#9481=EDGE_CURVE ( 'NONE', #8310, #6145, #10714, .T. ) ;
#9483=DIRECTION ( 'NONE',  ( -0.7635533937278216055, -0.2197766120036420967, -0.6071939193889598352 ) ) ;
#9488=CARTESIAN_POINT ( 'NONE',  ( 0.3095370825347224519, 3.806662003783598536, -13.20347358821910433 ) ) ;
#9490=CARTESIAN_POINT ( 'NONE',  ( 1.254255976357310010, 7.789651112956863521, 12.44256109021772438 ) ) ;
#9491=ORIENTED_EDGE ( 'NONE', *, *, #11670, .F. ) ;
#9495=ADVANCED_FACE ( 'NONE', ( #5838 ), #2002, .T. ) ;
#9509=CARTESIAN_POINT ( 'NONE',  ( 3.950837973638676281, -12.81214529934979929, 6.888253895133251703 ) ) ;
#9511=ORIENTED_EDGE ( 'NONE', *, *, #8168, .T. ) ;
#9515=ORIENTED_EDGE ( 'NONE', *, *, #10653, .F. ) ;
#9519=EDGE_LOOP ( 'NONE', ( #16483, #2717, #15445, #705 ) ) ;
#9520=CARTESIAN_POINT ( 'NONE',  ( 1.845755665166723736, -12.43231320373360482, -0.4784952423729852966 ) ) ;
#9521=CARTESIAN_POINT ( 'NONE',  ( 1.342453679581834924, 14.76648944001039254, 0.9602753779831241232 ) ) ;
#9522=CARTESIAN_POINT ( 'NONE',  ( 2.636624412715137922, -6.973567714907947135, 14.46769361191283920 ) ) ;
#9528=CARTESIAN_POINT ( 'NONE',  ( 16.56782317627811096, 0.003357783021327817585, 0.009228812961908668469 ) ) ;
#9530=EDGE_LOOP ( 'NONE', ( #18785, #14070, #7399, #11055 ) ) ;
#9532=ORIENTED_EDGE ( 'NONE', *, *, #13952, .F. ) ;
#9533=CARTESIAN_POINT ( 'NONE',  ( 16.56872352241294521, 0.007240717549633990044, -0.007512283835805476720 ) ) ;
#9536=CARTESIAN_POINT ( 'NONE',  ( 16.58200780006414732, -0.002844973367391502410, 0.01080144354108869553 ) ) ;
#9541=CARTESIAN_POINT ( 'NONE',  ( 16.58200780006414732, -0.008650561019685852962, -0.007066318000005976374 ) ) ;
#9546=CARTESIAN_POINT ( 'NONE',  ( 1.562796894703937678, 0.000000000000000000, 0.000000000000000000 ) ) ;
#9548=CARTESIAN_POINT ( 'NONE',  ( 3.664313757352979373, 13.97913389346637736, -2.831308606787096949 ) ) ;
#9550=CARTESIAN_POINT ( 'NONE',  ( 0.3170788640506440603, 11.02668139258442359, 8.200855617524574370 ) ) ;
#9551=ORIENTED_EDGE ( 'NONE', *, *, #11670, .T. ) ;
#9552=CARTESIAN_POINT ( 'NONE',  ( 16.57210152137263393, 0.0006600038696346007027, -0.01453130299868522768 ) ) ;
#9553=EDGE_CURVE ( 'NONE', #17458, #17275, #454, .T. ) ;
#9559=ORIENTED_EDGE ( 'NONE', *, *, #13442, .F. ) ;
#9561=CARTESIAN_POINT ( 'NONE',  ( 2.636624412715362631, -15.80357026013197519, 2.862162146984090327 ) ) ;
#9565=FILL_AREA_STYLE ('',( #8243 ) ) ;
#9571=CARTESIAN_POINT ( 'NONE',  ( 2.002547531651520885, -4.532360870844412304, 11.75462648437100377 ) ) ;
#9572=ORIENTED_EDGE ( 'NONE', *, *, #10653, .T. ) ;
#9573=FACE_OUTER_BOUND ( 'NONE', #11742, .T. ) ;
#9574=CARTESIAN_POINT ( 'NONE',  ( 16.56753206892534891, 0.006669401563384923064, -0.006760771273036194837 ) ) ;
#9577=ORIENTED_EDGE ( 'NONE', *, *, #11899, .F. ) ;
#9579=CARTESIAN_POINT ( 'NONE',  ( 0.3058872367615230181, 11.46514199369357989, 7.578326039752647958 ) ) ;
#9581=CARTESIAN_POINT ( 'NONE',  ( 16.57210152137263393, -0.01402404281922924566, 0.003862718596009228310 ) ) ;
#9587=CARTESIAN_POINT ( 'NONE',  ( 3.512766787570761107, 14.91422000116819468, -2.025881399556438200 ) ) ;
#9590=LINE ( 'NONE', #6650, #16884 ) ;
#9592=CARTESIAN_POINT ( 'NONE',  ( 8.522092701127531811, -0.3779863304871711183, 6.946128462138593918 ) ) ;
#9602=ORIENTED_EDGE ( 'NONE', *, *, #16891, .T. ) ;
#9605=CARTESIAN_POINT ( 'NONE',  ( 1.846955891736116184, -0.2634721419534329923, -12.44001089941741611 ) ) ;
#9613=FACE_OUTER_BOUND ( 'NONE', #9447, .T. ) ;
#9616=CARTESIAN_POINT ( 'NONE',  ( 16.56753206892534891, -0.009389754735541561842, 0.001421777558676752366 ) ) ;
#9620=ORIENTED_EDGE ( 'NONE', *, *, #11622, .F. ) ;
#9622=VERTEX_POINT ( 'NONE', #16563 ) ;
#9625=CARTESIAN_POINT ( 'NONE',  ( 8.438534575730034959, 6.862570336891075762, -0.2320579683290367456 ) ) ;
#9628=CARTESIAN_POINT ( 'NONE',  ( 0.3095370825347224519, -13.73357284481724427, -0.4597470195091612477 ) ) ;
#9631=ORIENTED_EDGE ( 'NONE', *, *, #7390, .T. ) ;
#9633=DIRECTION ( 'NONE',  ( -0.7561779333270775005, -0.5491072561318312006, -0.3559159372837374935 ) ) ;
#9635=CARTESIAN_POINT ( 'NONE',  ( 0.4385251269669948049, 13.84299131624729817, 0.7363879510385874516 ) ) ;
#9637=CARTESIAN_POINT ( 'NONE',  ( 1.977436885027412439, 13.27782258182005748, -7.806953934146017460 ) ) ;
#9640=CARTESIAN_POINT ( 'NONE',  ( 0.3137051932979809665, 10.83767969834803324, 8.442169467526891680 ) ) ;
#9641=ORIENTED_EDGE ( 'NONE', *, *, #3804, .F. ) ;
#9643=ORIENTED_EDGE ( 'NONE', *, *, #4070, .F. ) ;
#9644=CARTESIAN_POINT ( 'NONE',  ( 0.3137051932979792457, -10.83767969834809008, 8.442169467526815296 ) ) ;
#9647=DIRECTION ( 'NONE',  ( 0.000000000000000000, 0.000000000000000000, 1.000000000000000000 ) ) ;
#9648=EDGE_LOOP ( 'NONE', ( #10575, #7316, #17058, #3047 ) ) ;
#9649=CARTESIAN_POINT ( 'NONE',  ( 0.3137051932979792457, -11.37800749014136592, 7.698472063774431717 ) ) ;
#9650=EDGE_CURVE ( 'NONE', #1657, #8563, #14809, .T. ) ;
#9652=EDGE_LOOP ( 'NONE', ( #9532, #1112, #14088, #12226 ) ) ;
#9653=CARTESIAN_POINT ( 'NONE',  ( 1.846613052777651198, -12.43780859207240042, 0.3401093050881381363 ) ) ;
#9656=CARTESIAN_POINT ( 'NONE',  ( 0.3137051932979757485, 13.73004976592202020, -0.4596302728640235258 ) ) ;
#9664=CARTESIAN_POINT ( 'NONE',  ( 2.002547531651519996, 12.57989064830759496, -0.6781519942172177240 ) ) ;
#9668=EDGE_LOOP ( 'NONE', ( #80, #9559, #15831, #10037 ) ) ;
#9673=EDGE_LOOP ( 'NONE', ( #5496, #1337, #2901, #11219 ) ) ;
#9682=CARTESIAN_POINT ( 'NONE',  ( 2.123976203522053741, -13.47898556379307244, -7.899625852120357727 ) ) ;
#9690=CARTESIAN_POINT ( 'NONE',  ( 0.4862570985993252548, 13.44146924561381162, 3.580942890621718888 ) ) ;
#9693=CARTESIAN_POINT ( 'NONE',  ( 0.4862570985993235340, -5.003653737315397976, -12.97920246947884770 ) ) ;
#9708=CARTESIAN_POINT ( 'NONE',  ( 16.56753206892534891, -0.008432171035096417550, 0.004368917149005420789 ) ) ;
#9715=ORIENTED_EDGE ( 'NONE', *, *, #3216, .T. ) ;
#9716=EDGE_LOOP ( 'NONE', ( #10922, #17400, #1642, #11239 ) ) ;
#9717=( BOUNDED_SURFACE ( )  B_SPLINE_SURFACE ( 3, 1, ( 
 ( #8447, #5296 ),
 ( #9967, #4149 ),
 ( #18757, #16961 ),
 ( #12834, #5654 ) ),
 .UNSPECIFIED., .F., .F., .T. ) 
 B_SPLINE_SURFACE_WITH_KNOTS ( ( 4, 4 ),
 ( 2, 2 ),
 ( 0.000000000000000000, 1.000000000000000000 ),
 ( 0.000000000000000000, 1.000000000000000000 ),
 .UNSPECIFIED. ) 
 GEOMETRIC_REPRESENTATION_ITEM ( )  RATIONAL_B_SPLINE_SURFACE ( (
 ( 1.000000000000000000, 1.000000000000000000),
 ( 0.9933953342250438912, 0.8357391271907739227),
 ( 0.9933953342250438912, 0.8357391271907739227),
 ( 1.000000000000000000, 1.000000000000000000) ) ) 
 REPRESENTATION_ITEM ( '' )  SURFACE ( )  );
#9719=EDGE_CURVE ( 'NONE', #11500, #257, #14486, .T. ) ;
#9729=CARTESIAN_POINT ( 'NONE',  ( 3.950837973638675393, -10.51028938476210328, -10.05648675950137871 ) ) ;
#9731=CARTESIAN_POINT ( 'NONE',  ( 0.3095370825347224519, -10.84046130709052491, -8.444334731364122604 ) ) ;
#9732=CARTESIAN_POINT ( 'NONE',  ( 2.002547531651519996, 12.17374746633578475, 3.242439124566693476 ) ) ;
#9736=ORIENTED_EDGE ( 'NONE', *, *, #13998, .F. ) ;
#9744=CARTESIAN_POINT ( 'NONE',  ( 2.002547531651519996, -12.17374746633575988, -3.242439124566779185 ) ) ;
#9750=DIRECTION ( 'NONE',  ( -1.000000000000000000, -0.000000000000000000, -0.000000000000000000 ) ) ;
#9751=LINE ( 'NONE', #16929, #13841 ) ;
#9754=ORIENTED_EDGE ( 'NONE', *, *, #10921, .F. ) ;
#9755=CARTESIAN_POINT ( 'NONE',  ( 0.4862570985993235340, 10.79774104611385965, -8.769551628660616771 ) ) ;
#9759=ORIENTED_EDGE ( 'NONE', *, *, #11257, .T. ) ;
#9762=ORIENTED_EDGE ( 'NONE', *, *, #9553, .F. ) ;
#9764=EDGE_CURVE ( 'NONE', #11032, #14416, #8510, .T. ) ;
#9766=DIRECTION ( 'NONE',  ( -1.000000000000000000, -0.000000000000000000, -0.000000000000000000 ) ) ;
#9774=FACE_OUTER_BOUND ( 'NONE', #1143, .T. ) ;
#9776=CARTESIAN_POINT ( 'NONE',  ( 1.562796894703937678, 0.000000000000000000, -12.15840553252917289 ) ) ;
#9777=ORIENTED_EDGE ( 'NONE', *, *, #16792, .F. ) ;
#9779=ORIENTED_EDGE ( 'NONE', *, *, #16891, .F. ) ;
#9780=VERTEX_POINT ( 'NONE', #7078 ) ;
#9781=ORIENTED_EDGE ( 'NONE', *, *, #1397, .T. ) ;
#9786=CARTESIAN_POINT ( 'NONE',  ( 8.438534575730034959, 5.415535776177522465, 4.221456476902686106 ) ) ;
#9791=CARTESIAN_POINT ( 'NONE',  ( 0.3058872367615226295, 12.87003593440628357, 4.821066432589371509 ) ) ;
#9792=EDGE_LOOP ( 'NONE', ( #6589, #6471, #13504, #2973 ) ) ;
#9793=ORIENTED_EDGE ( 'NONE', *, *, #6662, .T. ) ;
#9798=LINE ( 'NONE', #15828, #1994 ) ;
#9803=ORIENTED_EDGE ( 'NONE', *, *, #17934, .T. ) ;
#9805=CARTESIAN_POINT ( 'NONE',  ( 1.845755665166725734, -11.97169564665393970, 3.386720041070682363 ) ) ;
#9806=DIRECTION ( 'NONE',  ( 0.7561779333270775005, -0.2350349629540270657, 0.6106991889125030770 ) ) ;
#9807=CARTESIAN_POINT ( 'NONE',  ( 0.3939822652208105902, 13.80035637018652395, 0.7002900021918435636 ) ) ;
#9809=CARTESIAN_POINT ( 'NONE',  ( 0.8740779401507027258, 13.83508928787419912, 3.609949156401401904 ) ) ;
#9812=CARTESIAN_POINT ( 'NONE',  ( 3.950837973638676281, -6.316429227969383220, -13.10350451991847009 ) ) ;
#9814=CARTESIAN_POINT ( 'NONE',  ( 16.56753206892534891, 0.004368917149004243779, -0.008432171035096398468 ) ) ;
#9815=ORIENTED_EDGE ( 'NONE', *, *, #17435, .F. ) ;
#9816=CARTESIAN_POINT ( 'NONE',  ( 0.3137051932979792457, -10.83767969834796929, -8.442169467526971616 ) ) ;
#9818=CARTESIAN_POINT ( 'NONE',  ( 0.3720661004400040439, -13.34435358167250207, -3.575426119359325750 ) ) ;
#9822=EDGE_CURVE ( 'NONE', #6216, #13188, #9322, .T. ) ;
#9824=CARTESIAN_POINT ( 'NONE',  ( 1.846138399168762101, -12.43476674860266940, 0.4167076046095114505 ) ) ;
#9827=DIRECTION ( 'NONE',  ( -1.000000000000000000, -0.000000000000000000, -0.000000000000000000 ) ) ;
#9830=CARTESIAN_POINT ( 'NONE',  ( 2.636624412714236865, 0.000000000000000000, 0.000000000000000000 ) ) ;
#9831=B_SPLINE_CURVE_WITH_KNOTS ( 'NONE', 3,
 ( #6295, #4950, #12304, #6390 ),
 .UNSPECIFIED., .F., .F.,
 ( 4, 4 ),
 ( 1.734723475976807094E-17, 0.003005512676784844427 ),
 .UNSPECIFIED. ) ;
#9835=( NAMED_UNIT ( * ) SI_UNIT ( $, .STERADIAN. ) SOLID_ANGLE_UNIT ( ) );
#9837=FACE_OUTER_BOUND ( 'NONE', #16690, .T. ) ;
#9838=CARTESIAN_POINT ( 'NONE',  ( 2.002547531651519996, -12.57989064830760206, 0.6781519942171299054 ) ) ;
#9839=VERTEX_POINT ( 'NONE', #3570 ) ;
#9841=CARTESIAN_POINT ( 'NONE',  ( 0.3142014840576535795, -12.94260032291125562, -4.608051180497059640 ) ) ;
#9843=CARTESIAN_POINT ( 'NONE',  ( 1.845756295923361323, -9.776763338604659737, 7.694561132136919390 ) ) ;
#9844=CARTESIAN_POINT ( 'NONE',  ( 1.918918678667074440, 12.49849921341423276, -0.6348738215465657975 ) ) ;
#9846=ORIENTED_EDGE ( 'NONE', *, *, #11458, .F. ) ;
#9848=CARTESIAN_POINT ( 'NONE',  ( 1.342453679581834924, 0.9602753779832786662, -14.76648944001038188 ) ) ;
#9849=EDGE_CURVE ( 'NONE', #14945, #8143, #5061, .T. ) ;
#9854=ORIENTED_EDGE ( 'NONE', *, *, #16963, .F. ) ;
#9856=CARTESIAN_POINT ( 'NONE',  ( 0.3058872367615226295, 0.6080468242582872662, -13.72992299905059177 ) ) ;
#9865=CARTESIAN_POINT ( 'NONE',  ( 1.846138399168762101, 6.971848976711159551, -10.30487220521562541 ) ) ;
#9866=VERTEX_POINT ( 'NONE', #9744 ) ;
#9871=ORIENTED_EDGE ( 'NONE', *, *, #13442, .T. ) ;
#9878=CARTESIAN_POINT ( 'NONE',  ( 2.636624412715138366, -11.10302021257964888, 11.60464335004044223 ) ) ;
#9882=CARTESIAN_POINT ( 'NONE',  ( 0.3307726912345178572, 7.596084275799059427, -11.46720933246390572 ) ) ;
#9884=CARTESIAN_POINT ( 'NONE',  ( 16.56872352241294521, -0.009382111268606286789, 0.004564908236400187953 ) ) ;
#9886=B_SPLINE_CURVE_WITH_KNOTS ( 'NONE', 3,
 ( #2503, #16958, #8178, #3863, #12741, #9693 ),
 .UNSPECIFIED., .F., .F.,
 ( 4, 2, 4 ),
 ( 1.748223473168675632E-18, 0.0002017457492448088553, 0.0004034914984896159759 ),
 .UNSPECIFIED. ) ;
#9890=VERTEX_POINT ( 'NONE', #529 ) ;
#9891=B_SPLINE_CURVE_WITH_KNOTS ( 'NONE', 3,
 ( #13243, #4459, #16215, #14676 ),
 .UNSPECIFIED., .F., .F.,
 ( 4, 4 ),
 ( 1.629624753548408703E-17, 0.003005512676784843126 ),
 .UNSPECIFIED. ) ;
#9893=EDGE_CURVE ( 'NONE', #9212, #6154, #13794, .T. ) ;
#9895=ORIENTED_EDGE ( 'NONE', *, *, #14449, .F. ) ;
#9897=VECTOR ( 'NONE', #7534, 1000.000000000000000 ) ;
#9899=CARTESIAN_POINT ( 'NONE',  ( 1.846138399168762101, -11.69739621335925328, 4.238866729160359448 ) ) ;
#9902=CARTESIAN_POINT ( 'NONE',  ( 1.846955891736119293, -7.098901504650428684, 10.21904526726843798 ) ) ;
#9906=CARTESIAN_POINT ( 'NONE',  ( 0.4862570985993252548, -3.580942890621766406, 13.44146924561379741 ) ) ;
#9909=CARTESIAN_POINT ( 'NONE',  ( 3.950837973638668288, 0.000000000000000000, 0.000000000000000000 ) ) ;
#9912=CARTESIAN_POINT ( 'NONE',  ( 3.664313757352976708, 5.926151963190554817, -12.97355833021534011 ) ) ;
#9915=AXIS2_PLACEMENT_3D ( 'NONE', #10247, #2963, #1549 ) ;
#9921=CARTESIAN_POINT ( 'NONE',  ( 0.3058872367615230181, -10.75034008168922206, 8.562166468153680654 ) ) ;
#9927=VERTEX_POINT ( 'NONE', #3969 ) ;
#9929=CARTESIAN_POINT ( 'NONE',  ( 8.522092701127531811, -3.777034505568479528, -5.841710761610173108 ) ) ;
#9930=B_SPLINE_CURVE_WITH_KNOTS ( 'NONE', 3,
 ( #2195, #9635, #9807, #14117, #17088, #8217 ),
 .UNSPECIFIED., .F., .F.,
 ( 4, 2, 4 ),
 ( 4.206917491929696500E-17, 0.0002014099069817281611, 0.0004028198139634142552 ),
 .UNSPECIFIED. ) ;
#9937=( LENGTH_UNIT ( ) NAMED_UNIT ( * ) SI_UNIT ( .MILLI., .METRE. ) );
#9942=FACE_OUTER_BOUND ( 'NONE', #9792, .T. ) ;
#9946=CARTESIAN_POINT ( 'NONE',  ( 2.636624412715137922, -14.46769361191291559, 6.973567714907789927 ) ) ;
#9949=CARTESIAN_POINT ( 'NONE',  ( 0.3939822652208145870, 10.75310269629521365, 8.678192463540208124 ) ) ;
#9954=DIRECTION ( 'NONE',  ( -0.000000000000000000, 0.000000000000000000, 1.000000000000000000 ) ) ;
#9957=STYLED_ITEM ( 'NONE', ( #5392 ), #16223 ) ;
#9960=CARTESIAN_POINT ( 'NONE',  ( 1.845755665166724180, 7.694641135842960722, -9.776700214453546423 ) ) ;
#9967=CARTESIAN_POINT ( 'NONE',  ( 16.56822296793089322, 0.0007467251401288622394, -0.01011126603341004279 ) ) ;
#9974=DIRECTION ( 'NONE',  ( 0.000000000000000000, 0.000000000000000000, 1.000000000000000000 ) ) ;
#9978=CARTESIAN_POINT ( 'NONE',  ( 8.438534575730034959, -0.2320579683290609485, 6.862570336891074874 ) ) ;
#9979=CARTESIAN_POINT ( 'NONE',  ( 0.3148208552358952583, 12.99355031785211168, -4.463611911212083783 ) ) ;
#9983=CARTESIAN_POINT ( 'NONE',  ( 0.4862570985993235340, 7.559321496869593204, -11.67702470553357053 ) ) ;
#9984=CARTESIAN_POINT ( 'NONE',  ( 0.3151928476913565258, -0.0002082997482820912163, -13.73922860838471927 ) ) ;
#9990=VERTEX_POINT ( 'NONE', #5404 ) ;
#9991=CIRCLE ( 'NONE', #14889, 16.06066017081991149 ) ;
#9994=EDGE_LOOP ( 'NONE', ( #1390, #4075, #13526, #18120 ) ) ;
#9996=CARTESIAN_POINT ( 'NONE',  ( 16.56753206892534891, -0.001421777558676855365, -0.009389754735541546229 ) ) ;
#9999=CARTESIAN_POINT ( 'NONE',  ( 2.320521194582183977, 6.542541239684722676, 14.32454473829914399 ) ) ;
#10007=CARTESIAN_POINT ( 'NONE',  ( 0.3720661004400040439, -7.524064345033547596, 11.58636699658212699 ) ) ;
#10009=EDGE_LOOP ( 'NONE', ( #5611, #6849, #15919, #731 ) ) ;
#10012=ORIENTED_EDGE ( 'NONE', *, *, #14630, .F. ) ;
#10014=ORIENTED_EDGE ( 'NONE', *, *, #9134, .T. ) ;
#10019=CARTESIAN_POINT ( 'NONE',  ( 0.3137051932979792457, -12.91601973349266963, -4.679953077377624560 ) ) ;
#10022=B_SPLINE_CURVE_WITH_KNOTS ( 'NONE', 3,
 ( #15579, #3738, #8333, #14251, #18273, #5451 ),
 .UNSPECIFIED., .F., .F.,
 ( 4, 2, 4 ),
 ( 2.710505431213761085E-19, 0.001657017934712013297, 0.003314035869424026594 ),
 .UNSPECIFIED. ) ;
#10027=CARTESIAN_POINT ( 'NONE',  ( 0.3151928476913619104, -4.245853234426296474, -13.06671852871093265 ) ) ;
#10028=CARTESIAN_POINT ( 'NONE',  ( 2.636624412714236865, 0.000000000000000000, 0.000000000000000000 ) ) ;
#10031=CARTESIAN_POINT ( 'NONE',  ( 8.438534575730034959, -5.688336279099016402, -3.845978796786099885 ) ) ;
#10037=ORIENTED_EDGE ( 'NONE', *, *, #10814, .F. ) ;
#10046=FACE_OUTER_BOUND ( 'NONE', #13005, .T. ) ;
#10047=EDGE_CURVE ( 'NONE', #12518, #11575, #11148, .T. ) ;
#10049=EDGE_CURVE ( 'NONE', #17236, #2621, #16200, .T. ) ;
#10052=CARTESIAN_POINT ( 'NONE',  ( 1.847034903785818694, -9.929438108952092890, -7.498375632854726192 ) ) ;
#10054=FACE_BOUND ( 'NONE', #8277, .T. ) ;
#10058=CARTESIAN_POINT ( 'NONE',  ( 16.57210152137263393, 0.009075239946109033701, 0.01136813053532163831 ) ) ;
#10060=B_SPLINE_CURVE_WITH_KNOTS ( 'NONE', 3,
 ( #18203, #5110, #15329, #9416, #13801, #1967 ),
 .UNSPECIFIED., .F., .F.,
 ( 4, 2, 4 ),
 ( 0.000000000000000000, 0.0001828790815886950779, 0.0003657581631773901558 ),
 .UNSPECIFIED. ) ;
#10066=CARTESIAN_POINT ( 'NONE',  ( 1.845756295923360435, -7.694561132136879422, -9.776763338604684606 ) ) ;
#10073=ORIENTED_EDGE ( 'NONE', *, *, #7389, .F. ) ;
#10078=CARTESIAN_POINT ( 'NONE',  ( 1.959283090834839314, 9.750336807931262229, -7.909254450748897547 ) ) ;
#10079=FACE_OUTER_BOUND ( 'NONE', #8702, .T. ) ;
#10082=CARTESIAN_POINT ( 'NONE',  ( 16.57778382496167424, -0.001819584982832002807, 0.01482878558584568851 ) ) ;
#10083=CARTESIAN_POINT ( 'NONE',  ( 1.959283090834842200, 10.53516775895160507, 6.829027319138286423 ) ) ;
#10084=CARTESIAN_POINT ( 'NONE',  ( 0.3095370825347224519, 11.38092634279639626, -7.700448427571749299 ) ) ;
#10095=VERTEX_POINT ( 'NONE', #14377 ) ;
#10106=CARTESIAN_POINT ( 'NONE',  ( 1.847034903785824023, 3.625649561595307269, 11.90269060117935496 ) ) ;
#10107=CARTESIAN_POINT ( 'NONE',  ( 0.3170788640506440603, -11.02668139258435787, -8.200855617524654306 ) ) ;
#10113=ORIENTED_EDGE ( 'NONE', *, *, #5855, .F. ) ;
#10121=LINE ( 'NONE', #7363, #12331 ) ;
#10134=VECTOR ( 'NONE', #16534, 1000.000000000000000 ) ;
#10136=CARTESIAN_POINT ( 'NONE',  ( 1.847372867223026738, 0.1054171785008226614, -12.44269075185938433 ) ) ;
#10139=CARTESIAN_POINT ( 'NONE',  ( 2.002547531651519996, -10.57595306287287329, -6.845637710436306200 ) ) ;
#10145=CARTESIAN_POINT ( 'NONE',  ( 0.3058872367615226295, 7.578326039752606214, 11.46514199369360298 ) ) ;
#10146=CARTESIAN_POINT ( 'NONE',  ( 16.57210152137263393, 0.01361613799508961699, -0.005118120558001958316 ) ) ;
#10147=CARTESIAN_POINT ( 'NONE',  ( 0.3148213771069381384, -4.463459503829087183, 12.99360322443201277 ) ) ;
#10148=CARTESIAN_POINT ( 'NONE',  ( 0.4385251269669942498, 11.63205320541534071, -7.540955776459614235 ) ) ;
#10153=CARTESIAN_POINT ( 'NONE',  ( 0.4754618798421171855, 13.89949764182682657, -0.7484603771384882309 ) ) ;
#10154=ADVANCED_FACE ( 'NONE', ( #10079 ), #12476, .F. ) ;
#10155=CARTESIAN_POINT ( 'NONE',  ( 0.4754618798421171855, -13.45049478164057000, -3.583352865732813530 ) ) ;
#10157=CARTESIAN_POINT ( 'NONE',  ( 1.342453679581834924, 14.34050741580211508, -3.649820028552582585 ) ) ;
#10160=CARTESIAN_POINT ( 'NONE',  ( 2.002547531651519996, -9.778737580845639599, -7.942910686618280813 ) ) ;
#10162=ORIENTED_EDGE ( 'NONE', *, *, #17675, .F. ) ;
#10168=VERTEX_POINT ( 'NONE', #18021 ) ;
#10171=CARTESIAN_POINT ( 'NONE',  ( 16.56822296793089322, 0.01011126603341077484, -0.0007467251401297481410 ) ) ;
#10172=DIRECTION ( 'NONE',  ( 0.000000000000000000, 0.000000000000000000, 1.000000000000000000 ) ) ;
#10174=CARTESIAN_POINT ( 'NONE',  ( 2.123976203522053741, -15.54801196254788209, 1.531817366691698545 ) ) ;
#10176=CARTESIAN_POINT ( 'NONE',  ( 0.3137051932979757485, -8.442169467526770887, -10.83767969834812561 ) ) ;
#10180=ORIENTED_EDGE ( 'NONE', *, *, #14874, .T. ) ;
#10181=ADVANCED_FACE ( 'NONE', ( #13799 ), #8708, .T. ) ;
#10184=ORIENTED_EDGE ( 'NONE', *, *, #9719, .F. ) ;
#10197=CARTESIAN_POINT ( 'NONE',  ( 2.747332970342022840, 14.49942876448603180, -7.555624153089486761 ) ) ;
#10203=EDGE_LOOP ( 'NONE', ( #17519, #2982, #7161, #2471 ) ) ;
#10206=EDGE_CURVE ( 'NONE', #14287, #11172, #630, .T. ) ;
#10209=EDGE_CURVE ( 'NONE', #13548, #16346, #9031, .T. ) ;
#10214=CARTESIAN_POINT ( 'NONE',  ( 1.846138399168762101, 11.95493567637855392, -3.446241763652874379 ) ) ;
#10215=CARTESIAN_POINT ( 'NONE',  ( 1.342453679581834924, 12.51077660954477189, -7.902645620902311485 ) ) ;
#10216=ORIENTED_EDGE ( 'NONE', *, *, #3988, .T. ) ;
#10222=CARTESIAN_POINT ( 'NONE',  ( 1.846524061778021419, 11.71897913237549105, 4.180439405448364454 ) ) ;
#10225=AXIS2_PLACEMENT_3D ( 'NONE', #9127, #6715, #6366 ) ;
#10228=ORIENTED_EDGE ( 'NONE', *, *, #4112, .T. ) ;
#10231=CARTESIAN_POINT ( 'NONE',  ( 3.512766787570793969, 2.682019731918377836, 14.81029789862155255 ) ) ;
#10233=ORIENTED_EDGE ( 'NONE', *, *, #1458, .T. ) ;
#10240=VECTOR ( 'NONE', #5351, 1000.000000000000227 ) ;
#10247=CARTESIAN_POINT ( 'NONE',  ( 3.950837973638668288, 0.000000000000000000, 0.000000000000000000 ) ) ;
#10250=DIRECTION ( 'NONE',  ( -1.000000000000000000, -0.000000000000000000, -0.000000000000000000 ) ) ;
#10251=CARTESIAN_POINT ( 'NONE',  ( 1.342453679581834924, 14.76648944001039254, -0.9602753779831244563 ) ) ;
#10252=VECTOR ( 'NONE', #15456, 1000.000000000000114 ) ;
#10258=CARTESIAN_POINT ( 'NONE',  ( 2.002547531651519996, 4.532360870844327039, 11.75462648437103752 ) ) ;
#10259=CARTESIAN_POINT ( 'NONE',  ( 16.56679352167444819, 0.008252760440870188924, -0.004277682826583317083 ) ) ;
#10265=EDGE_LOOP ( 'NONE', ( #9779, #4288, #8777, #6487 ) ) ;
#10273=CARTESIAN_POINT ( 'NONE',  ( 1.861706995891664773, 10.38589138506426934, 6.878962591851789377 ) ) ;
#10274=CONICAL_SURFACE ( 'NONE', #11808, 14.54644660717763927, 0.8559913436420816257 ) ;
#10275=CARTESIAN_POINT ( 'NONE',  ( 1.342453679581834924, 5.476372339890016150, 13.74702459364886487 ) ) ;
#10276=VECTOR ( 'NONE', #12854, 1000.000000000000114 ) ;
#10281=ORIENTED_EDGE ( 'NONE', *, *, #4070, .T. ) ;
#10282=VECTOR ( 'NONE', #14921, 1000.000000000000227 ) ;
#10284=VERTEX_POINT ( 'NONE', #12990 ) ;
#10286=CARTESIAN_POINT ( 'NONE',  ( 2.002547531651519996, -3.242439124566566910, -12.17374746633581495 ) ) ;
#10289=CARTESIAN_POINT ( 'NONE',  ( 3.950837973638677170, 12.81214529934985080, -6.888253895133152227 ) ) ;
#10292=VECTOR ( 'NONE', #3742, 1000.000000000000000 ) ;
#10295=LINE ( 'NONE', #12212, #6544 ) ;
#10297=CARTESIAN_POINT ( 'NONE',  ( 1.918918678667047129, -3.258447776119917094, 12.08296592096907318 ) ) ;
#10302=CARTESIAN_POINT ( 'NONE',  ( 0.3939822652208129217, -12.90851734139303453, -4.930560016699199188 ) ) ;
#10303=B_SPLINE_CURVE_WITH_KNOTS ( 'NONE', 3,
 ( #16043, #8788, #14331, #17578, #5616, #8876 ),
 .UNSPECIFIED., .F., .F.,
 ( 4, 2, 4 ),
 ( 3.522439207679730663E-17, 0.0001825746017570575039, 0.0003651492035140797713 ),
 .UNSPECIFIED. ) ;
#10305=CARTESIAN_POINT ( 'NONE',  ( 1.847372867223024073, 7.228345833872753978, 10.12831093686724238 ) ) ;
#10307=VERTEX_POINT ( 'NONE', #4304 ) ;
#10309=ORIENTED_EDGE ( 'NONE', *, *, #7639, .F. ) ;
#10310=ORIENTED_EDGE ( 'NONE', *, *, #2510, .F. ) ;
#10312=CARTESIAN_POINT ( 'NONE',  ( 16.56782317627811096, -0.008141063682853446129, 0.005492611183758502880 ) ) ;
#10316=CARTESIAN_POINT ( 'NONE',  ( 1.977228804422745512, -10.21522664410476366, -11.52787183731191512 ) ) ;
#10318=ORIENTED_EDGE ( 'NONE', *, *, #12264, .F. ) ;
#10321=CARTESIAN_POINT ( 'NONE',  ( 3.353306896162456585, 10.44017738170056298, 9.252610477110303933 ) ) ;
#10325=VECTOR ( 'NONE', #1060, 1000.000000000000114 ) ;
#10329=CARTESIAN_POINT ( 'NONE',  ( 1.846138399168762101, 0.4167076046097279440, -12.43476674860266051 ) ) ;
#10345=CARTESIAN_POINT ( 'NONE',  ( 0.000000000000000000, 4.769696007084728073, 1.500000000000000000 ) ) ;
#10346=CARTESIAN_POINT ( 'NONE',  ( 16.57778382496167424, 0.01306626476309378365, 0.007244066302947740205 ) ) ;
#10347=EDGE_CURVE ( 'NONE', #15522, #13528, #4215, .T. ) ;
#10348=CARTESIAN_POINT ( 'NONE',  ( 0.3095370825347224519, -8.444334731364081748, 10.84046130709055689 ) ) ;
#10351=CARTESIAN_POINT ( 'NONE',  ( 1.959283090834842200, 4.509128209890970851, 11.71721539537256618 ) ) ;
#10352=CARTESIAN_POINT ( 'NONE',  ( 0.3137051932979792457, -7.698472063774386420, -11.37800749014139612 ) ) ;
#10365=CARTESIAN_POINT ( 'NONE',  ( 3.950837973638676281, 1.958075594453990487, -14.41405733518058341 ) ) ;
#10369=CARTESIAN_POINT ( 'NONE',  ( 2.002547531651519996, 9.778737580845815458, -7.942910686618064986 ) ) ;
#10371=CARTESIAN_POINT ( 'NONE',  ( 1.847426409206469611, 0.06227732482722434654, 12.44303504652092762 ) ) ;
#10372=CARTESIAN_POINT ( 'NONE',  ( 2.002547531651520885, 10.57595306287292480, 6.845637710436228929 ) ) ;
#10375=EDGE_CURVE ( 'NONE', #1375, #5025, #14878, .T. ) ;
#10380=VERTEX_POINT ( 'NONE', #8795 ) ;
#10391=DIRECTION ( 'NONE',  ( 1.000000000000000000, 0.000000000000000000, 0.000000000000000000 ) ) ;
#10392=B_SPLINE_CURVE_WITH_KNOTS ( 'NONE', 3,
 ( #2795, #11610, #14661, #17442, #11703, #1574, #1484, #4258, #141, #242, #13136, #8641, #7513 ),
 .UNSPECIFIED., .F., .F.,
 ( 4, 3, 3, 3, 4 ),
 ( 3.878959614448864246E-18, 0.0002299780670421047908, 0.0004599561239687891445, 0.0006896788984287886056, 0.0009194956271626397379 ),
 .UNSPECIFIED. ) ;
#10396=CARTESIAN_POINT ( 'NONE',  ( 1.847168016377982003, 7.464000291196414061, 9.955470380986653822 ) ) ;
#10398=ORIENTED_EDGE ( 'NONE', *, *, #4312, .T. ) ;
#10399=EDGE_CURVE ( 'NONE', #6039, #14233, #18069, .T. ) ;
#10401=VERTEX_POINT ( 'NONE', #1531 ) ;
#10403=VERTEX_POINT ( 'NONE', #4593 ) ;
#10406=CARTESIAN_POINT ( 'NONE',  ( 1.977436885026044200, -13.27782258181834685, 7.806953934146225293 ) ) ;
#10409=ORIENTED_EDGE ( 'NONE', *, *, #11899, .T. ) ;
#10413=CARTESIAN_POINT ( 'NONE',  ( 0.3720661004400040439, 12.89739157014199833, -4.951033743989506242 ) ) ;
#10414=ORIENTED_EDGE ( 'NONE', *, *, #15649, .F. ) ;
#10417=CARTESIAN_POINT ( 'NONE',  ( 1.861706995891665439, -6.878962591851823127, 10.38589138506424092 ) ) ;
#10419=VERTEX_POINT ( 'NONE', #4783 ) ;
#10420=AXIS2_PLACEMENT_3D ( 'NONE', #4990, #6241, #13496 ) ;
#10422=CARTESIAN_POINT ( 'NONE',  ( 8.438534575730034959, -6.454982381540271597, -2.341351102130346362 ) ) ;
#10426=EDGE_CURVE ( 'NONE', #5784, #12474, #10793, .T. ) ;
#10433=ORIENTED_EDGE ( 'NONE', *, *, #16193, .T. ) ;
#10434=CARTESIAN_POINT ( 'NONE',  ( 1.846822687350018644, 4.121816957446363894, -11.74004266906800353 ) ) ;
#10435=CARTESIAN_POINT ( 'NONE',  ( 3.950837973638677170, 13.10350451991849141, -6.316429227969337923 ) ) ;
#10441=LINE ( 'NONE', #16277, #17187 ) ;
#10442=DIRECTION ( 'NONE',  ( 0.000000000000000000, 0.000000000000000000, 1.000000000000000000 ) ) ;
#10446=( BOUNDED_SURFACE ( )  B_SPLINE_SURFACE ( 3, 1, ( 
 ( #6451, #14078 ),
 ( #5281, #15507 ),
 ( #5007, #15322 ),
 ( #6816, #18290 ) ),
 .UNSPECIFIED., .F., .F., .T. ) 
 B_SPLINE_SURFACE_WITH_KNOTS ( ( 4, 4 ),
 ( 2, 2 ),
 ( 0.000000000000000000, 1.000000000000000000 ),
 ( 0.000000000000000000, 1.000000000000000000 ),
 .UNSPECIFIED. ) 
 GEOMETRIC_REPRESENTATION_ITEM ( )  RATIONAL_B_SPLINE_SURFACE ( (
 ( 1.000000000000000000, 1.000000000000000000),
 ( 0.9933953342250436691, 0.8357391271907733676),
 ( 0.9933953342250436691, 0.8357391271907733676),
 ( 1.000000000000000000, 1.000000000000000000) ) ) 
 REPRESENTATION_ITEM ( '' )  SURFACE ( )  );
#10448=DIRECTION ( 'NONE',  ( -1.000000000000000000, -0.000000000000000000, -0.000000000000000000 ) ) ;
#10450=ORIENTED_EDGE ( 'NONE', *, *, #13789, .F. ) ;
#10451=EDGE_CURVE ( 'NONE', #15061, #620, #16352, .T. ) ;
#10459=CARTESIAN_POINT ( 'NONE',  ( 1.846138399168762101, 10.30487220521580305, -6.971848976710897539 ) ) ;
#10460=CARTESIAN_POINT ( 'NONE',  ( 0.3148208552358917056, -13.73693263646118901, 0.2299193288886990094 ) ) ;
#10461=CARTESIAN_POINT ( 'NONE',  ( 0.3095370825347224519, 0.4597470195090193057, 13.73357284481724960 ) ) ;
#10463=B_SPLINE_CURVE_WITH_KNOTS ( 'NONE', 3,
 ( #10703, #16538, #13665, #14278 ),
 .UNSPECIFIED., .F., .F.,
 ( 4, 4 ),
 ( 0.000000000000000000, 0.002004993803842703825 ),
 .UNSPECIFIED. ) ;
#10472=CARTESIAN_POINT ( 'NONE',  ( 0.4754618798421162973, -0.7484603771385398563, 13.89949764182682301 ) ) ;
#10473=EDGE_CURVE ( 'NONE', #3538, #10284, #5595, .T. ) ;
#10478=EDGE_LOOP ( 'NONE', ( #17543, #4173, #2488, #9643 ) ) ;
#10479=ORIENTED_EDGE ( 'NONE', *, *, #4799, .F. ) ;
#10488=FACE_OUTER_BOUND ( 'NONE', #11054, .T. ) ;
#10492=CARTESIAN_POINT ( 'NONE',  ( 1.918918678667044686, -4.466049546133833203, -11.69059232068582865 ) ) ;
#10496=CARTESIAN_POINT ( 'NONE',  ( 1.846138399168762101, 0.4167076046097279440, -12.43476674860266051 ) ) ;
#10499=ORIENTED_EDGE ( 'NONE', *, *, #10715, .T. ) ;
#10502=CARTESIAN_POINT ( 'NONE',  ( 1.846138399168762101, -7.646096044339819819, -9.815003036200495856 ) ) ;
#10504=CONICAL_SURFACE ( 'NONE', #16912, 14.54644660717763927, 0.8559913436420816257 ) ;
#10509=CARTESIAN_POINT ( 'NONE',  ( 0.4862570985993252548, 3.580942890621670482, 13.44146924561382583 ) ) ;
#10512=EDGE_CURVE ( 'NONE', #7527, #14389, #8076, .T. ) ;
#10516=B_SPLINE_CURVE_WITH_KNOTS ( 'NONE', 3,
 ( #9008, #16082, #3160, #8904 ),
 .UNSPECIFIED., .F., .F.,
 ( 4, 4 ),
 ( 3.727890075251872641E-16, 0.002004993803842877297 ),
 .UNSPECIFIED. ) ;
#10520=CARTESIAN_POINT ( 'NONE',  ( 1.959283090834840202, 7.909254450749005017, 9.750336807931171634 ) ) ;
#10522=CARTESIAN_POINT ( 'NONE',  ( 2.002547531651519996, -7.942910686618100513, -9.778737580845787036 ) ) ;
#10523=CARTESIAN_POINT ( 'NONE',  ( 3.377929128793399016, 10.50432311212916225, -9.234024516648208447 ) ) ;
#10525=CARTESIAN_POINT ( 'NONE',  ( 0.3939875929385671105, 11.57636969881034084, 7.545068896001249747 ) ) ;
#10526=CARTESIAN_POINT ( 'NONE',  ( 0.3720661004400040439, 13.79610186261029980, -0.7231997263365288475 ) ) ;
#10527=VERTEX_POINT ( 'NONE', #8038 ) ;
#10532=CARTESIAN_POINT ( 'NONE',  ( 1.847412631396506022, 3.886120457021560171, -11.82061107079959861 ) ) ;
#10534=CARTESIAN_POINT ( 'NONE',  ( 0.3145734862173251711, 13.73540602248380971, 0.3064017202075832724 ) ) ;
#10535=FACE_OUTER_BOUND ( 'NONE', #9652, .T. ) ;
#10538=AXIS2_PLACEMENT_3D ( 'NONE', #11222, #5373, #17038 ) ;
#10540=EDGE_CURVE ( 'NONE', #2120, #5801, #8057, .T. ) ;
#10543=CARTESIAN_POINT ( 'NONE',  ( 1.846138399168762101, -9.815003036200465658, 7.646096044339859787 ) ) ;
#10544=CARTESIAN_POINT ( 'NONE',  ( 2.002547531651520885, -4.532360870844412304, 11.75462648437100377 ) ) ;
#10546=CARTESIAN_POINT ( 'NONE',  ( 16.56872352241294521, 0.007512283835804314455, -0.007240717549633915451 ) ) ;
#10547=CARTESIAN_POINT ( 'NONE',  ( 1.846138399168762101, -0.4167076046094680408, -12.43476674860266940 ) ) ;
#10551=CARTESIAN_POINT ( 'NONE',  ( 2.636624412716062960, 6.973567714909310489, -14.46769361191320868 ) ) ;
#10552=ADVANCED_FACE ( 'NONE', ( #12150 ), #5273, .F. ) ;
#10553=ORIENTED_EDGE ( 'NONE', *, *, #548, .T. ) ;
#10556=ORIENTED_EDGE ( 'NONE', *, *, #11389, .T. ) ;
#10562=CARTESIAN_POINT ( 'NONE',  ( 0.4862570985993235340, -8.769551628660812170, 10.79774104611370333 ) ) ;
#10563=VECTOR ( 'NONE', #1966, 1000.000000000000227 ) ;
#10564=CARTESIAN_POINT ( 'NONE',  ( 3.950837973638676281, -14.41405733518061716, 1.958075594453740687 ) ) ;
#10567=DIRECTION ( 'NONE',  ( -1.000000000000000000, -0.000000000000000000, -0.000000000000000000 ) ) ;
#10570=EDGE_CURVE ( 'NONE', #10770, #3191, #7148, .T. ) ;
#10573=CARTESIAN_POINT ( 'NONE',  ( 1.846138399168762101, -11.95493567637848109, -3.446241763653124401 ) ) ;
#10574=CARTESIAN_POINT ( 'NONE',  ( 0.3058872367615226295, 11.46514199369368825, -7.578326039752480092 ) ) ;
#10575=ORIENTED_EDGE ( 'NONE', *, *, #15649, .T. ) ;
#10578=ORIENTED_EDGE ( 'NONE', *, *, #10570, .F. ) ;
#10580=ORIENTED_EDGE ( 'NONE', *, *, #1398, .T. ) ;
#10582=CARTESIAN_POINT ( 'NONE',  ( 0.3145734862173198421, -7.825584895511444650, -11.29227530924455003 ) ) ;
#10584=CARTESIAN_POINT ( 'NONE',  ( 0.3137051932979757485, 7.698472063774634222, -11.37800749014122736 ) ) ;
#10587=CARTESIAN_POINT ( 'NONE',  ( 3.950837973638675393, -6.888253895133384930, 12.81214529934972823 ) ) ;
#10589=CARTESIAN_POINT ( 'NONE',  ( 16.57210152137263393, -0.003862718596009370557, 0.01402404281923043221 ) ) ;
#10590=CARTESIAN_POINT ( 'NONE',  ( 0.3720661004400037664, -8.694226082900666341, 10.73619472937699015 ) ) ;
#10592=CARTESIAN_POINT ( 'NONE',  ( 1.254009781011254265, 9.426200207651111995, 11.25324419414182664 ) ) ;
#10593=B_SPLINE_CURVE_WITH_KNOTS ( 'NONE', 3,
 ( #18598, #1016, #6857, #1661, #17081, #9899 ),
 .UNSPECIFIED., .F., .F.,
 ( 4, 2, 4 ),
 ( 3.229102830436655475E-17, 0.0001825746017570572058, 0.0003651492035140821565 ),
 .UNSPECIFIED. ) ;
#10599=CARTESIAN_POINT ( 'NONE',  ( 1.847380140988739594, 7.402792205949101145, 10.00162556679653214 ) ) ;
#10606=EDGE_LOOP ( 'NONE', ( #8826, #18831, #7899, #12936 ) ) ;
#10612=CARTESIAN_POINT ( 'NONE',  ( 1.846138399168762101, 4.238866729160568170, -11.69739621335917690 ) ) ;
#10613=CARTESIAN_POINT ( 'NONE',  ( 1.562796894703937678, 0.000000000000000000, 0.000000000000000000 ) ) ;
#10617=FACE_OUTER_BOUND ( 'NONE', #3546, .T. ) ;
#10618=CARTESIAN_POINT ( 'NONE',  ( 16.56872352241294521, -0.01033355228142402750, 0.001442253899401767583 ) ) ;
#10619=LINE ( 'NONE', #14708, #16338 ) ;
#10620=CARTESIAN_POINT ( 'NONE',  ( 0.3148208552358988666, 13.13564827777588917, 4.026279359288469806 ) ) ;
#10623=CARTESIAN_POINT ( 'NONE',  ( 0.3095370825347224519, 11.38092634279628790, 7.700448427571914500 ) ) ;
#10627=CARTESIAN_POINT ( 'NONE',  ( 16.56782317627811096, -0.008141063682853442660, -0.005492611183757281634 ) ) ;
#10629=EDGE_CURVE ( 'NONE', #16167, #12510, #8711, .T. ) ;
#10630=VERTEX_POINT ( 'NONE', #17003 ) ;
#10631=CARTESIAN_POINT ( 'NONE',  ( 2.002547531651519996, -0.6781519942170860515, -12.57989064830760206 ) ) ;
#10637=CARTESIAN_POINT ( 'NONE',  ( 0.3939822652208094800, -7.545099438011941828, -11.57634296752776137 ) ) ;
#10638=CARTESIAN_POINT ( 'NONE',  ( 0.3308579732647051186, 3.680601586799872482, 13.25341063505876882 ) ) ;
#10642=CARTESIAN_POINT ( 'NONE',  ( 1.845755665166725068, 12.43231320373361193, 0.4784952423728983106 ) ) ;
#10643=CARTESIAN_POINT ( 'NONE',  ( 1.846138399168762989, -4.238866729160486457, 11.69739621335920710 ) ) ;
#10644=DIRECTION ( 'NONE',  ( 0.000000000000000000, 0.000000000000000000, 1.000000000000000000 ) ) ;
#10647=CARTESIAN_POINT ( 'NONE',  ( 0.4862570985993235340, -12.97920246947883172, 5.003653737315437944 ) ) ;
#10653=EDGE_CURVE ( 'NONE', #10095, #8886, #11902, .T. ) ;
#10669=CARTESIAN_POINT ( 'NONE',  ( 1.254255976357308233, 13.61551404021196277, 5.487601330834896096 ) ) ;
#10670=CARTESIAN_POINT ( 'NONE',  ( 16.56679352167444819, -0.008252760440870216679, 0.004277682826583264174 ) ) ;
#10675=EDGE_CURVE ( 'NONE', #4457, #12775, #15543, .T. ) ;
#10680=ORIENTED_EDGE ( 'NONE', *, *, #3412, .T. ) ;
#10681=EDGE_CURVE ( 'NONE', #78, #9622, #6891, .T. ) ;
#10682=CARTESIAN_POINT ( 'NONE',  ( 0.3150692679896004988, 4.099798979280845579, 13.11337225490253644 ) ) ;
#10685=CARTESIAN_POINT ( 'NONE',  ( 2.002547531651519996, 0.6781519942171739812, 12.57989064830759851 ) ) ;
#10686=DIRECTION ( 'NONE',  ( 0.000000000000000000, 0.000000000000000000, 1.000000000000000000 ) ) ;
#10688=CARTESIAN_POINT ( 'NONE',  ( 0.4754618798421167414, 7.564402563418470393, 11.68486377711969126 ) ) ;
#10690=CARTESIAN_POINT ( 'NONE',  ( 1.254009781011994340, -1.011465182608154434, -14.64464726212624690 ) ) ;
#10693=CARTESIAN_POINT ( 'NONE',  ( 2.636624412714236865, 0.000000000000000000, 0.000000000000000000 ) ) ;
#10695=VERTEX_POINT ( 'NONE', #14592 ) ;
#10696=ORIENTED_EDGE ( 'NONE', *, *, #1753, .F. ) ;
#10699=CARTESIAN_POINT ( 'NONE',  ( 3.950837973638676281, -6.888253895133199300, -12.81214529934982949 ) ) ;
#10701=EDGE_CURVE ( 'NONE', #6249, #8937, #4143, .T. ) ;
#10702=LINE ( 'NONE', #16537, #5625 ) ;
#10703=CARTESIAN_POINT ( 'NONE',  ( 3.950837973638676281, -12.81214529934979929, 6.888253895133251703 ) ) ;
#10704=CARTESIAN_POINT ( 'NONE',  ( 3.950837973638677170, -14.31366178983255466, 2.591948120961746760 ) ) ;
#10706=CARTESIAN_POINT ( 'NONE',  ( 0.3308579732647026761, -0.5950689966505304795, 13.74211098745268522 ) ) ;
#10709=CARTESIAN_POINT ( 'NONE',  ( 0.3095370825347233956, 12.91933430393614302, -4.681152801286028620 ) ) ;
#10713=VERTEX_POINT ( 'NONE', #13254 ) ;
#10714=B_SPLINE_CURVE_WITH_KNOTS ( 'NONE', 3,
 ( #12068, #4806, #4411, #10638, #8811, #9193 ),
 .UNSPECIFIED., .F., .F.,
 ( 4, 2, 4 ),
 ( 4.063025038712889623E-17, 0.0002014099069817291640, 0.0004028198139634176704 ),
 .UNSPECIFIED. ) ;
#10715=EDGE_CURVE ( 'NONE', #14742, #11007, #13357, .T. ) ;
#10716=FACE_OUTER_BOUND ( 'NONE', #682, .T. ) ;
#10719=CARTESIAN_POINT ( 'NONE',  ( 0.3132642857406554571, 12.89240536501346313, 4.743831191224429311 ) ) ;
#10722=CARTESIAN_POINT ( 'NONE',  ( 16.56753206892534891, 0.006669401563385194548, 0.006760771273035138390 ) ) ;
#10726=CARTESIAN_POINT ( 'NONE',  ( 0.3308579732647007887, -10.76782854710821269, -8.558831104907037357 ) ) ;
#10727=CARTESIAN_POINT ( 'NONE',  ( 1.846138399168762989, 11.69739621335922308, 4.238866729160444713 ) ) ;
#10733=CARTESIAN_POINT ( 'NONE',  ( 3.950837973638676281, -14.41405733518059229, -1.958075594453940971 ) ) ;
#10734=B_SPLINE_CURVE_WITH_KNOTS ( 'NONE', 3,
 ( #6169, #7996, #12001, #5111, #6553, #3673 ),
 .UNSPECIFIED., .F., .F.,
 ( 4, 2, 4 ),
 ( 0.000000000000000000, 0.001656992708823640335, 0.003313985417647279802 ),
 .UNSPECIFIED. ) ;
#10738=CARTESIAN_POINT ( 'NONE',  ( 16.56822296793089322, -0.01011126603341077138, 0.0007467251401298242519 ) ) ;
#10740=ORIENTED_EDGE ( 'NONE', *, *, #3044, .T. ) ;
#10744=CARTESIAN_POINT ( 'NONE',  ( 0.3145729642390365788, 10.93201268464384768, -8.321438378985135387 ) ) ;
#10747=ORIENTED_EDGE ( 'NONE', *, *, #10681, .F. ) ;
#10760=CARTESIAN_POINT ( 'NONE',  ( 1.918918678667044686, -10.48466773720556766, -6.832809802519125064 ) ) ;
#10764=CARTESIAN_POINT ( 'NONE',  ( 8.438534575730034959, -4.221456476902624821, -5.415535776177568650 ) ) ;
#10768=ORIENTED_EDGE ( 'NONE', *, *, #12164, .F. ) ;
#10770=VERTEX_POINT ( 'NONE', #9057 ) ;
#10772=ORIENTED_EDGE ( 'NONE', *, *, #6124, .T. ) ;
#10778=CARTESIAN_POINT ( 'NONE',  ( 2.747332970342022840, 7.555624153089646633, 14.49942876448594831 ) ) ;
#10779=CARTESIAN_POINT ( 'NONE',  ( 2.747332970342022840, 16.17136872824898575, 2.409922051470737348 ) ) ;
#10793=B_SPLINE_CURVE_WITH_KNOTS ( 'NONE', 3,
 ( #16252, #7373, #13471, #3134, #293, #14710, #13183, #8980, #1921, #10620, #1722, #99, #6123 ),
 .UNSPECIFIED., .F., .F.,
 ( 4, 3, 3, 3, 4 ),
 ( 1.734723475976807094E-18, 0.0002299780670421060647, 0.0004599561239687893072, 0.0006896788984287890393, 0.0009194956271626404968 ),
 .UNSPECIFIED. ) ;
#10798=CARTESIAN_POINT ( 'NONE',  ( 0.4862570985993235340, 7.559321496869593204, -11.67702470553357053 ) ) ;
#10799=ORIENTED_EDGE ( 'NONE', *, *, #875, .T. ) ;
#10800=CARTESIAN_POINT ( 'NONE',  ( 1.846138399168762989, -4.238866729160486457, 11.69739621335920710 ) ) ;
#10804=CARTESIAN_POINT ( 'NONE',  ( 0.4862570985993235340, -10.79774104611379215, 8.769551628660700260 ) ) ;
#10806=CARTESIAN_POINT ( 'NONE',  ( 3.353306896162455697, -1.348936822032921423, 13.88482890973696016 ) ) ;
#10811=ORIENTED_EDGE ( 'NONE', *, *, #143, .F. ) ;
#10814=EDGE_CURVE ( 'NONE', #15883, #9927, #1848, .T. ) ;
#10820=CARTESIAN_POINT ( 'NONE',  ( 16.57210152137263393, 0.003862718596009469003, -0.01402404281923040792 ) ) ;
#10824=AXIS2_PLACEMENT_3D ( 'NONE', #6242, #17618, #17513 ) ;
#10826=EDGE_CURVE ( 'NONE', #10770, #1445, #3508, .T. ) ;
#10827=PRODUCT_DEFINITION_FORMATION_WITH_SPECIFIED_SOURCE ( 'ANY', '', #206, .NOT_KNOWN. ) ;
#10828=B_SPLINE_CURVE_WITH_KNOTS ( 'NONE', 3,
 ( #12829, #18477, #11232, #8355, #14172, #1078, #2419, #8269, #14084, #18569, #990, #6825, #15425 ),
 .UNSPECIFIED., .F., .F.,
 ( 4, 3, 3, 3, 4 ),
 ( 8.673617379884035472E-19, 0.0002299804304191491514, 0.0004599608082120254429, 0.0006467586077648011496, 0.0008336169836825998080 ),
 .UNSPECIFIED. ) ;
#10838=CARTESIAN_POINT ( 'NONE',  ( 0.4754618798421162973, -13.45049478164062329, 3.583352865732616355 ) ) ;
#10842=CARTESIAN_POINT ( 'NONE',  ( 1.847247051441591514, -0.1676840720646167182, 12.44188156437794213 ) ) ;
#10843=VERTEX_POINT ( 'NONE', #15176 ) ;
#10853=CARTESIAN_POINT ( 'NONE',  ( 16.57210152137263393, -0.008007331252332796495, -0.01214401161737526519 ) ) ;
#10854=DIRECTION ( 'NONE',  ( 0.000000000000000000, 0.000000000000000000, 1.000000000000000000 ) ) ;
#10857=CARTESIAN_POINT ( 'NONE',  ( 3.950837973638668288, 0.000000000000000000, 0.000000000000000000 ) ) ;
#10858=CARTESIAN_POINT ( 'NONE',  ( 16.57605080000000086, 4.769696007084728073, -1.500000000000000000 ) ) ;
#10864=B_SPLINE_CURVE_WITH_KNOTS ( 'NONE', 3,
 ( #10573, #9136, #13626, #4934, #17941, #6174, #3189, #16594, #14958, #549, #251, #4841, #7521 ),
 .UNSPECIFIED., .F., .F.,
 ( 4, 3, 3, 3, 4 ),
 ( 1.734723475976807094E-18, 0.0002299804304191480130, 0.0004599608082120234913, 0.0006467586077648008244, 0.0008336169836825994828 ),
 .UNSPECIFIED. ) ;
#10865=CARTESIAN_POINT ( 'NONE',  ( 0.4862570985993235340, -11.67702470553359539, -7.559321496869553236 ) ) ;
#10866=CARTESIAN_POINT ( 'NONE',  ( 8.438534575730034959, 5.688336279099046600, 3.845978796786057696 ) ) ;
#10870=ORIENTED_EDGE ( 'NONE', *, *, #4017, .F. ) ;
#10873=ADVANCED_FACE ( 'NONE', ( #10883 ), #17808, .T. ) ;
#10874=B_SPLINE_CURVE_WITH_KNOTS ( 'NONE', 3,
 ( #10905, #1024, #3716, #13844, #6689, #5148 ),
 .UNSPECIFIED., .F., .F.,
 ( 4, 2, 4 ),
 ( 2.462833906345087556E-18, 0.0001828790815886951863, 0.0003657581631773856022 ),
 .UNSPECIFIED. ) ;
#10876=AXIS2_PLACEMENT_3D ( 'NONE', #14316, #1214, #18697 ) ;
#10883=FACE_OUTER_BOUND ( 'NONE', #8963, .T. ) ;
#10885=CARTESIAN_POINT ( 'NONE',  ( 0.4385251269669940277, 8.732456510146231921, -10.76637725024242442 ) ) ;
#10887=ORIENTED_EDGE ( 'NONE', *, *, #15898, .F. ) ;
#10893=CARTESIAN_POINT ( 'NONE',  ( 3.074695600507134419, -7.366518011945905720, -13.70113613813221676 ) ) ;
#10898=CARTESIAN_POINT ( 'NONE',  ( 0.8740764193772003754, 13.83508774436055511, -3.609949042658134211 ) ) ;
#10902=FACE_OUTER_BOUND ( 'NONE', #5000, .T. ) ;
#10905=CARTESIAN_POINT ( 'NONE',  ( 1.846138399168762101, -7.646096044339961040, 9.815003036200383946 ) ) ;
#10917=B_SPLINE_CURVE_WITH_KNOTS ( 'NONE', 3,
 ( #5910, #4210, #5528, #7367, #4497, #14612, #10027, #3031, #17483, #11565, #2749, #8879, #11658 ),
 .UNSPECIFIED., .F., .F.,
 ( 4, 3, 3, 3, 4 ),
 ( 3.878959614448864246E-18, 0.0002299780670421054142, 0.0004599561239687919093, 0.0006896788984287899067, 0.0009194956271626406052 ),
 .UNSPECIFIED. ) ;
#10921=EDGE_CURVE ( 'NONE', #3029, #4457, #14195, .T. ) ;
#10922=ORIENTED_EDGE ( 'NONE', *, *, #11488, .T. ) ;
#10923=CARTESIAN_POINT ( 'NONE',  ( 0.4862570985993235340, -8.769551628660812170, 10.79774104611370333 ) ) ;
#10926=VECTOR ( 'NONE', #16413, 1000.000000000000114 ) ;
#10931=CARTESIAN_POINT ( 'NONE',  ( 2.002547531651519996, 3.242439124566821818, -12.17374746633574745 ) ) ;
#10932=( BOUNDED_SURFACE ( )  B_SPLINE_SURFACE ( 3, 1, ( 
 ( #319, #17718 ),
 ( #9010, #2970 ),
 ( #4419, #5940 ),
 ( #13402, #17420 ) ),
 .UNSPECIFIED., .F., .F., .T. ) 
 B_SPLINE_SURFACE_WITH_KNOTS ( ( 4, 4 ),
 ( 2, 2 ),
 ( 0.000000000000000000, 1.000000000000000000 ),
 ( 0.000000000000000000, 1.000000000000000000 ),
 .UNSPECIFIED. ) 
 GEOMETRIC_REPRESENTATION_ITEM ( )  RATIONAL_B_SPLINE_SURFACE ( (
 ( 1.000000000000000000, 1.000000000000000000),
 ( 0.9933953342250438912, 0.8357391271907739227),
 ( 0.9933953342250438912, 0.8357391271907739227),
 ( 1.000000000000000000, 1.000000000000000000) ) ) 
 REPRESENTATION_ITEM ( '' )  SURFACE ( )  );
#10933=CARTESIAN_POINT ( 'NONE',  ( 0.3137051932979809665, -3.805684345189881856, 13.20008686438104739 ) ) ;
#10934=CARTESIAN_POINT ( 'NONE',  ( 2.002547531651519996, -11.75462648437105173, 4.532360870844282630 ) ) ;
#10935=ORIENTED_EDGE ( 'NONE', *, *, #15449, .F. ) ;
#10942=VERTEX_POINT ( 'NONE', #15618 ) ;
#10943=DIRECTION ( 'NONE',  ( 1.000000000000000000, 0.000000000000000000, 0.000000000000000000 ) ) ;
#10945=ORIENTED_EDGE ( 'NONE', *, *, #2090, .T. ) ;
#10947=CARTESIAN_POINT ( 'NONE',  ( 16.58200780006414732, -0.01041078477703985539, 0.004047297414157853025 ) ) ;
#10958=B_SPLINE_CURVE_WITH_KNOTS ( 'NONE', 3,
 ( #5642, #6913, #18468, #7007, #8717, #5464, #11498, #12822, #3948, #5738, #14353, #1259, #15597 ),
 .UNSPECIFIED., .F., .F.,
 ( 4, 3, 3, 3, 4 ),
 ( 3.878959614448864246E-18, 0.0002299780670421063358, 0.0004599561239687880061, 0.0006896788984287903403, 0.0009194956271626402800 ),
 .UNSPECIFIED. ) ;
#10964=B_SPLINE_CURVE_WITH_KNOTS ( 'NONE', 3,
 ( #10733, #411, #608, #7780 ),
 .UNSPECIFIED., .F., .F.,
 ( 4, 4 ),
 ( 0.000000000000000000, 0.002004993803842712932 ),
 .UNSPECIFIED. ) ;
#10966=( BOUNDED_SURFACE ( )  B_SPLINE_SURFACE ( 3, 1, ( 
 ( #3375, #9214 ),
 ( #15415, #12629 ),
 ( #8346, #11397 ),
 ( #15321, #16850 ) ),
 .UNSPECIFIED., .F., .F., .T. ) 
 B_SPLINE_SURFACE_WITH_KNOTS ( ( 4, 4 ),
 ( 2, 2 ),
 ( 0.000000000000000000, 1.000000000000000000 ),
 ( 0.000000000000000000, 1.000000000000000000 ),
 .UNSPECIFIED. ) 
 GEOMETRIC_REPRESENTATION_ITEM ( )  RATIONAL_B_SPLINE_SURFACE ( (
 ( 1.000000000000000000, 1.000000000000000000),
 ( 0.9933953342250438912, 0.8357391271907739227),
 ( 0.9933953342250438912, 0.8357391271907739227),
 ( 1.000000000000000000, 1.000000000000000000) ) ) 
 REPRESENTATION_ITEM ( '' )  SURFACE ( )  );
#10969=CARTESIAN_POINT ( 'NONE',  ( 1.918921323896322750, -12.49850046818174398, -0.6349083173281465653 ) ) ;
#10970=CARTESIAN_POINT ( 'NONE',  ( 1.846524061778021419, -11.93805390544203426, 3.506196582971057740 ) ) ;
#10974=CARTESIAN_POINT ( 'NONE',  ( 0.8740764193769885448, -7.708542792189400750, -12.04241474978016058 ) ) ;
#10982=ORIENTED_EDGE ( 'NONE', *, *, #3294, .T. ) ;
#10983=CARTESIAN_POINT ( 'NONE',  ( 0.000000000000000000, 6.799999999999999822, 0.000000000000000000 ) ) ;
#10984=CARTESIAN_POINT ( 'NONE',  ( 3.950837973638668288, 0.000000000000000000, 0.000000000000000000 ) ) ;
#10987=CARTESIAN_POINT ( 'NONE',  ( 16.57778382496167424, -0.01018821665058842162, -0.01092721432669105028 ) ) ;
#10992=CARTESIAN_POINT ( 'NONE',  ( 2.320521194581854907, 15.64520804578206281, -1.795798718312993758 ) ) ;
#10994=B_SPLINE_CURVE_WITH_KNOTS ( 'NONE', 3,
 ( #13371, #13559, #16244, #3425 ),
 .UNSPECIFIED., .F., .F.,
 ( 4, 4 ),
 ( 0.000000000000000000, 0.002004993803841946618 ),
 .UNSPECIFIED. ) ;
#10996=DIRECTION ( 'NONE',  ( 0.000000000000000000, 0.000000000000000000, 1.000000000000000000 ) ) ;
#11000=CARTESIAN_POINT ( 'NONE',  ( 1.845755665166727066, -4.296872077620760066, 11.67596932341233007 ) ) ;
#11001=EDGE_CURVE ( 'NONE', #8116, #8373, #16452, .T. ) ;
#11002=EDGE_LOOP ( 'NONE', ( #5956, #11010, #15494, #12515 ) ) ;
#11006=CARTESIAN_POINT ( 'NONE',  ( 16.56753206892534891, 0.009389754735541551434, -0.001421777558676823056 ) ) ;
#11007=VERTEX_POINT ( 'NONE', #8555 ) ;
#11010=ORIENTED_EDGE ( 'NONE', *, *, #8602, .T. ) ;
#11017=ADVANCED_FACE ( 'NONE', ( #17067 ), #13087, .F. ) ;
#11021=CARTESIAN_POINT ( 'NONE',  ( 0.4862570985993235340, -11.67702470553370553, 7.559321496869385371 ) ) ;
#11024=CARTESIAN_POINT ( 'NONE',  ( 16.56782317627811096, -0.007739510688079557534, -0.006045301465876337828 ) ) ;
#11030=CARTESIAN_POINT ( 'NONE',  ( 3.074695600507132198, -14.01296402267896823, -6.754521329825003306 ) ) ;
#11032=VERTEX_POINT ( 'NONE', #4446 ) ;
#11033=CARTESIAN_POINT ( 'NONE',  ( 16.57778382496167424, -0.01482878558584568157, -0.001819584982832054632 ) ) ;
#11036=CARTESIAN_POINT ( 'NONE',  ( 0.4754618798421171855, -11.68486377711960778, -7.564402563418600067 ) ) ;
#11037=B_SPLINE_CURVE_WITH_KNOTS ( 'NONE', 3,
 ( #18624, #5527, #15759, #17780, #3427, #6117, #482, #14994, #6406, #14804, #13272, #288, #10800 ),
 .UNSPECIFIED., .F., .F.,
 ( 4, 3, 3, 3, 4 ),
 ( 2.168404344971008868E-18, 0.0002299804304191472269, 0.0004599608082120226239, 0.0006467586077647999570, 0.0008336169836825976396 ),
 .UNSPECIFIED. ) ;
#11039=FACE_OUTER_BOUND ( 'NONE', #9530, .T. ) ;
#11043=CARTESIAN_POINT ( 'NONE',  ( 2.002547531651519996, 7.942910686618313676, -9.778737580845612953 ) ) ;
#11047=CARTESIAN_POINT ( 'NONE',  ( 2.002547531651519996, -9.778737580845639599, -7.942910686618280813 ) ) ;
#11048=B_SPLINE_CURVE_WITH_KNOTS ( 'NONE', 3,
 ( #4144, #11135, #1266, #18656, #11505, #15604 ),
 .UNSPECIFIED., .F., .F.,
 ( 4, 2, 4 ),
 ( 0.000000000000000000, 0.0002017457492448075543, 0.0004034914984896151085 ),
 .UNSPECIFIED. ) ;
#11050=EDGE_CURVE ( 'NONE', #4529, #12695, #8670, .T. ) ;
#11052=ORIENTED_EDGE ( 'NONE', *, *, #8315, .T. ) ;
#11054=EDGE_LOOP ( 'NONE', ( #10578, #13632, #12744, #18501, #4538, #16577, #12107, #6449, #2386, #4958, #5138, #9445, #8868, #14064, #10982, #14503, #6226, #4632, #2360, #1584, #14515, #14459, #17429, #3318, #15846, #499, #12800, #5655, #2880, #9088, #6447, #14328, #5676, #10216, #12487, #13980, #6084, #14803, #6685, #17130, #708, #15255, #6807, #6445, #1219, #6159, #5748, #5460, #17073, #10409, #9168, #3622, #9551, #4356, #7647, #15412, #2440, #12400, #17821, #3426, #11531, #8288, #924, #17953 ) ) ;
#11055=ORIENTED_EDGE ( 'NONE', *, *, #6124, .F. ) ;
#11059=CARTESIAN_POINT ( 'NONE',  ( 1.861628059977342264, -3.332996951203546665, -12.00316790821105073 ) ) ;
#11065=AXIS2_PLACEMENT_3D ( 'NONE', #3821, #5346, #9647 ) ;
#11067=FACE_OUTER_BOUND ( 'NONE', #4311, .T. ) ;
#11072=ORIENTED_EDGE ( 'NONE', *, *, #18161, .F. ) ;
#11073=ORIENTED_EDGE ( 'NONE', *, *, #3713, .T. ) ;
#11074=( BOUNDED_SURFACE ( )  B_SPLINE_SURFACE ( 3, 1, ( 
 ( #8300, #6686 ),
 ( #16808, #13754 ),
 ( #11082, #8031 ),
 ( #18151, #13933 ) ),
 .UNSPECIFIED., .F., .F., .T. ) 
 B_SPLINE_SURFACE_WITH_KNOTS ( ( 4, 4 ),
 ( 2, 2 ),
 ( 0.000000000000000000, 1.000000000000000000 ),
 ( 0.000000000000000000, 1.000000000000000000 ),
 .UNSPECIFIED. ) 
 GEOMETRIC_REPRESENTATION_ITEM ( )  RATIONAL_B_SPLINE_SURFACE ( (
 ( 1.000000000000000000, 1.000000000000000000),
 ( 0.7792777138730160313, 0.9689936506012927220),
 ( 0.7792777138730160313, 0.9689936506012927220),
 ( 1.000000000000000000, 1.000000000000000000) ) ) 
 REPRESENTATION_ITEM ( '' )  SURFACE ( )  );
#11079=CARTESIAN_POINT ( 'NONE',  ( 8.522092701127531811, -0.3779863304870734741, -6.946128462138600135 ) ) ;
#11080=CARTESIAN_POINT ( 'NONE',  ( 1.846524061778018977, -7.597197846158149304, 9.853584647934361840 ) ) ;
#11081=ORIENTED_EDGE ( 'NONE', *, *, #6662, .F. ) ;
#11082=CARTESIAN_POINT ( 'NONE',  ( 16.57778382496167424, 0.007244066302947695102, -0.01306626476309380794 ) ) ;
#11092=ORIENTED_EDGE ( 'NONE', *, *, #8033, .T. ) ;
#11094=CARTESIAN_POINT ( 'NONE',  ( 2.747332970342022840, 16.12459247543626617, 2.705255688517901103 ) ) ;
#11099=CARTESIAN_POINT ( 'NONE',  ( 8.522092701127531811, -6.489356537178172957, -2.505958102592690473 ) ) ;
#11108=AXIS2_PLACEMENT_3D ( 'NONE', #4523, #18849, #18747 ) ;
#11111=CARTESIAN_POINT ( 'NONE',  ( 16.56679352167444819, -0.006618561353599251677, 0.006526964904752932846 ) ) ;
#11112=DIRECTION ( 'NONE',  ( 0.000000000000000000, 0.000000000000000000, 1.000000000000000000 ) ) ;
#11113=ORIENTED_EDGE ( 'NONE', *, *, #7745, .F. ) ;
#11118=ORIENTED_EDGE ( 'NONE', *, *, #7501, .F. ) ;
#11122=CARTESIAN_POINT ( 'NONE',  ( 0.3145729642390391878, -8.321438378985172690, -10.93201268464381748 ) ) ;
#11123=ADVANCED_FACE ( 'NONE', ( #14859 ), #15049, .F. ) ;
#11132=DIRECTION ( 'NONE',  ( -1.000000000000000000, -0.000000000000000000, -0.000000000000000000 ) ) ;
#11134=EDGE_CURVE ( 'NONE', #14697, #9064, #15512, .T. ) ;
#11135=CARTESIAN_POINT ( 'NONE',  ( 0.3132635586635980074, -10.79541209008109703, 8.495712071659360376 ) ) ;
#11136=CARTESIAN_POINT ( 'NONE',  ( 3.950837973638675393, 10.51028938476217967, 10.05648675950130233 ) ) ;
#11139=ORIENTED_EDGE ( 'NONE', *, *, #9413, .T. ) ;
#11142=AXIS2_PLACEMENT_3D ( 'NONE', #10984, #843, #2102 ) ;
#11143=ORIENTED_EDGE ( 'NONE', *, *, #5194, .T. ) ;
#11146=( BOUNDED_SURFACE ( )  B_SPLINE_SURFACE ( 3, 1, ( 
 ( #16114, #8847 ),
 ( #11278, #1580 ),
 ( #12598, #5342 ),
 ( #9814, #2457 ) ),
 .UNSPECIFIED., .F., .F., .T. ) 
 B_SPLINE_SURFACE_WITH_KNOTS ( ( 4, 4 ),
 ( 2, 2 ),
 ( 0.000000000000000000, 1.000000000000000000 ),
 ( 0.000000000000000000, 1.000000000000000000 ),
 .UNSPECIFIED. ) 
 GEOMETRIC_REPRESENTATION_ITEM ( )  RATIONAL_B_SPLINE_SURFACE ( (
 ( 1.000000000000000000, 1.000000000000000000),
 ( 0.9933953342250438912, 0.8357391271907739227),
 ( 0.9933953342250438912, 0.8357391271907739227),
 ( 1.000000000000000000, 1.000000000000000000) ) ) 
 REPRESENTATION_ITEM ( '' )  SURFACE ( )  );
#11148=B_SPLINE_CURVE_WITH_KNOTS ( 'NONE', 3,
 ( #6072, #142, #4546, #17443 ),
 .UNSPECIFIED., .F., .F.,
 ( 4, 4 ),
 ( 1.811104479740059440E-17, 0.003005512676784850932 ),
 .UNSPECIFIED. ) ;
#11156=CARTESIAN_POINT ( 'NONE',  ( 16.56679352167444819, -0.009170718284672552470, -0.001518074900130618379 ) ) ;
#11157=DIRECTION ( 'NONE',  ( -0.7635533937278214944, 0.3966532189476597581, 0.5095610256143870975 ) ) ;
#11158=CARTESIAN_POINT ( 'NONE',  ( 0.3058872367615230181, -12.87003593440631732, 4.821066432589277362 ) ) ;
#11161=ORIENTED_EDGE ( 'NONE', *, *, #10399, .T. ) ;
#11163=ORIENTED_EDGE ( 'NONE', *, *, #15765, .F. ) ;
#11164=AXIS2_PLACEMENT_3D ( 'NONE', #3380, #13423, #3578 ) ;
#11168=CARTESIAN_POINT ( 'NONE',  ( 3.664313757352974488, -12.97355833021536498, -5.926151963190507743 ) ) ;
#11171=CARTESIAN_POINT ( 'NONE',  ( 1.846613052777651198, -7.035606253495386930, 10.26230975746757146 ) ) ;
#11172=VERTEX_POINT ( 'NONE', #541 ) ;
#11173=CARTESIAN_POINT ( 'NONE',  ( 0.4862570985993235340, 13.89016912371017476, -0.7479633556562934604 ) ) ;
#11180=CARTESIAN_POINT ( 'NONE',  ( 16.56679352167444819, 0.008311568981097982450, 0.004162264567718830001 ) ) ;
#11183=EDGE_CURVE ( 'NONE', #15858, #16388, #3430, .T. ) ;
#11186=( BOUNDED_SURFACE ( )  B_SPLINE_SURFACE ( 3, 1, ( 
 ( #4705, #16271 ),
 ( #10820, #3352 ),
 ( #506, #1937 ),
 ( #6335, #17993 ) ),
 .UNSPECIFIED., .F., .F., .F. ) 
 B_SPLINE_SURFACE_WITH_KNOTS ( ( 4, 4 ),
 ( 2, 2 ),
 ( 0.000000000000000000, 1.000000000000000000 ),
 ( 0.000000000000000000, 1.000000000000000000 ),
 .UNSPECIFIED. ) 
 GEOMETRIC_REPRESENTATION_ITEM ( )  RATIONAL_B_SPLINE_SURFACE ( (
 ( 1.000000000000000000, 1.000000000000000000),
 ( 0.7792777138730160313, 0.9689936506012927220),
 ( 0.7792777138730160313, 0.9689936506012927220),
 ( 1.000000000000000000, 1.000000000000000000) ) ) 
 REPRESENTATION_ITEM ( '' )  SURFACE ( )  );
#11188=ORIENTED_EDGE ( 'NONE', *, *, #6552, .T. ) ;
#11189=CARTESIAN_POINT ( 'NONE',  ( 16.57778382496167424, 0.006312874906843677844, -0.01354073047775769707 ) ) ;
#11190=EDGE_CURVE ( 'NONE', #18880, #7816, #12591, .T. ) ;
#11199=CARTESIAN_POINT ( 'NONE',  ( 3.950837973638676281, 2.591948120962007884, -14.31366178983250670 ) ) ;
#11203=VECTOR ( 'NONE', #14527, 1000.000000000000114 ) ;
#11204=VECTOR ( 'NONE', #8287, 1000.000000000000114 ) ;
#11205=( NAMED_UNIT ( * ) SI_UNIT ( $, .STERADIAN. ) SOLID_ANGLE_UNIT ( ) );
#11206=EDGE_CURVE ( 'NONE', #7454, #13762, #10060, .T. ) ;
#11208=DIRECTION ( 'NONE',  ( 0.7635533937278216055, 0.3620487483322444855, 0.5347026451755978460 ) ) ;
#11219=ORIENTED_EDGE ( 'NONE', *, *, #1340, .F. ) ;
#11222=CARTESIAN_POINT ( 'NONE',  ( 3.950837973638668288, 0.000000000000000000, 0.000000000000000000 ) ) ;
#11228=PLANE ( 'NONE',  #16646 ) ;
#11229=CARTESIAN_POINT ( 'NONE',  ( 16.57605080000000086, 0.000000000000000000, 1.500000000000000000 ) ) ;
#11232=CARTESIAN_POINT ( 'NONE',  ( 1.846955891736120181, -4.094751675596620011, -11.74973605926568077 ) ) ;
#11234=CARTESIAN_POINT ( 'NONE',  ( 0.4754618798421162973, 13.45049478164060019, 3.583352865732715387 ) ) ;
#11239=ORIENTED_EDGE ( 'NONE', *, *, #16542, .F. ) ;
#11240=ORIENTED_EDGE ( 'NONE', *, *, #2853, .T. ) ;
#11243=CIRCLE ( 'NONE', #14576, 16.06066017081991149 ) ;
#11244=CARTESIAN_POINT ( 'NONE',  ( 1.847426409206471831, -0.06227732482761883653, -12.44303504652092229 ) ) ;
#11245=CARTESIAN_POINT ( 'NONE',  ( 0.3720661004400037664, -10.73619472937695640, -8.694226082900707198 ) ) ;
#11248=DIRECTION ( 'NONE',  ( 0.000000000000000000, 0.000000000000000000, 1.000000000000000000 ) ) ;
#11250=CARTESIAN_POINT ( 'NONE',  ( 0.3151928479966097374, -6.943324943027912228E-05, -13.73922861026898623 ) ) ;
#11251=CARTESIAN_POINT ( 'NONE',  ( 0.3150692679895942816, -13.11337225490255776, 4.099798979280796729 ) ) ;
#11252=EDGE_CURVE ( 'NONE', #11465, #15522, #17585, .T. ) ;
#11257=EDGE_CURVE ( 'NONE', #14985, #3963, #5717, .T. ) ;
#11258=ORIENTED_EDGE ( 'NONE', *, *, #3555, .T. ) ;
#11261=( BOUNDED_SURFACE ( )  B_SPLINE_SURFACE ( 3, 1, ( 
 ( #5987, #4849 ),
 ( #12014, #6382 ),
 ( #13534, #7532 ),
 ( #7433, #11823 ) ),
 .UNSPECIFIED., .F., .F., .T. ) 
 B_SPLINE_SURFACE_WITH_KNOTS ( ( 4, 4 ),
 ( 2, 2 ),
 ( 0.000000000000000000, 1.000000000000000000 ),
 ( 0.000000000000000000, 1.000000000000000000 ),
 .UNSPECIFIED. ) 
 GEOMETRIC_REPRESENTATION_ITEM ( )  RATIONAL_B_SPLINE_SURFACE ( (
 ( 1.000000000000000000, 1.000000000000000000),
 ( 0.9933953342250436691, 0.8357391271907733676),
 ( 0.9933953342250436691, 0.8357391271907733676),
 ( 1.000000000000000000, 1.000000000000000000) ) ) 
 REPRESENTATION_ITEM ( '' )  SURFACE ( )  );
#11274=CARTESIAN_POINT ( 'NONE',  ( 1.846138399168762101, -10.30487220521574976, 6.971848976710974810 ) ) ;
#11278=CARTESIAN_POINT ( 'NONE',  ( 16.56822296793089322, 0.006547366384935510326, -0.007741272030791107074 ) ) ;
#11282=VECTOR ( 'NONE', #9806, 1000.000000000000114 ) ;
#11286=CARTESIAN_POINT ( 'NONE',  ( 3.074695600507223681, -13.70113613813211195, -7.366518011946086908 ) ) ;
#11292=CARTESIAN_POINT ( 'NONE',  ( 0.4385251269669950269, -13.84299131624728929, -0.7363879510386833749 ) ) ;
#11297=EDGE_CURVE ( 'NONE', #9839, #5025, #714, .T. ) ;
#11298=CARTESIAN_POINT ( 'NONE',  ( 0.3170788640506441158, 7.952793437297734691, -11.20690911610894958 ) ) ;
#11301=CARTESIAN_POINT ( 'NONE',  ( 1.342453679581834924, -5.476372339889922003, -13.74702459364890039 ) ) ;
#11305=VERTEX_POINT ( 'NONE', #9690 ) ;
#11309=CARTESIAN_POINT ( 'NONE',  ( 0.3150686449036065317, -8.199336701264455129, -11.02450593298027570 ) ) ;
#11313=B_SPLINE_CURVE_WITH_KNOTS ( 'NONE', 3,
 ( #16588, #13962, #1047, #10564 ),
 .UNSPECIFIED., .F., .F.,
 ( 4, 4 ),
 ( 1.914591753770035818E-17, 0.002004993803842692549 ),
 .UNSPECIFIED. ) ;
#11315=ADVANCED_FACE ( 'NONE', ( #5553 ), #17498, .F. ) ;
#11319=EDGE_CURVE ( 'NONE', #7003, #8226, #9590, .T. ) ;
#11322=CARTESIAN_POINT ( 'NONE',  ( 2.636624412714236865, 0.000000000000000000, 0.000000000000000000 ) ) ;
#11326=( NAMED_UNIT ( * ) PLANE_ANGLE_UNIT ( ) SI_UNIT ( $, .RADIAN. ) );
#11327=ORIENTED_EDGE ( 'NONE', *, *, #11252, .F. ) ;
#11328=ORIENTED_EDGE ( 'NONE', *, *, #11830, .T. ) ;
#11332=CARTESIAN_POINT ( 'NONE',  ( 0.4384471787762835859, 13.39294437382618419, 3.577367180593594043 ) ) ;
#11333=CARTESIAN_POINT ( 'NONE',  ( 16.56872352241294521, 0.01027347319884441834, -0.001821578298044677175 ) ) ;
#11338=CONICAL_SURFACE ( 'NONE', #3693, 14.54644660717763927, 0.8559913436420816257 ) ;
#11339=CARTESIAN_POINT ( 'NONE',  ( 0.3137051932979775248, -0.4596302728638797519, -13.73004976592202553 ) ) ;
#11358=CARTESIAN_POINT ( 'NONE',  ( 8.522092701127531811, 2.505958102592713121, -6.489356537178164075 ) ) ;
#11360=CONICAL_SURFACE ( 'NONE', #17777, 14.54644660717763927, 0.8559913436420816257 ) ;
#11363=CARTESIAN_POINT ( 'NONE',  ( 0.3170788640506441158, -11.20690911610897800, -7.952793437297696499 ) ) ;
#11364=CARTESIAN_POINT ( 'NONE',  ( 3.074695600507753479, -6.754521329825609932, -14.01296402267891317 ) ) ;
#11366=CARTESIAN_POINT ( 'NONE',  ( 1.342453679581834924, -9.456403821038714241, -11.38190519890864039 ) ) ;
#11371=CARTESIAN_POINT ( 'NONE',  ( 16.56822296793089322, 0.01011126603341004106, 0.0007467251401288980180 ) ) ;
#11372=ORIENTED_EDGE ( 'NONE', *, *, #11050, .F. ) ;
#11373=CARTESIAN_POINT ( 'NONE',  ( 1.846138399168762101, 3.446241763653166590, -11.95493567637846866 ) ) ;
#11376=VERTEX_POINT ( 'NONE', #2686 ) ;
#11379=CARTESIAN_POINT ( 'NONE',  ( 1.847372867223025628, 12.44269075185938789, 0.1054171785006922379 ) ) ;
#11382=ADVANCED_FACE ( 'NONE', ( #12464 ), #3196, .F. ) ;
#11385=CARTESIAN_POINT ( 'NONE',  ( 16.56753206892534891, -0.008490833999798035742, 0.004253784598196731770 ) ) ;
#11388=CARTESIAN_POINT ( 'NONE',  ( 1.562796894703937678, 0.000000000000000000, 1.500000000000000000 ) ) ;
#11389=EDGE_CURVE ( 'NONE', #15773, #9839, #10516, .T. ) ;
#11391=CARTESIAN_POINT ( 'NONE',  ( 0.8740779401508862456, -13.31469722824359891, 5.211551231203810808 ) ) ;
#11392=VERTEX_POINT ( 'NONE', #14546 ) ;
#11394=CARTESIAN_POINT ( 'NONE',  ( 0.4385251269669978580, 10.76637725024251857, 8.732456510146114681 ) ) ;
#11397=CARTESIAN_POINT ( 'NONE',  ( 0.3058872367615230181, -13.72992299905060598, 0.6080468242580479021 ) ) ;
#11400=ADVANCED_FACE ( 'NONE', ( #4240 ), #12306, .T. ) ;
#11407=EDGE_CURVE ( 'NONE', #8226, #11439, #13826, .T. ) ;
#11409=CARTESIAN_POINT ( 'NONE',  ( 16.56753206892534891, 0.004368917149005337522, 0.008432171035096464387 ) ) ;
#11416=ORIENTED_EDGE ( 'NONE', *, *, #18690, .T. ) ;
#11421=ORIENTED_EDGE ( 'NONE', *, *, #16253, .T. ) ;
#11422=CARTESIAN_POINT ( 'NONE',  ( 16.56782317627811096, 0.008141063682853480823, -0.005492611183758445634 ) ) ;
#11424=CARTESIAN_POINT ( 'NONE',  ( 8.438534575730034959, -5.415535776177489602, -4.221456476902725186 ) ) ;
#11430=FACE_OUTER_BOUND ( 'NONE', #15386, .T. ) ;
#11436=ADVANCED_FACE ( 'NONE', ( #17418 ), #6524, .T. ) ;
#11437=ORIENTED_EDGE ( 'NONE', *, *, #5261, .F. ) ;
#11439=VERTEX_POINT ( 'NONE', #10345 ) ;
#11443=CARTESIAN_POINT ( 'NONE',  ( 0.3150686449036038672, 7.951193823202562072, -11.20479228691389118 ) ) ;
#11445=CARTESIAN_POINT ( 'NONE',  ( 2.002547531651519996, -12.17374746633575988, -3.242439124566779185 ) ) ;
#11448=CARTESIAN_POINT ( 'NONE',  ( 1.562796894703937678, 1.488975241814732168E-15, 12.15840553252917289 ) ) ;
#11450=CARTESIAN_POINT ( 'NONE',  ( 1.918921323896323639, -10.48468902844557071, 6.832782632379341692 ) ) ;
#11455=CIRCLE ( 'NONE', #10876, 14.54644660717763927 ) ;
#11458=EDGE_CURVE ( 'NONE', #12775, #15569, #11864, .T. ) ;
#11461=ORIENTED_EDGE ( 'NONE', *, *, #7041, .T. ) ;
#11462=ORIENTED_EDGE ( 'NONE', *, *, #5498, .F. ) ;
#11463=B_SPLINE_CURVE_WITH_KNOTS ( 'NONE', 3,
 ( #2613, #4061, #15808, #12659, #5665, #17244, #13037, #18670, #7122, #9979, #8551, #1002, #12941 ),
 .UNSPECIFIED., .F., .F.,
 ( 4, 3, 3, 3, 4 ),
 ( 3.035766082959412415E-18, 0.0002299780670421045197, 0.0004599561239687880061, 0.0006896788984287874130, 0.0009194956271626412558 ),
 .UNSPECIFIED. ) ;
#11465=VERTEX_POINT ( 'NONE', #5938 ) ;
#11467=CARTESIAN_POINT ( 'NONE',  ( 1.847247051441592403, -12.44188156437794035, -0.1676840720646602112 ) ) ;
#11472=CARTESIAN_POINT ( 'NONE',  ( 2.002547531651521773, 9.778737580845699995, 7.942910686618207983 ) ) ;
#11474=CARTESIAN_POINT ( 'NONE',  ( 1.846138399168762101, 12.43476674860266584, 0.4167076046095977149 ) ) ;
#11480=ADVANCED_FACE ( 'NONE', ( #14733 ), #18232, .F. ) ;
#11481=CARTESIAN_POINT ( 'NONE',  ( 1.847461586945730261, 7.286856109515200686, -10.08650590720928619 ) ) ;
#11482=CARTESIAN_POINT ( 'NONE',  ( 3.377929128793395908, -13.92579934231096495, 1.296196549818894539 ) ) ;
#11483=ORIENTED_EDGE ( 'NONE', *, *, #6019, .T. ) ;
#11484=CARTESIAN_POINT ( 'NONE',  ( 16.56753206892534891, -0.004368917149004301892, 0.008432171035096367243 ) ) ;
#11488=EDGE_CURVE ( 'NONE', #10380, #9401, #10441, .T. ) ;
#11490=CARTESIAN_POINT ( 'NONE',  ( 0.3058872367615226295, -4.821066432589418582, 12.87003593440626403 ) ) ;
#11491=EDGE_CURVE ( 'NONE', #5922, #15858, #16871, .T. ) ;
#11492=B_SPLINE_CURVE_WITH_KNOTS ( 'NONE', 3,
 ( #18079, #3446, #7674, #4603 ),
 .UNSPECIFIED., .F., .F.,
 ( 4, 4 ),
 ( 1.524041208624749586E-16, 0.002004993803842462265 ),
 .UNSPECIFIED. ) ;
#11493=CARTESIAN_POINT ( 'NONE',  ( 1.959283090834856189, 12.53713130127477804, -0.6676170829052656686 ) ) ;
#11494=ORIENTED_EDGE ( 'NONE', *, *, #10206, .T. ) ;
#11496=CARTESIAN_POINT ( 'NONE',  ( 16.57778382496167424, 0.01092721432669108844, -0.01018821665058837478 ) ) ;
#11498=CARTESIAN_POINT ( 'NONE',  ( 0.3151928476913618549, -11.11514699826556196, 8.075884471919712482 ) ) ;
#11500=VERTEX_POINT ( 'NONE', #3261 ) ;
#11503=CARTESIAN_POINT ( 'NONE',  ( 0.3095370825347234511, 13.20347358821919848, -3.806662003783274795 ) ) ;
#11504=CARTESIAN_POINT ( 'NONE',  ( 16.56872352241294521, 0.001821578298044641397, 0.01027347319884442528 ) ) ;
#11505=CARTESIAN_POINT ( 'NONE',  ( 0.4384471787762838635, -10.76632603192792459, 8.732395932355645485 ) ) ;
#11506=CARTESIAN_POINT ( 'NONE',  ( 16.57778382496167424, -0.007244066302947598825, 0.01306626476309386518 ) ) ;
#11507=CARTESIAN_POINT ( 'NONE',  ( 16.56679352167444819, -0.004277682826583350043, -0.008252760440870175046 ) ) ;
#11510=CARTESIAN_POINT ( 'NONE',  ( 2.002547531651519996, -6.845637710436264456, 10.57595306287289638 ) ) ;
#11516=EDGE_CURVE ( 'NONE', #3683, #16167, #2498, .T. ) ;
#11522=CARTESIAN_POINT ( 'NONE',  ( 8.438534575730034959, -6.598402093327866424, -1.899950616255257740 ) ) ;
#11527=CARTESIAN_POINT ( 'NONE',  ( 16.56753206892534891, -0.004253784598196240843, 0.008490833999798906573 ) ) ;
#11528=CARTESIAN_POINT ( 'NONE',  ( 0.3720661004400037664, 12.89739157014192550, 4.951033743989683877 ) ) ;
#11529=VERTEX_POINT ( 'NONE', #10931 ) ;
#11531=ORIENTED_EDGE ( 'NONE', *, *, #17675, .T. ) ;
#11533=VERTEX_POINT ( 'NONE', #12258 ) ;
#11534=ORIENTED_EDGE ( 'NONE', *, *, #2512, .T. ) ;
#11537=CARTESIAN_POINT ( 'NONE',  ( 0.4862570985993235340, -5.003653737315397976, -12.97920246947884770 ) ) ;
#11539=ORIENTED_EDGE ( 'NONE', *, *, #13131, .T. ) ;
#11540=CARTESIAN_POINT ( 'NONE',  ( 1.977228804421669262, 6.152949558600965041, 14.12033626431027322 ) ) ;
#11542=LINE ( 'NONE', #15926, #7456 ) ;
#11556=CARTESIAN_POINT ( 'NONE',  ( 3.950837973638676281, -12.81214529934979929, 6.888253895133251703 ) ) ;
#11565=CARTESIAN_POINT ( 'NONE',  ( 0.3148208552358936485, -4.463611911212133521, -12.99355031785210102 ) ) ;
#11570=CARTESIAN_POINT ( 'NONE',  ( 1.847412631396506022, 11.82061107079964124, 3.886120457021434493 ) ) ;
#11571=EDGE_CURVE ( 'NONE', #5025, #678, #10964, .T. ) ;
#11575=VERTEX_POINT ( 'NONE', #7883 ) ;
#11576=CARTESIAN_POINT ( 'NONE',  ( 1.846613052777651198, 7.035606253495462425, -10.26230975746752350 ) ) ;
#11577=CARTESIAN_POINT ( 'NONE',  ( 2.705023505549862595, -13.27418276223636795, 0.8488853074252508124 ) ) ;
#11579=CARTESIAN_POINT ( 'NONE',  ( 8.522092701127531811, -4.388629235579537102, -5.397361180353192012 ) ) ;
#11581=CARTESIAN_POINT ( 'NONE',  ( 0.3137051932979792457, -13.20008686438103140, -3.805684345189927154 ) ) ;
#11586=ORIENTED_EDGE ( 'NONE', *, *, #4292, .T. ) ;
#11594=EDGE_CURVE ( 'NONE', #16417, #5702, #9751, .T. ) ;
#11596=FACE_OUTER_BOUND ( 'NONE', #1013, .T. ) ;
#11599=FACE_OUTER_BOUND ( 'NONE', #2978, .T. ) ;
#11601=DIRECTION ( 'NONE',  ( -0.7561779333270775005, 0.3559159372837393809, -0.5491072561318300904 ) ) ;
#11604=CARTESIAN_POINT ( 'NONE',  ( 1.342453679581834924, -11.38190519890860131, 9.456403821038760427 ) ) ;
#11605=VERTEX_POINT ( 'NONE', #14145 ) ;
#11607=ORIENTED_EDGE ( 'NONE', *, *, #17295, .T. ) ;
#11609=CARTESIAN_POINT ( 'NONE',  ( 0.3058872367615226295, -10.75034008168909416, -8.562166468153835197 ) ) ;
#11610=CARTESIAN_POINT ( 'NONE',  ( 0.3142014840576498602, -8.382000553815529997, 10.88517824918540278 ) ) ;
#11616=VERTEX_POINT ( 'NONE', #8060 ) ;
#11618=DIRECTION ( 'NONE',  ( -1.000000000000000000, -0.000000000000000000, -0.000000000000000000 ) ) ;
#11620=VERTEX_POINT ( 'NONE', #9664 ) ;
#11621=ORIENTED_EDGE ( 'NONE', *, *, #9822, .F. ) ;
#11622=EDGE_CURVE ( 'NONE', #4533, #14938, #2568, .T. ) ;
#11627=CARTESIAN_POINT ( 'NONE',  ( 0.3095370825347224519, 7.700448427571875420, 11.38092634279631099 ) ) ;
#11630=CARTESIAN_POINT ( 'NONE',  ( 2.002547531651519996, -0.6781519942172617998, 12.57989064830759318 ) ) ;
#11632=CONICAL_SURFACE ( 'NONE', #32, 14.54644660717763927, 0.8559913436420816257 ) ;
#11641=CARTESIAN_POINT ( 'NONE',  ( 0.3132642857406524595, -12.89240536501342760, -4.743831191224519905 ) ) ;
#11651=VERTEX_POINT ( 'NONE', #15398 ) ;
#11652=CARTESIAN_POINT ( 'NONE',  ( 1.918918678667043576, 3.258447776120001915, -12.08296592096904298 ) ) ;
#11654=LINE ( 'NONE', #5807, #1338 ) ;
#11656=ORIENTED_EDGE ( 'NONE', *, *, #17240, .F. ) ;
#11658=CARTESIAN_POINT ( 'NONE',  ( 0.3137051932979757485, -4.679953077377398074, -12.91601973349275134 ) ) ;
#11659=CARTESIAN_POINT ( 'NONE',  ( 2.747332970342022840, -7.555624153089749662, 14.49942876448589679 ) ) ;
#11662=CARTESIAN_POINT ( 'NONE',  ( 1.959283090834840646, -6.829027319138321062, 10.53516775895158020 ) ) ;
#11666=CARTESIAN_POINT ( 'NONE',  ( 2.636624412717099908, 11.60464335004051861, -11.10302021258208249 ) ) ;
#11667=CARTESIAN_POINT ( 'NONE',  ( 0.3148208552358962575, 0.2299193288887468323, 13.73693263646118190 ) ) ;
#11670=EDGE_CURVE ( 'NONE', #8373, #13548, #10022, .T. ) ;
#11678=CARTESIAN_POINT ( 'NONE',  ( 1.847372867223022297, -10.00438561114518521, -7.398914411685100667 ) ) ;
#11681=CARTESIAN_POINT ( 'NONE',  ( 16.56753206892534891, 0.008490833999798920451, 0.004253784598196212220 ) ) ;
#11682=CARTESIAN_POINT ( 'NONE',  ( 2.747332970342022840, -16.12459247543624130, -2.705255688518015234 ) ) ;
#11685=ORIENTED_EDGE ( 'NONE', *, *, #4371, .T. ) ;
#11687=CARTESIAN_POINT ( 'NONE',  ( 16.56753206892534891, 0.009389754735541551434, -0.001421777558676823056 ) ) ;
#11692=ORIENTED_EDGE ( 'NONE', *, *, #3211, .T. ) ;
#11694=VERTEX_POINT ( 'NONE', #17203 ) ;
#11699=CARTESIAN_POINT ( 'NONE',  ( 16.56872352241294521, 0.001821578298043785094, -0.01027347319884367241 ) ) ;
#11703=CARTESIAN_POINT ( 'NONE',  ( 0.3150692679895986670, -8.199139630396084399, 11.02465386701225469 ) ) ;
#11708=CARTESIAN_POINT ( 'NONE',  ( 1.847168016377985778, 0.1868244120189564983, 12.44137401948661115 ) ) ;
#11710=CARTESIAN_POINT ( 'NONE',  ( 1.342453679581834924, 12.51077660954466353, 7.902645620902494450 ) ) ;
#11713=ORIENTED_EDGE ( 'NONE', *, *, #6196, .F. ) ;
#11717=ORIENTED_EDGE ( 'NONE', *, *, #15596, .F. ) ;
#11724=CARTESIAN_POINT ( 'NONE',  ( 0.8740764193764966050, 11.05257066464512405, 9.070946295053792241 ) ) ;
#11726=DIRECTION ( 'NONE',  ( 0.7635533937278214944, -0.1790966170213922626, -0.6204116510013485408 ) ) ;
#11727=CARTESIAN_POINT ( 'NONE',  ( 0.4862570985993235340, 0.7479633556562450547, 13.89016912371017831 ) ) ;
#11728=AXIS2_PLACEMENT_3D ( 'NONE', #8787, #17479, #90 ) ;
#11729=CARTESIAN_POINT ( 'NONE',  ( 1.254255976357838698, 9.426444230097315469, -11.25336128106935973 ) ) ;
#11731=CARTESIAN_POINT ( 'NONE',  ( 1.977228804422197062, -15.04020501276157518, -3.321884655131998265 ) ) ;
#11733=CARTESIAN_POINT ( 'NONE',  ( 1.847461586945734702, 11.82388984758123840, -3.877048136045254001 ) ) ;
#11735=B_SPLINE_CURVE_WITH_KNOTS ( 'NONE', 3,
 ( #6188, #7539, #15070, #459 ),
 .UNSPECIFIED., .F., .F.,
 ( 4, 4 ),
 ( 2.006682199098010609E-17, 0.003005512676784846595 ),
 .UNSPECIFIED. ) ;
#11736=CARTESIAN_POINT ( 'NONE',  ( 0.3142011359265350912, -11.33549115679417696, -7.762194356530893735 ) ) ;
#11738=CARTESIAN_POINT ( 'NONE',  ( 1.846138399168762101, 6.971848976711011225, 10.30487220521572667 ) ) ;
#11742=EDGE_LOOP ( 'NONE', ( #15451, #12329, #5978, #303 ) ) ;
#11750=CARTESIAN_POINT ( 'NONE',  ( 16.57778382496167424, 0.01018821665058833661, 0.01092721432669112661 ) ) ;
#11753=CARTESIAN_POINT ( 'NONE',  ( 2.002547531651519996, 3.242439124566649511, 12.17374746633579541 ) ) ;
#11756=( BOUNDED_SURFACE ( )  B_SPLINE_SURFACE ( 3, 1, ( 
 ( #17797, #7380 ),
 ( #6037, #10526 ),
 ( #10627, #12058 ),
 ( #2955, #14819 ) ),
 .UNSPECIFIED., .F., .F., .T. ) 
 B_SPLINE_SURFACE_WITH_KNOTS ( ( 4, 4 ),
 ( 2, 2 ),
 ( 0.000000000000000000, 1.000000000000000000 ),
 ( 0.000000000000000000, 1.000000000000000000 ),
 .UNSPECIFIED. ) 
 GEOMETRIC_REPRESENTATION_ITEM ( )  RATIONAL_B_SPLINE_SURFACE ( (
 ( 1.000000000000000000, 1.000000000000000000),
 ( 0.9933953342250438912, 0.8357391271907739227),
 ( 0.9933953342250438912, 0.8357391271907739227),
 ( 1.000000000000000000, 1.000000000000000000) ) ) 
 REPRESENTATION_ITEM ( '' )  SURFACE ( )  );
#11758=CARTESIAN_POINT ( 'NONE',  ( 2.002547531651519996, -6.845637710436264456, 10.57595306287289638 ) ) ;
#11760=CONICAL_SURFACE ( 'NONE', #3519, 12.15840553252917289, 0.7853981625000049371 ) ;
#11762=DIRECTION ( 'NONE',  ( 0.000000000000000000, 0.000000000000000000, 1.000000000000000000 ) ) ;
#11764=CARTESIAN_POINT ( 'NONE',  ( 1.846955891736117072, 7.098901504650503291, -10.21904526726839002 ) ) ;
#11765=CARTESIAN_POINT ( 'NONE',  ( 0.3142011359265339254, 0.3830873813806325301, 13.73310835363014171 ) ) ;
#11769=ORIENTED_EDGE ( 'NONE', *, *, #16443, .T. ) ;
#11775=VERTEX_POINT ( 'NONE', #15867 ) ;
#11777=CARTESIAN_POINT ( 'NONE',  ( 2.123976203522053297, -7.899625852120107261, -13.47898556379321633 ) ) ;
#11781=CARTESIAN_POINT ( 'NONE',  ( 3.950837973638668288, 0.000000000000000000, 0.000000000000000000 ) ) ;
#11787=CARTESIAN_POINT ( 'NONE',  ( 16.58200780006414732, 0.008650561019685807859, 0.007066318000006031885 ) ) ;
#11792=CARTESIAN_POINT ( 'NONE',  ( 0.4862570985993235340, 5.003653737315670647, -12.97920246947874112 ) ) ;
#11795=CARTESIAN_POINT ( 'NONE',  ( 16.56872352241294521, 0.01027347319884366721, 0.001821578298043820656 ) ) ;
#11796=EDGE_LOOP ( 'NONE', ( #12654, #9641, #5895, #16437 ) ) ;
#11797=CARTESIAN_POINT ( 'NONE',  ( 16.56822296793089322, 0.003834730849371879857, 0.009385634690642069913 ) ) ;
#11798=EDGE_LOOP ( 'NONE', ( #7961, #12730, #18563, #15479 ) ) ;
#11800=CARTESIAN_POINT ( 'NONE',  ( 0.3137051932979792457, -13.20008686438103140, -3.805684345189927154 ) ) ;
#11806=EDGE_CURVE ( 'NONE', #15560, #3963, #8697, .T. ) ;
#11808=AXIS2_PLACEMENT_3D ( 'NONE', #12528, #18363, #11112 ) ;
#11811=CARTESIAN_POINT ( 'NONE',  ( 1.846138399168762101, 7.646096044340033870, -9.815003036200328879 ) ) ;
#11812=CIRCLE ( 'NONE', #4486, 5.000000000000000000 ) ;
#11814=CARTESIAN_POINT ( 'NONE',  ( 2.636624412716062515, -6.973567714909003179, -14.46769361191335790 ) ) ;
#11820=ORIENTED_EDGE ( 'NONE', *, *, #1397, .F. ) ;
#11821=CARTESIAN_POINT ( 'NONE',  ( 1.959212340397943120, -9.750290364083578964, -7.909199412631276793 ) ) ;
#11822=CARTESIAN_POINT ( 'NONE',  ( 16.56679352167444819, -0.006618561353600137254, -0.006526964904752322223 ) ) ;
#11823=CARTESIAN_POINT ( 'NONE',  ( 0.4754618798421162973, -12.98792082933640835, -5.007009103465388300 ) ) ;
#11824=EDGE_LOOP ( 'NONE', ( #9043, #2952, #4427, #15986 ) ) ;
#11829=CARTESIAN_POINT ( 'NONE',  ( 0.3142011359265305392, 8.382042760265909109, 10.88514493056445076 ) ) ;
#11830=EDGE_CURVE ( 'NONE', #18306, #18321, #18404, .T. ) ;
#11831=EDGE_CURVE ( 'NONE', #16063, #15590, #4697, .T. ) ;
#11835=CARTESIAN_POINT ( 'NONE',  ( 0.3150692679895942816, -11.02465386701222805, -8.199139630396127032 ) ) ;
#11837=CIRCLE ( 'NONE', #3597, 5.000000000000000000 ) ;
#11838=VERTEX_POINT ( 'NONE', #14524 ) ;
#11839=ORIENTED_EDGE ( 'NONE', *, *, #2636, .F. ) ;
#11843=ORIENTED_EDGE ( 'NONE', *, *, #3294, .F. ) ;
#11853=CARTESIAN_POINT ( 'NONE',  ( 0.4754618798421171855, 7.564402563418640035, -11.68486377711958291 ) ) ;
#11860=CARTESIAN_POINT ( 'NONE',  ( 1.847034903785825799, 0.2299360331935915713, -12.44051878787772480 ) ) ;
#11864=B_SPLINE_CURVE_WITH_KNOTS ( 'NONE', 3,
 ( #5645, #15886, #13115, #219 ),
 .UNSPECIFIED., .F., .F.,
 ( 4, 4 ),
 ( 9.796581096179191873E-17, 0.002004993803842611885 ),
 .UNSPECIFIED. ) ;
#11865=ORIENTED_EDGE ( 'NONE', *, *, #6920, .F. ) ;
#11866=CARTESIAN_POINT ( 'NONE',  ( 2.705023505549862595, -7.115606223895247773, 11.23800170568054568 ) ) ;
#11874=CARTESIAN_POINT ( 'NONE',  ( 0.4862570985993235340, -10.79774104611366781, -8.769551628660854803 ) ) ;
#11880=FACE_OUTER_BOUND ( 'NONE', #14984, .T. ) ;
#11881=CARTESIAN_POINT ( 'NONE',  ( 16.57210152137263393, 0.01402404281922921964, -0.003862718596009325888 ) ) ;
#11885=CARTESIAN_POINT ( 'NONE',  ( 0.3170788640506440603, -11.20690911610909168, 7.952793437297537515 ) ) ;
#11889=ORIENTED_EDGE ( 'NONE', *, *, #6422, .F. ) ;
#11893=ORIENTED_EDGE ( 'NONE', *, *, #10701, .F. ) ;
#11898=CARTESIAN_POINT ( 'NONE',  ( 0.4385251269669960816, -8.732456510146150208, 10.76637725024249193 ) ) ;
#11899=EDGE_CURVE ( 'NONE', #15560, #348, #8070, .T. ) ;
#11900=FACE_OUTER_BOUND ( 'NONE', #4820, .T. ) ;
#11902=B_SPLINE_CURVE_WITH_KNOTS ( 'NONE', 3,
 ( #2543, #12965, #8667, #18796, #941, #3908, #17367, #4283, #2454, #10106, #15933, #8306, #16131 ),
 .UNSPECIFIED., .F., .F.,
 ( 4, 3, 3, 3, 4 ),
 ( 1.734723475976807094E-18, 0.0002299804304191470643, 0.0004599608082120238165, 0.0006467586077648016917, 0.0008336169836825990491 ),
 .UNSPECIFIED. ) ;
#11905=CARTESIAN_POINT ( 'NONE',  ( 2.747332970342022840, 7.289199830147106596, 14.63517873738950037 ) ) ;
#11908=CARTESIAN_POINT ( 'NONE',  ( 16.56822296793089322, -0.006547366384936689071, -0.007741272030791150442 ) ) ;
#11912=ORIENTED_EDGE ( 'NONE', *, *, #8274, .T. ) ;
#11913=B_SPLINE_CURVE_WITH_KNOTS ( 'NONE', 3,
 ( #13487, #6233, #10637, #4900, #13299, #6045 ),
 .UNSPECIFIED., .F., .F.,
 ( 4, 2, 4 ),
 ( 4.256846838097967453E-17, 0.0002014099069817298958, 0.0004028198139634172367 ),
 .UNSPECIFIED. ) ;
#11916=CARTESIAN_POINT ( 'NONE',  ( 16.56782317627811096, -0.009814734722106369796, 0.0003415813796014346851 ) ) ;
#11922=CARTESIAN_POINT ( 'NONE',  ( 2.636624412716062960, -2.161493821598612808, -15.91454522070331912 ) ) ;
#11923=CARTESIAN_POINT ( 'NONE',  ( 2.002547531651519996, -4.532360870844247991, -11.75462648437106417 ) ) ;
#11925=CARTESIAN_POINT ( 'NONE',  ( 0.3145734862173208413, -10.93207848441427643, -8.321353293018953323 ) ) ;
#11927=CARTESIAN_POINT ( 'NONE',  ( 0.3145734862173253377, 4.535879238195112073, -12.96846406299301258 ) ) ;
#11929=B_SPLINE_CURVE_WITH_KNOTS ( 'NONE', 3,
 ( #330, #9022, #4824, #11987 ),
 .UNSPECIFIED., .F., .F.,
 ( 4, 4 ),
 ( 0.000000000000000000, 0.002004993803840905784 ),
 .UNSPECIFIED. ) ;
#11931=EDGE_LOOP ( 'NONE', ( #7861, #13622, #13977, #5773 ) ) ;
#11935=EDGE_CURVE ( 'NONE', #6348, #6138, #4886, .T. ) ;
#11937=EDGE_CURVE ( 'NONE', #2927, #14774, #15818, .T. ) ;
#11939=DIRECTION ( 'NONE',  ( -1.000000000000000000, -0.000000000000000000, -0.000000000000000000 ) ) ;
#11942=CARTESIAN_POINT ( 'NONE',  ( 0.4862570985993235340, -8.769551628660655851, -10.79774104611382946 ) ) ;
#11949=CARTESIAN_POINT ( 'NONE',  ( 2.636624412714134280, 2.862162146984768896, 15.80357026013147426 ) ) ;
#11951=B_SPLINE_CURVE_WITH_KNOTS ( 'NONE', 3,
 ( #9522, #2350, #16608, #15347, #3409, #9439 ),
 .UNSPECIFIED., .F., .F.,
 ( 4, 2, 4 ),
 ( 0.000000000000000000, 0.001656992708822828484, 0.003313985417645657836 ),
 .UNSPECIFIED. ) ;
#11952=CARTESIAN_POINT ( 'NONE',  ( 2.002547531651519996, 7.942910686618173344, 9.778737580845726640 ) ) ;
#11953=ORIENTED_EDGE ( 'NONE', *, *, #8274, .F. ) ;
#11958=CARTESIAN_POINT ( 'NONE',  ( 2.002547531651519996, 12.57989064830759496, 0.6781519942172178350 ) ) ;
#11965=CARTESIAN_POINT ( 'NONE',  ( 1.846138399168762101, 4.238866729160568170, -11.69739621335917690 ) ) ;
#11966=FACE_OUTER_BOUND ( 'NONE', #8003, .T. ) ;
#11969=CARTESIAN_POINT ( 'NONE',  ( 8.522092701127531811, -6.722964936702084948, -1.786985377232103600 ) ) ;
#11972=CONICAL_SURFACE ( 'NONE', #14701, 14.54644660717763927, 0.8559913436420816257 ) ;
#11973=ADVANCED_FACE ( 'NONE', ( #8197 ), #655, .F. ) ;
#11974=CARTESIAN_POINT ( 'NONE',  ( 0.000000000000000000, 4.769696007084728073, -1.500000000000000000 ) ) ;
#11981=CARTESIAN_POINT ( 'NONE',  ( 0.4384471787762824757, -13.84291427302852107, 0.7363690479465839767 ) ) ;
#11982=( BOUNDED_SURFACE ( )  B_SPLINE_SURFACE ( 3, 1, ( 
 ( #4742, #1780 ),
 ( #1877, #6374 ),
 ( #10670, #13237 ),
 ( #16504, #18026 ) ),
 .UNSPECIFIED., .F., .F., .T. ) 
 B_SPLINE_SURFACE_WITH_KNOTS ( ( 4, 4 ),
 ( 2, 2 ),
 ( 0.000000000000000000, 1.000000000000000000 ),
 ( 0.000000000000000000, 1.000000000000000000 ),
 .UNSPECIFIED. ) 
 GEOMETRIC_REPRESENTATION_ITEM ( )  RATIONAL_B_SPLINE_SURFACE ( (
 ( 1.000000000000000000, 1.000000000000000000),
 ( 0.9593108457356467333, 0.9995965569486454649),
 ( 0.9593108457356467333, 0.9995965569486454649),
 ( 1.000000000000000000, 1.000000000000000000) ) ) 
 REPRESENTATION_ITEM ( '' )  SURFACE ( )  );
#11985=CARTESIAN_POINT ( 'NONE',  ( 1.846138399168762101, -0.4167076046096411246, 12.43476674860266407 ) ) ;
#11987=CARTESIAN_POINT ( 'NONE',  ( 2.636624412717140764, -2.862162146982851763, -15.80357026013259514 ) ) ;
#11991=ADVANCED_FACE ( 'NONE', ( #11067 ), #2615, .F. ) ;
#11992=EDGE_CURVE ( 'NONE', #11620, #10419, #17156, .T. ) ;
#12001=CARTESIAN_POINT ( 'NONE',  ( 1.977436885026784941, 6.153171729169462090, -14.12046670317587704 ) ) ;
#12004=EDGE_CURVE ( 'NONE', #14287, #4150, #17640, .T. ) ;
#12006=CARTESIAN_POINT ( 'NONE',  ( 2.636624412714236865, 0.000000000000000000, 0.000000000000000000 ) ) ;
#12008=VECTOR ( 'NONE', #15348, 1000.000000000000000 ) ;
#12010=VERTEX_POINT ( 'NONE', #17070 ) ;
#12013=CARTESIAN_POINT ( 'NONE',  ( 16.56872352241294521, -0.01027347319884365333, -0.001821578298043897851 ) ) ;
#12014=CARTESIAN_POINT ( 'NONE',  ( 16.56782317627811096, 0.009439921864426886397, -0.002708056627498675335 ) ) ;
#12016=CARTESIAN_POINT ( 'NONE',  ( 1.918918678667072442, -12.49849921341423276, 0.6348738215464800883 ) ) ;
#12018=CARTESIAN_POINT ( 'NONE',  ( 1.254009781011619307, -7.789615163754444183, 12.44229282923071445 ) ) ;
#12019=CARTESIAN_POINT ( 'NONE',  ( 16.56782317627811096, 0.0003415813796006246777, -0.009814734722107084502 ) ) ;
#12020=AXIS2_PLACEMENT_3D ( 'NONE', #4219, #7278, #2843 ) ;
#12025=CARTESIAN_POINT ( 'NONE',  ( 0.3137051932979792457, -12.91601973349266963, -4.679953077377624560 ) ) ;
#12027=CARTESIAN_POINT ( 'NONE',  ( 0.3137051932979775248, 3.805684345189972895, -13.20008686438101719 ) ) ;
#12028=ADVANCED_FACE ( 'NONE', ( #18402 ), #2577, .F. ) ;
#12029=ORIENTED_EDGE ( 'NONE', *, *, #18640, .F. ) ;
#12032=VERTEX_POINT ( 'NONE', #18678 ) ;
#12038=CARTESIAN_POINT ( 'NONE',  ( 0.4754618798421162973, 5.007009103465249744, 12.98792082933646341 ) ) ;
#12049=EDGE_CURVE ( 'NONE', #2427, #15029, #8372, .T. ) ;
#12054=ORIENTED_EDGE ( 'NONE', *, *, #16782, .F. ) ;
#12057=VECTOR ( 'NONE', #14025, 1000.000000000000114 ) ;
#12058=CARTESIAN_POINT ( 'NONE',  ( 0.3058872367615230181, 13.72992299905060065, -0.6080468242581438254 ) ) ;
#12063=CARTESIAN_POINT ( 'NONE',  ( 3.950837973638676281, 10.05648675950141602, -10.51028938476206953 ) ) ;
#12066=CARTESIAN_POINT ( 'NONE',  ( 1.861628059977342486, 4.358833901513207820, -11.66985327793194216 ) ) ;
#12068=CARTESIAN_POINT ( 'NONE',  ( 0.4862570985993252548, 3.580942890621670482, 13.44146924561382583 ) ) ;
#12073=CARTESIAN_POINT ( 'NONE',  ( 0.4862570985993235340, -3.580942890621579444, -13.44146924561384537 ) ) ;
#12086=CARTESIAN_POINT ( 'NONE',  ( 1.846138399168762101, -0.4167076046096411246, 12.43476674860266407 ) ) ;
#12089=ORIENTED_EDGE ( 'NONE', *, *, #6909, .F. ) ;
#12090=CARTESIAN_POINT ( 'NONE',  ( 0.3142014840576499712, -13.73311050063163563, -0.3830336514510319090 ) ) ;
#12094=DIRECTION ( 'NONE',  ( 0.000000000000000000, 0.000000000000000000, 1.000000000000000000 ) ) ;
#12100=CARTESIAN_POINT ( 'NONE',  ( 0.4384471787762828088, -12.93784327393176881, 4.978024343488995918 ) ) ;
#12101=B_SPLINE_CURVE_WITH_KNOTS ( 'NONE', 3,
 ( #1711, #286, #6115, #16444, #18412, #16990 ),
 .UNSPECIFIED., .F., .F.,
 ( 4, 2, 4 ),
 ( 9.263427422397552964E-19, 0.001500839035891551789, 0.003001678071783102711 ),
 .UNSPECIFIED. ) ;
#12102=EDGE_CURVE ( 'NONE', #14389, #7527, #8650, .T. ) ;
#12104=CARTESIAN_POINT ( 'NONE',  ( 0.4754618798421162973, 11.68486377711977475, -7.564402563418339831 ) ) ;
#12107=ORIENTED_EDGE ( 'NONE', *, *, #18338, .T. ) ;
#12111=CARTESIAN_POINT ( 'NONE',  ( 3.353306896162455253, -3.007732942432324474, -13.62210141459498303 ) ) ;
#12119=ORIENTED_EDGE ( 'NONE', *, *, #3339, .F. ) ;
#12122=CARTESIAN_POINT ( 'NONE',  ( 0.4862570985993235340, -0.7479633556561480212, -13.89016912371018186 ) ) ;
#12132=ORIENTED_EDGE ( 'NONE', *, *, #15343, .F. ) ;
#12135=CARTESIAN_POINT ( 'NONE',  ( 1.846524061778019421, -7.023652644192194927, -10.27028962889604813 ) ) ;
#12144=ADVANCED_FACE ( 'NONE', ( #1490 ), #9081, .F. ) ;
#12145=CARTESIAN_POINT ( 'NONE',  ( 0.3058872367615226295, -3.664492643742672584, -13.24582953854928569 ) ) ;
#12147=CARTESIAN_POINT ( 'NONE',  ( 2.123976203522053741, 7.899625852120402136, -13.47898556379304580 ) ) ;
#12149=ADVANCED_FACE ( 'NONE', ( #7327 ), #3825, .F. ) ;
#12150=FACE_OUTER_BOUND ( 'NONE', #6012, .T. ) ;
#12155=VERTEX_POINT ( 'NONE', #10176 ) ;
#12156=DIRECTION ( 'NONE',  ( 0.000000000000000000, 0.000000000000000000, -1.000000000000000000 ) ) ;
#12164=EDGE_CURVE ( 'NONE', #14694, #5775, #12407, .T. ) ;
#12171=CARTESIAN_POINT ( 'NONE',  ( 2.002547531651519996, -10.57595306287296921, 6.845637710436153434 ) ) ;
#12172=LINE ( 'NONE', #12443, #1741 ) ;
#12173=ORIENTED_EDGE ( 'NONE', *, *, #13093, .T. ) ;
#12175=B_SPLINE_CURVE_WITH_KNOTS ( 'NONE', 3,
 ( #9824, #9653, #1231, #6881, #15657, #3919, #12517, #2555, #11467, #12886, #14235, #3824, #12796 ),
 .UNSPECIFIED., .F., .F.,
 ( 4, 3, 3, 3, 4 ),
 ( 1.788933584601082316E-18, 0.0002299804304191483382, 0.0004599608082120253344, 0.0006467586077648016917, 0.0008336169836825988323 ),
 .UNSPECIFIED. ) ;
#12178=CARTESIAN_POINT ( 'NONE',  ( 2.320520222536477384, 7.743191299717406828, 13.71278186123164922 ) ) ;
#12179=B_SPLINE_CURVE_WITH_KNOTS ( 'NONE', 3,
 ( #3315, #1900, #8865, #10396, #10599, #3213, #4475, #10305, #7736, #5893, #2920, #16133, #11738 ),
 .UNSPECIFIED., .F., .F.,
 ( 4, 3, 3, 3, 4 ),
 ( 0.000000000000000000, 0.0002299804304191501543, 0.0004599608082120262018, 0.0006467586077648019086, 0.0008336169836825998080 ),
 .UNSPECIFIED. ) ;
#12185=ORIENTED_EDGE ( 'NONE', *, *, #15126, .F. ) ;
#12188=ADVANCED_FACE ( 'NONE', ( #6556 ), #17654, .F. ) ;
#12189=B_SPLINE_CURVE_WITH_KNOTS ( 'NONE', 3,
 ( #15215, #7967, #311, #13775 ),
 .UNSPECIFIED., .F., .F.,
 ( 4, 4 ),
 ( 2.211347213673310975E-17, 0.003005512676784851799 ),
 .UNSPECIFIED. ) ;
#12191=B_SPLINE_CURVE_WITH_KNOTS ( 'NONE', 3,
 ( #13465, #6205, #188, #10706, #17974, #1713 ),
 .UNSPECIFIED., .F., .F.,
 ( 4, 2, 4 ),
 ( 4.206917491929696500E-17, 0.0002014099069817275648, 0.0004028198139634130625 ),
 .UNSPECIFIED. ) ;
#12195=( BOUNDED_SURFACE ( )  B_SPLINE_SURFACE ( 3, 1, ( 
 ( #6208, #11659 ),
 ( #16450, #8977 ),
 ( #8880, #7754 ),
 ( #191, #1619 ) ),
 .UNSPECIFIED., .F., .F., .T. ) 
 B_SPLINE_SURFACE_WITH_KNOTS ( ( 4, 4 ),
 ( 2, 2 ),
 ( 0.000000000000000000, 1.000000000000000000 ),
 ( 0.000000000000000000, 1.000000000000000000 ),
 .UNSPECIFIED. ) 
 GEOMETRIC_REPRESENTATION_ITEM ( )  RATIONAL_B_SPLINE_SURFACE ( (
 ( 1.000000000000000000, 1.000000000000000000),
 ( 0.7792777138730158093, 0.9689936506012928330),
 ( 0.7792777138730158093, 0.9689936506012928330),
 ( 1.000000000000000000, 1.000000000000000000) ) ) 
 REPRESENTATION_ITEM ( '' )  SURFACE ( )  );
#12199=CARTESIAN_POINT ( 'NONE',  ( 0.3720661004400040439, -8.694226082900513575, -10.73619472937711983 ) ) ;
#12204=ORIENTED_EDGE ( 'NONE', *, *, #5498, .T. ) ;
#12208=AXIS2_PLACEMENT_3D ( 'NONE', #1596, #10391, #14685 ) ;
#12212=CARTESIAN_POINT ( 'NONE',  ( 8.438534575730034959, 1.899950616255281055, -6.598402093327859319 ) ) ;
#12213=EDGE_CURVE ( 'NONE', #12695, #2120, #15052, .T. ) ;
#12214=ORIENTED_EDGE ( 'NONE', *, *, #11134, .T. ) ;
#12215=CARTESIAN_POINT ( 'NONE',  ( 16.58200780006414732, -0.004047297414158971054, 0.01041078477704053193 ) ) ;
#12216=CARTESIAN_POINT ( 'NONE',  ( 1.847412631396502025, -11.84727953344286533, 3.804043368582616935 ) ) ;
#12220=DIRECTION ( 'NONE',  ( 0.000000000000000000, 0.000000000000000000, 1.000000000000000000 ) ) ;
#12221=CARTESIAN_POINT ( 'NONE',  ( 2.636624412714237309, 15.91454522070173638, -2.161493821596664144 ) ) ;
#12225=EDGE_LOOP ( 'NONE', ( #15746, #8677, #13398, #2011 ) ) ;
#12226=ORIENTED_EDGE ( 'NONE', *, *, #14106, .T. ) ;
#12227=CARTESIAN_POINT ( 'NONE',  ( 0.8740779401512879243, 13.31469722824398794, -5.211551231203936929 ) ) ;
#12231=CARTESIAN_POINT ( 'NONE',  ( 16.57778382496167424, 0.002851818597093403688, 0.01466529584256672306 ) ) ;
#12232=EDGE_CURVE ( 'NONE', #6002, #3979, #17668, .T. ) ;
#12237=EDGE_CURVE ( 'NONE', #17311, #4902, #8293, .T. ) ;
#12240=CARTESIAN_POINT ( 'NONE',  ( 16.56782317627811096, -0.009439921864426449247, -0.002708056627497712563 ) ) ;
#12250=CARTESIAN_POINT ( 'NONE',  ( 0.3095370825347224519, -12.91933430393604709, -4.681152801286295073 ) ) ;
#12254=CARTESIAN_POINT ( 'NONE',  ( 2.002547531651519996, 4.532360870844327039, 11.75462648437103752 ) ) ;
#12258=CARTESIAN_POINT ( 'NONE',  ( 0.3151928479966097374, 0.000000000000000000, -13.73922861026898623 ) ) ;
#12259=( BOUNDED_SURFACE ( )  B_SPLINE_SURFACE ( 3, 1, ( 
 ( #154, #8934 ),
 ( #1677, #252 ),
 ( #11908, #17745 ),
 ( #4647, #10472 ) ),
 .UNSPECIFIED., .F., .F., .T. ) 
 B_SPLINE_SURFACE_WITH_KNOTS ( ( 4, 4 ),
 ( 2, 2 ),
 ( 0.000000000000000000, 1.000000000000000000 ),
 ( 0.000000000000000000, 1.000000000000000000 ),
 .UNSPECIFIED. ) 
 GEOMETRIC_REPRESENTATION_ITEM ( )  RATIONAL_B_SPLINE_SURFACE ( (
 ( 1.000000000000000000, 1.000000000000000000),
 ( 0.9933953342250436691, 0.8357391271907733676),
 ( 0.9933953342250436691, 0.8357391271907733676),
 ( 1.000000000000000000, 1.000000000000000000) ) ) 
 REPRESENTATION_ITEM ( '' )  SURFACE ( )  );
#12262=ORIENTED_EDGE ( 'NONE', *, *, #10347, .F. ) ;
#12263=CARTESIAN_POINT ( 'NONE',  ( 0.4862570985993235340, 8.769551628660890330, -10.79774104611363761 ) ) ;
#12264=EDGE_CURVE ( 'NONE', #14938, #14465, #9886, .T. ) ;
#12269=CARTESIAN_POINT ( 'NONE',  ( 0.3148208552358927048, 10.97826876274324270, -8.260375059853219071 ) ) ;
#12275=CIRCLE ( 'NONE', #6175, 14.54644660717763927 ) ;
#12277=CARTESIAN_POINT ( 'NONE',  ( 0.3308579732647022875, 13.25341063505880967, -3.680601586799737923 ) ) ;
#12281=DIRECTION ( 'NONE',  ( -1.000000000000000000, 0.000000000000000000, 0.000000000000000000 ) ) ;
#12290=VERTEX_POINT ( 'NONE', #3957 ) ;
#12291=ORIENTED_EDGE ( 'NONE', *, *, #1658, .F. ) ;
#12292=ORIENTED_EDGE ( 'NONE', *, *, #11206, .T. ) ;
#12294=( BOUNDED_SURFACE ( )  B_SPLINE_SURFACE ( 3, 1, ( 
 ( #8194, #18313 ),
 ( #918, #18043 ),
 ( #4857, #6759 ),
 ( #649, #7926 ) ),
 .UNSPECIFIED., .F., .F., .T. ) 
 B_SPLINE_SURFACE_WITH_KNOTS ( ( 4, 4 ),
 ( 2, 2 ),
 ( 0.000000000000000000, 1.000000000000000000 ),
 ( 0.000000000000000000, 1.000000000000000000 ),
 .UNSPECIFIED. ) 
 GEOMETRIC_REPRESENTATION_ITEM ( )  RATIONAL_B_SPLINE_SURFACE ( (
 ( 1.000000000000000000, 1.000000000000000000),
 ( 0.7792777138730158093, 0.9689936506012928330),
 ( 0.7792777138730158093, 0.9689936506012928330),
 ( 1.000000000000000000, 1.000000000000000000) ) ) 
 REPRESENTATION_ITEM ( '' )  SURFACE ( )  );
#12296=CARTESIAN_POINT ( 'NONE',  ( 0.3939875929385628361, 12.90850834464107244, -4.930599594904421679 ) ) ;
#12301=CARTESIAN_POINT ( 'NONE',  ( 8.522092701127531811, 3.777034505568523048, 5.841710761610143798 ) ) ;
#12302=CARTESIAN_POINT ( 'NONE',  ( 16.57778382496167424, 0.01354073047775767452, 0.006312874906843726416 ) ) ;
#12303=DIRECTION ( 'NONE',  ( 0.000000000000000000, 0.000000000000000000, 1.000000000000000000 ) ) ;
#12304=CARTESIAN_POINT ( 'NONE',  ( 2.705023505549862151, 8.489131503859777439, 10.24007717649583782 ) ) ;
#12305=DIRECTION ( 'NONE',  ( -0.7561779333270775005, -0.2350349629540143537, -0.6106991889125079620 ) ) ;
#12306=CONICAL_SURFACE ( 'NONE', #1616, 14.54644660717763927, 0.8559913436420816257 ) ;
#12308=EDGE_CURVE ( 'NONE', #15961, #2927, #11048, .T. ) ;
#12311=EDGE_CURVE ( 'NONE', #4533, #7061, #10828, .T. ) ;
#12312=ORIENTED_EDGE ( 'NONE', *, *, #17793, .T. ) ;
#12313=CARTESIAN_POINT ( 'NONE',  ( 0.4862570985993235340, 12.97920246947886191, -5.003653737315353567 ) ) ;
#12317=CARTESIAN_POINT ( 'NONE',  ( 3.074695600507241444, -15.30693405987796751, 2.772091048739207864 ) ) ;
#12319=LINE ( 'NONE', #13839, #17864 ) ;
#12320=EDGE_CURVE ( 'NONE', #3538, #617, #3038, .T. ) ;
#12322=B_SPLINE_CURVE_WITH_KNOTS ( 'NONE', 3,
 ( #2778, #8625, #1361, #4418, #7104, #8905 ),
 .UNSPECIFIED., .F., .F.,
 ( 4, 2, 4 ),
 ( 0.000000000000000000, 0.001500839035891552223, 0.003001678071783104446 ),
 .UNSPECIFIED. ) ;
#12324=CARTESIAN_POINT ( 'NONE',  ( 1.861628059977344263, -6.879051339207215676, -10.38573835516720401 ) ) ;
#12325=CARTESIAN_POINT ( 'NONE',  ( 16.57778382496167424, -0.002851818597093896349, 0.01466529584256787665 ) ) ;
#12329=ORIENTED_EDGE ( 'NONE', *, *, #269, .T. ) ;
#12330=DIRECTION ( 'NONE',  ( -1.000000000000000000, -0.000000000000000000, -0.000000000000000000 ) ) ;
#12331=VECTOR ( 'NONE', #1426, 1000.000000000000114 ) ;
#12332=CARTESIAN_POINT ( 'NONE',  ( 16.56753206892534891, -0.008490833999798035742, 0.004253784598196731770 ) ) ;
#12337=ORIENTED_EDGE ( 'NONE', *, *, #5415, .F. ) ;
#12343=AXIS2_PLACEMENT_3D ( 'NONE', #11322, #18478, #14454 ) ;
#12345=CARTESIAN_POINT ( 'NONE',  ( 1.847372867223027848, -10.12831093686727080, 7.228345833872717563 ) ) ;
#12358=CARTESIAN_POINT ( 'NONE',  ( 2.636624412714236865, 0.000000000000000000, 0.000000000000000000 ) ) ;
#12371=( BOUNDED_SURFACE ( )  B_SPLINE_SURFACE ( 3, 1, ( 
 ( #14015, #18047 ),
 ( #18317, #17960 ),
 ( #9528, #9444 ),
 ( #16528, #15268 ) ),
 .UNSPECIFIED., .F., .F., .T. ) 
 B_SPLINE_SURFACE_WITH_KNOTS ( ( 4, 4 ),
 ( 2, 2 ),
 ( 0.000000000000000000, 1.000000000000000000 ),
 ( 0.000000000000000000, 1.000000000000000000 ),
 .UNSPECIFIED. ) 
 GEOMETRIC_REPRESENTATION_ITEM ( )  RATIONAL_B_SPLINE_SURFACE ( (
 ( 1.000000000000000000, 1.000000000000000000),
 ( 0.9933953342250438912, 0.8357391271907739227),
 ( 0.9933953342250438912, 0.8357391271907739227),
 ( 1.000000000000000000, 1.000000000000000000) ) ) 
 REPRESENTATION_ITEM ( '' )  SURFACE ( )  );
#12383=ORIENTED_EDGE ( 'NONE', *, *, #8315, .F. ) ;
#12384=ORIENTED_EDGE ( 'NONE', *, *, #6070, .F. ) ;
#12386=CARTESIAN_POINT ( 'NONE',  ( 0.4862570985993235340, -10.79774104611366781, -8.769551628660854803 ) ) ;
#12387=ADVANCED_FACE ( 'NONE', ( #11880 ), #10932, .F. ) ;
#12389=CARTESIAN_POINT ( 'NONE',  ( 2.123976203522053297, 7.899625852120206737, 13.47898556379315771 ) ) ;
#12390=CARTESIAN_POINT ( 'NONE',  ( 1.846138399168762101, -11.95493567637852905, 3.446241763652952539 ) ) ;
#12391=CARTESIAN_POINT ( 'NONE',  ( 1.846138399168762101, -4.238866729160323032, -11.69739621335926394 ) ) ;
#12394=CARTESIAN_POINT ( 'NONE',  ( 1.254009781011619307, -11.25324419414205224, 9.426200207651413976 ) ) ;
#12397=AXIS2_PLACEMENT_3D ( 'NONE', #10613, #2105, #6496 ) ;
#12400=ORIENTED_EDGE ( 'NONE', *, *, #12232, .T. ) ;
#12402=( BOUNDED_SURFACE ( )  B_SPLINE_SURFACE ( 3, 1, ( 
 ( #18246, #14114 ),
 ( #15365, #18415 ),
 ( #2367, #15280 ),
 ( #8124, #5328 ) ),
 .UNSPECIFIED., .F., .F., .T. ) 
 B_SPLINE_SURFACE_WITH_KNOTS ( ( 4, 4 ),
 ( 2, 2 ),
 ( 0.000000000000000000, 1.000000000000000000 ),
 ( 0.000000000000000000, 1.000000000000000000 ),
 .UNSPECIFIED. ) 
 GEOMETRIC_REPRESENTATION_ITEM ( )  RATIONAL_B_SPLINE_SURFACE ( (
 ( 1.000000000000000000, 1.000000000000000000),
 ( 0.9933953342250436691, 0.8357391271907733676),
 ( 0.9933953342250436691, 0.8357391271907733676),
 ( 1.000000000000000000, 1.000000000000000000) ) ) 
 REPRESENTATION_ITEM ( '' )  SURFACE ( )  );
#12403=LINE ( 'NONE', #10983, #3108 ) ;
#12405=CARTESIAN_POINT ( 'NONE',  ( 3.950837973638675393, 14.31366178983257242, -2.591948120961654833 ) ) ;
#12406=CARTESIAN_POINT ( 'NONE',  ( 16.58200780006414732, -0.01041078477704051979, -0.004047297414159007484 ) ) ;
#12407=B_SPLINE_CURVE_WITH_KNOTS ( 'NONE', 3,
 ( #17643, #16002, #4549, #4738, #16111, #2894 ),
 .UNSPECIFIED., .F., .F.,
 ( 4, 2, 4 ),
 ( 4.014301552767626103E-17, 0.0002014099069817288116, 0.0004028198139634175078 ),
 .UNSPECIFIED. ) ;
#12410=EDGE_CURVE ( 'NONE', #5432, #16388, #3473, .T. ) ;
#12414=CARTESIAN_POINT ( 'NONE',  ( 16.57210152137263393, -0.0006600038696348781500, -0.01453130299868639688 ) ) ;
#12415=ADVANCED_FACE ( 'NONE', ( #122 ), #7121, .F. ) ;
#12420=CARTESIAN_POINT ( 'NONE',  ( 0.3095370825347233956, 3.806662003783596759, -13.20347358821910433 ) ) ;
#12421=DIRECTION ( 'NONE',  ( -1.000000000000000000, -0.000000000000000000, -0.000000000000000000 ) ) ;
#12422=CARTESIAN_POINT ( 'NONE',  ( 3.377929128793397684, -9.234024516648242198, -10.50432311212913028 ) ) ;
#12423=CARTESIAN_POINT ( 'NONE',  ( 1.254255976357895763, -3.563435620217493494, -14.24071337840814166 ) ) ;
#12424=EDGE_LOOP ( 'NONE', ( #8299, #6380, #3357, #2267 ) ) ;
#12437=CARTESIAN_POINT ( 'NONE',  ( 3.512766787570921867, 14.81029789862138912, 2.682019731918403593 ) ) ;
#12443=CARTESIAN_POINT ( 'NONE',  ( 8.522092701127531811, 0.3779863304871219909, 6.946128462138597470 ) ) ;
#12444=ORIENTED_EDGE ( 'NONE', *, *, #2888, .T. ) ;
#12445=CARTESIAN_POINT ( 'NONE',  ( 16.57210152137263393, -0.01214401161737523396, 0.008007331252332839863 ) ) ;
#12446=B_SPLINE_CURVE_WITH_KNOTS ( 'NONE', 3,
 ( #10562, #11898, #17529, #16398, #7510, #17927 ),
 .UNSPECIFIED., .F., .F.,
 ( 4, 2, 4 ),
 ( 4.023840028577795923E-17, 0.0002014099069817275377, 0.0004028198139634147973 ),
 .UNSPECIFIED. ) ;
#12447=ORIENTED_EDGE ( 'NONE', *, *, #13767, .F. ) ;
#12449=CARTESIAN_POINT ( 'NONE',  ( 1.846138399168762101, 11.69739621335927815, -4.238866729160283064 ) ) ;
#12450=EDGE_LOOP ( 'NONE', ( #11685, #4202, #17917, #1999 ) ) ;
#12452=CARTESIAN_POINT ( 'NONE',  ( 2.636624412715362631, -15.80357026013197519, 2.862162146984090327 ) ) ;
#12453=CARTESIAN_POINT ( 'NONE',  ( 3.512766787570877902, 13.25664064834461264, 7.127386085302796381 ) ) ;
#12455=CARTESIAN_POINT ( 'NONE',  ( 16.58200780006414732, -0.009393638146078483672, -0.006043560077721808060 ) ) ;
#12456=CARTESIAN_POINT ( 'NONE',  ( 0.8740779401510752056, 3.609949156401575543, -13.83508928787453662 ) ) ;
#12457=CARTESIAN_POINT ( 'NONE',  ( 16.56872352241294521, 0.001442253899401802278, 0.01033355228142402403 ) ) ;
#12464=FACE_OUTER_BOUND ( 'NONE', #1105, .T. ) ;
#12465=CARTESIAN_POINT ( 'NONE',  ( 3.950837973638668288, 0.000000000000000000, 0.000000000000000000 ) ) ;
#12467=CARTESIAN_POINT ( 'NONE',  ( 1.846138399168762101, 6.971848976711011225, 10.30487220521572667 ) ) ;
#12469=CARTESIAN_POINT ( 'NONE',  ( 1.846138399168762101, -7.646096044339961040, 9.815003036200383946 ) ) ;
#12470=VERTEX_POINT ( 'NONE', #1363 ) ;
#12474=VERTEX_POINT ( 'NONE', #16379 ) ;
#12476=( BOUNDED_SURFACE ( )  B_SPLINE_SURFACE ( 3, 1, ( 
 ( #16495, #9414 ),
 ( #5108, #6167 ),
 ( #16589, #5011 ),
 ( #433, #13618 ) ),
 .UNSPECIFIED., .F., .F., .T. ) 
 B_SPLINE_SURFACE_WITH_KNOTS ( ( 4, 4 ),
 ( 2, 2 ),
 ( 0.000000000000000000, 1.000000000000000000 ),
 ( 0.000000000000000000, 1.000000000000000000 ),
 .UNSPECIFIED. ) 
 GEOMETRIC_REPRESENTATION_ITEM ( )  RATIONAL_B_SPLINE_SURFACE ( (
 ( 1.000000000000000000, 1.000000000000000000),
 ( 0.7792777138730160313, 0.9689936506012927220),
 ( 0.7792777138730160313, 0.9689936506012927220),
 ( 1.000000000000000000, 1.000000000000000000) ) ) 
 REPRESENTATION_ITEM ( '' )  SURFACE ( )  );
#12481=CARTESIAN_POINT ( 'NONE',  ( 1.845755665166724846, -11.67596932341231231, -4.296872077620800034 ) ) ;
#12482=CARTESIAN_POINT ( 'NONE',  ( 1.977436885026782276, -7.806953934146112495, -13.27782258181927233 ) ) ;
#12486=CARTESIAN_POINT ( 'NONE',  ( 0.4862570985993235340, 7.559321496869426227, 11.67702470553367711 ) ) ;
#12487=ORIENTED_EDGE ( 'NONE', *, *, #2062, .T. ) ;
#12489=VECTOR ( 'NONE', #12868, 1000.000000000000000 ) ;
#12492=VERTEX_POINT ( 'NONE', #10933 ) ;
#12493=CARTESIAN_POINT ( 'NONE',  ( 0.3145734862173242274, -0.3064017202076312341, 13.73540602248381148 ) ) ;
#12497=CARTESIAN_POINT ( 'NONE',  ( 2.747332970342022840, -14.63517873738952524, 7.289199830147050641 ) ) ;
#12500=CARTESIAN_POINT ( 'NONE',  ( 1.846138399168762989, 10.30487220521570357, 6.971848976711047641 ) ) ;
#12504=CARTESIAN_POINT ( 'NONE',  ( 0.3307726912345201886, -8.558645027434195640, -10.76786801061216714 ) ) ;
#12510=VERTEX_POINT ( 'NONE', #12171 ) ;
#12514=ADVANCED_FACE ( 'NONE', ( #514 ), #1893, .T. ) ;
#12515=ORIENTED_EDGE ( 'NONE', *, *, #7146, .T. ) ;
#12517=CARTESIAN_POINT ( 'NONE',  ( 1.847412631396504468, -12.44294644888238821, -0.04315047898448168967 ) ) ;
#12518=VERTEX_POINT ( 'NONE', #2217 ) ;
#12525=DIRECTION ( 'NONE',  ( 0.7635533937278216055, -0.6453904417649387604, -0.02138673900302107828 ) ) ;
#12528=CARTESIAN_POINT ( 'NONE',  ( 3.950837973638668288, 0.000000000000000000, 0.000000000000000000 ) ) ;
#12531=CARTESIAN_POINT ( 'NONE',  ( 0.3720661004400037664, 3.575426119359183197, 13.34435358167253938 ) ) ;
#12540=CARTESIAN_POINT ( 'NONE',  ( 16.56753206892534891, -0.004253784598196824578, -0.008490833999797990639 ) ) ;
#12545=CARTESIAN_POINT ( 'NONE',  ( 1.847412631396500249, -10.04119192206681177, -7.348689888531952263 ) ) ;
#12552=CARTESIAN_POINT ( 'NONE',  ( 1.861628059977341154, 7.751680370225533245, -9.751736252960284901 ) ) ;
#12557=CARTESIAN_POINT ( 'NONE',  ( 2.320521194583335500, -13.71278319228129483, -7.743190876766059105 ) ) ;
#12558=CARTESIAN_POINT ( 'NONE',  ( 0.3137051932979757485, -7.698472063774552510, 11.37800749014128421 ) ) ;
#12563=ORIENTED_EDGE ( 'NONE', *, *, #10629, .F. ) ;
#12565=EDGE_CURVE ( 'NONE', #4649, #8892, #13475, .T. ) ;
#12571=CARTESIAN_POINT ( 'NONE',  ( 1.342453679581834924, -5.476372339890114738, 13.74702459364882401 ) ) ;
#12572=AXIS2_PLACEMENT_3D ( 'NONE', #17772, #16617, #4676 ) ;
#12573=CARTESIAN_POINT ( 'NONE',  ( 0.3148208552358916501, -12.99355031785208681, 4.463611911212169936 ) ) ;
#12574=LINE ( 'NONE', #12947, #13028 ) ;
#12582=CARTESIAN_POINT ( 'NONE',  ( 0.4754618798421171855, -12.98792082933648118, 5.007009103465197342 ) ) ;
#12591=CIRCLE ( 'NONE', #4357, 14.54644660717763927 ) ;
#12595=CARTESIAN_POINT ( 'NONE',  ( 16.56753206892534891, 0.004253784598196760393, 0.008490833999798020129 ) ) ;
#12596=CARTESIAN_POINT ( 'NONE',  ( 0.3150692679895995552, 11.02465386701228844, 8.199139630396045320 ) ) ;
#12598=CARTESIAN_POINT ( 'NONE',  ( 16.56782317627811096, 0.005492611183757310257, -0.008141063682853423578 ) ) ;
#12601=FACE_OUTER_BOUND ( 'NONE', #12225, .T. ) ;
#12604=LINE ( 'NONE', #11099, #905 ) ;
#12605=CARTESIAN_POINT ( 'NONE',  ( 2.636624412717140764, -2.862162146982851763, -15.80357026013259514 ) ) ;
#12618=CIRCLE ( 'NONE', #2845, 16.06066017081991149 ) ;
#12620=VERTEX_POINT ( 'NONE', #5362 ) ;
#12621=CARTESIAN_POINT ( 'NONE',  ( 16.58200780006414732, -0.01080144354108868512, -0.002844973367391535370 ) ) ;
#12622=CARTESIAN_POINT ( 'NONE',  ( 1.977436885026099711, -15.33079650480437550, -1.488549889122204650 ) ) ;
#12624=EDGE_LOOP ( 'NONE', ( #3826, #1835, #7404, #11052 ) ) ;
#12626=CARTESIAN_POINT ( 'NONE',  ( 0.3150690434770175852, 0.1531837610935626592, -13.73846430619029313 ) ) ;
#12628=CARTESIAN_POINT ( 'NONE',  ( 3.950837973638677170, 13.10350451991849141, -6.316429227969337923 ) ) ;
#12629=CARTESIAN_POINT ( 'NONE',  ( 0.3720661004400040439, -13.79610186261030513, 0.7231997263364323691 ) ) ;
#12641=ADVANCED_FACE ( 'NONE', ( #2307 ), #8459, .F. ) ;
#12645=CARTESIAN_POINT ( 'NONE',  ( 3.950837973638677170, -1.958075594453692503, -14.41405733518062959 ) ) ;
#12651=B_SPLINE_CURVE_WITH_KNOTS ( 'NONE', 3,
 ( #734, #15260, #561, #6566, #16790, #4854 ),
 .UNSPECIFIED., .F., .F.,
 ( 4, 2, 4 ),
 ( 0.000000000000000000, 0.001656992708823243950, 0.003313985417646487033 ),
 .UNSPECIFIED. ) ;
#12654=ORIENTED_EDGE ( 'NONE', *, *, #9025, .F. ) ;
#12659=CARTESIAN_POINT ( 'NONE',  ( 0.3148213771069354738, 13.13560149728606419, -4.026433757158845772 ) ) ;
#12661=LINE ( 'NONE', #11522, #15411 ) ;
#12666=CARTESIAN_POINT ( 'NONE',  ( 0.3132635586635982849, 7.641727604904055227, -11.41586812343481583 ) ) ;
#12669=DIRECTION ( 'NONE',  ( -0.7561779333270775005, 0.6534392409364818688, -0.03481510524965020920 ) ) ;
#12683=ORIENTED_EDGE ( 'NONE', *, *, #14449, .T. ) ;
#12684=CARTESIAN_POINT ( 'NONE',  ( 1.847461586945732037, 10.08650590720936258, 7.286856109515091440 ) ) ;
#12685=CARTESIAN_POINT ( 'NONE',  ( 16.56872352241294521, 0.004564908236399969378, -0.009382111268607383134 ) ) ;
#12689=FACE_OUTER_BOUND ( 'NONE', #7244, .T. ) ;
#12695=VERTEX_POINT ( 'NONE', #18547 ) ;
#12697=ORIENTED_EDGE ( 'NONE', *, *, #5855, .T. ) ;
#12698=CARTESIAN_POINT ( 'NONE',  ( 0.3132635586635980629, 4.743936529203241825, 12.89236642382223508 ) ) ;
#12699=CARTESIAN_POINT ( 'NONE',  ( 16.56782317627811096, 0.006045301465876630996, 0.007739510688078455984 ) ) ;
#12700=ADVANCED_FACE ( 'NONE', ( #9837, #15671 ), #2572, .F. ) ;
#12710=CARTESIAN_POINT ( 'NONE',  ( 1.846822687350018866, 12.43915556955403900, 0.2922081769260583273 ) ) ;
#12718=CARTESIAN_POINT ( 'NONE',  ( 0.3095370825347224519, 8.444334731364161684, -10.84046130709049471 ) ) ;
#12721=CARTESIAN_POINT ( 'NONE',  ( 0.4862570985993235340, 0.7479633556564388996, -13.89016912371016765 ) ) ;
#12722=B_SPLINE_CURVE_WITH_KNOTS ( 'NONE', 3,
 ( #9561, #6795, #16921, #6886, #15571, #3734 ),
 .UNSPECIFIED., .F., .F.,
 ( 4, 2, 4 ),
 ( 0.000000000000000000, 0.001656992708822367915, 0.003313985417644735830 ),
 .UNSPECIFIED. ) ;
#12725=CARTESIAN_POINT ( 'NONE',  ( 0.3150692679895995552, -13.01874238516607285, -4.391039771493804089 ) ) ;
#12730=ORIENTED_EDGE ( 'NONE', *, *, #4932, .F. ) ;
#12731=CIRCLE ( 'NONE', #6946, 5.000000000000000000 ) ;
#12733=CARTESIAN_POINT ( 'NONE',  ( 2.320521194583478941, 3.126729093671432480, -15.43440938317170641 ) ) ;
#12734=CARTESIAN_POINT ( 'NONE',  ( 0.3151930723728453843, -4.318364831037682094, 13.04315954105013198 ) ) ;
#12741=CARTESIAN_POINT ( 'NONE',  ( 0.4384471787762845851, -4.978024343488958614, -12.93784327393178302 ) ) ;
#12742=CARTESIAN_POINT ( 'NONE',  ( 2.636624412715137922, -14.46769361191291559, 6.973567714907789927 ) ) ;
#12744=ORIENTED_EDGE ( 'NONE', *, *, #5440, .T. ) ;
#12745=CARTESIAN_POINT ( 'NONE',  ( 0.4754618798421162973, -3.583352865732763792, 13.45049478164058776 ) ) ;
#12750=EDGE_CURVE ( 'NONE', #11838, #1858, #1926, .T. ) ;
#12751=ORIENTED_EDGE ( 'NONE', *, *, #10512, .F. ) ;
#12752=EDGE_LOOP ( 'NONE', ( #4554, #6308, #14344, #15848, #14304, #2019, #17942, #8199, #4596, #4403, #3453, #14409, #10184, #14580, #14442, #7329, #9759, #15537, #16783, #12204, #6538, #4874, #12292, #518, #12952, #10772, #13427, #6697, #7959, #4401, #16210, #2739, #9631, #17183, #4975, #2428, #1680, #17256, #861, #17604, #7575, #17190, #13301, #3037, #4744, #10945, #16941, #2167, #11713, #5371, #7554, #9293, #7043, #16939, #11081, #4973, #4938, #9572, #10281, #10799, #17122, #4936, #11586, #12214 ) ) ;
#12754=LINE ( 'NONE', #11424, #7526 ) ;
#12758=VECTOR ( 'NONE', #3274, 1000.000000000000227 ) ;
#12760=CARTESIAN_POINT ( 'NONE',  ( 8.522092701127531811, -1.786985377232080285, 6.722964936702092054 ) ) ;
#12761=CARTESIAN_POINT ( 'NONE',  ( 2.747332970342022840, 2.705255688518072965, -16.12459247543623064 ) ) ;
#12767=VERTEX_POINT ( 'NONE', #17698 ) ;
#12769=EDGE_CURVE ( 'NONE', #13818, #18306, #1672, .T. ) ;
#12771=CARTESIAN_POINT ( 'NONE',  ( 1.847412631396500249, 10.09191835241973934, -7.278870946904142158 ) ) ;
#12775=VERTEX_POINT ( 'NONE', #8985 ) ;
#12777=CARTESIAN_POINT ( 'NONE',  ( 2.636624412714756005, -2.161493821597335607, 15.91454522070219113 ) ) ;
#12779=CARTESIAN_POINT ( 'NONE',  ( 1.254009781011695468, -14.24044713813331597, -3.563484327698402510 ) ) ;
#12780=EDGE_CURVE ( 'NONE', #9066, #8143, #12835, .T. ) ;
#12783=FACE_OUTER_BOUND ( 'NONE', #4054, .T. ) ;
#12784=CARTESIAN_POINT ( 'NONE',  ( 8.522092701127531811, 1.786985377232031436, 6.722964936702105376 ) ) ;
#12791=CARTESIAN_POINT ( 'NONE',  ( 3.950837973638668288, 0.000000000000000000, 0.000000000000000000 ) ) ;
#12794=EDGE_CURVE ( 'NONE', #10403, #14985, #993, .T. ) ;
#12796=CARTESIAN_POINT ( 'NONE',  ( 1.846138399168762101, -12.43476674860266229, -0.4167076046096845898 ) ) ;
#12800=ORIENTED_EDGE ( 'NONE', *, *, #10426, .T. ) ;
#12802=VECTOR ( 'NONE', #9360, 1000.000000000000000 ) ;
#12804=CARTESIAN_POINT ( 'NONE',  ( 0.3132642857406529591, -13.72733058964894681, -0.5276792104583708509 ) ) ;
#12805=DIRECTION ( 'NONE',  ( 0.000000000000000000, 0.000000000000000000, 1.000000000000000000 ) ) ;
#12811=ORIENTED_EDGE ( 'NONE', *, *, #16963, .T. ) ;
#12814=B_SPLINE_CURVE_WITH_KNOTS ( 'NONE', 3,
 ( #4830, #12090, #16583, #17925, #9028, #4636, #3478, #7901, #5959, #10460, #16297, #3666, #18105 ),
 .UNSPECIFIED., .F., .F.,
 ( 4, 3, 3, 3, 4 ),
 ( 3.144186300207962859E-18, 0.0002299780670421060105, 0.0004599561239687904998, 0.0006896788984287882803, 0.0009194956271626397379 ),
 .UNSPECIFIED. ) ;
#12816=CARTESIAN_POINT ( 'NONE',  ( 0.3307726912345211323, -0.5948952607471654774, -13.74203354050372461 ) ) ;
#12817=CARTESIAN_POINT ( 'NONE',  ( 0.3137051932979792457, 0.4596302728641686874, -13.73004976592201487 ) ) ;
#12819=CARTESIAN_POINT ( 'NONE',  ( 2.636624412715138366, -11.10302021257964888, 11.60464335004044223 ) ) ;
#12822=CARTESIAN_POINT ( 'NONE',  ( 0.3151926232592536792, -11.07013665200800645, 8.137833541809341042 ) ) ;
#12823=CARTESIAN_POINT ( 'NONE',  ( 2.636624412714236865, 0.000000000000000000, 0.000000000000000000 ) ) ;
#12829=CARTESIAN_POINT ( 'NONE',  ( 1.846138399168762101, -4.238866729160323032, -11.69739621335926394 ) ) ;
#12834=CARTESIAN_POINT ( 'NONE',  ( 16.56753206892534891, -0.001421777558676855365, -0.009389754735541546229 ) ) ;
#12835=B_SPLINE_CURVE_WITH_KNOTS ( 'NONE', 3,
 ( #3039, #10231, #8887, #4597 ),
 .UNSPECIFIED., .F., .F.,
 ( 4, 4 ),
 ( 0.000000000000000000, 0.002004993803842297466 ),
 .UNSPECIFIED. ) ;
#12840=ORIENTED_EDGE ( 'NONE', *, *, #922, .T. ) ;
#12841=CARTESIAN_POINT ( 'NONE',  ( 0.3150690434770172521, -0.1531837610934980720, 13.73846430619029491 ) ) ;
#12852=CARTESIAN_POINT ( 'NONE',  ( 0.3148208552358917611, -0.2299193288886511033, -13.73693263646119078 ) ) ;
#12853=CARTESIAN_POINT ( 'NONE',  ( 0.3720661004400040439, -12.89739157014196635, 4.951033743989591507 ) ) ;
#12854=DIRECTION ( 'NONE',  ( 0.7635533937278216055, -0.2197766120036547532, 0.6071939193889553943 ) ) ;
#12855=VERTEX_POINT ( 'NONE', #10522 ) ;
#12858=ORIENTED_EDGE ( 'NONE', *, *, #192, .F. ) ;
#12861=B_SPLINE_CURVE_WITH_KNOTS ( 'NONE', 3,
 ( #10865, #2336, #906, #13721, #12557, #8180 ),
 .UNSPECIFIED., .F., .F.,
 ( 4, 2, 4 ),
 ( 1.084202172485504314E-19, 0.001657017934711308349, 0.003314035869422615830 ),
 .UNSPECIFIED. ) ;
#12863=CARTESIAN_POINT ( 'NONE',  ( 8.438534575730034959, -0.2320579683289648587, -6.862570336891078426 ) ) ;
#12868=DIRECTION ( 'NONE',  ( 0.7561779333270775005, -0.03481510524965699543, 0.6534392409364816467 ) ) ;
#12871=B_SPLINE_CURVE_WITH_KNOTS ( 'NONE', 3,
 ( #16763, #2057, #7900, #9409 ),
 .UNSPECIFIED., .F., .F.,
 ( 4, 4 ),
 ( 0.000000000000000000, 0.002004993803842607548 ),
 .UNSPECIFIED. ) ;
#12883=ADVANCED_FACE ( 'NONE', ( #10716 ), #7013, .F. ) ;
#12884=ORIENTED_EDGE ( 'NONE', *, *, #566, .T. ) ;
#12885=CARTESIAN_POINT ( 'NONE',  ( 0.3308579732647013438, -3.680601586799781000, -13.25341063505879546 ) ) ;
#12886=CARTESIAN_POINT ( 'NONE',  ( 1.847034903785823579, -12.44051878787772836, -0.2299360331935480506 ) ) ;
#12888=CARTESIAN_POINT ( 'NONE',  ( 2.123976203522053297, 13.47898556379324297, -7.899625852120059299 ) ) ;
#12901=ORIENTED_EDGE ( 'NONE', *, *, #16232, .F. ) ;
#12906=EDGE_LOOP ( 'NONE', ( #135, #7288, #18118, #9177 ) ) ;
#12907=CARTESIAN_POINT ( 'NONE',  ( 8.522092701127531811, -6.489356537178209372, 2.505958102592595882 ) ) ;
#12911=CARTESIAN_POINT ( 'NONE',  ( 0.3132642857406558456, 10.79548167658034608, 8.495623922778108295 ) ) ;
#12912=ORIENTED_EDGE ( 'NONE', *, *, #17435, .T. ) ;
#12913=CARTESIAN_POINT ( 'NONE',  ( 16.56872352241294521, -0.01033355228142500762, -0.001442253899401184716 ) ) ;
#12915=CARTESIAN_POINT ( 'NONE',  ( 0.3148208552358935375, -4.026279359288518656, 13.13564827777588029 ) ) ;
#12918=B_SPLINE_CURVE_WITH_KNOTS ( 'NONE', 3,
 ( #13352, #8857, #9050, #559, #4464, #356 ),
 .UNSPECIFIED., .F., .F.,
 ( 4, 2, 4 ),
 ( 2.468197616305571356E-18, 0.0002017457492448094245, 0.0004034914984896164096 ),
 .UNSPECIFIED. ) ;
#12923=CARTESIAN_POINT ( 'NONE',  ( 1.846138399168762101, -6.971848976711082280, 10.30487220521567693 ) ) ;
#12927=VERTEX_POINT ( 'NONE', #14589 ) ;
#12929=SURFACE_SIDE_STYLE ('',( #15607 ) ) ;
#12933=CARTESIAN_POINT ( 'NONE',  ( 1.847426409206450959, -2.029922383240494730E-11, 12.44303504652081038 ) ) ;
#12935=VECTOR ( 'NONE', #16329, 1000.000000000000114 ) ;
#12936=ORIENTED_EDGE ( 'NONE', *, *, #428, .T. ) ;
#12937=CARTESIAN_POINT ( 'NONE',  ( 0.3142014840576501378, -0.3830336514509840029, 13.73311050063163918 ) ) ;
#12939=ORIENTED_EDGE ( 'NONE', *, *, #10209, .F. ) ;
#12941=CARTESIAN_POINT ( 'NONE',  ( 0.3137051932979757485, 12.91601973349276733, -4.679953077377353665 ) ) ;
#12944=DIRECTION ( 'NONE',  ( -0.7561779333270775005, -0.1688126975276600938, 0.6322161072786937064 ) ) ;
#12947=CARTESIAN_POINT ( 'NONE',  ( 16.57605080000000086, 4.769696007084728073, 1.500000000000000000 ) ) ;
#12952=ORIENTED_EDGE ( 'NONE', *, *, #5570, .F. ) ;
#12965=CARTESIAN_POINT ( 'NONE',  ( 1.846613052777651198, 4.166957398589849149, 11.72395935470500028 ) ) ;
#12967=( BOUNDED_SURFACE ( )  B_SPLINE_SURFACE ( 3, 1, ( 
 ( #18777, #16978 ),
 ( #2801, #9791 ),
 ( #7130, #11528 ),
 ( #15622, #3887 ) ),
 .UNSPECIFIED., .F., .F., .T. ) 
 B_SPLINE_SURFACE_WITH_KNOTS ( ( 4, 4 ),
 ( 2, 2 ),
 ( 0.000000000000000000, 1.000000000000000000 ),
 ( 0.000000000000000000, 1.000000000000000000 ),
 .UNSPECIFIED. ) 
 GEOMETRIC_REPRESENTATION_ITEM ( )  RATIONAL_B_SPLINE_SURFACE ( (
 ( 1.000000000000000000, 1.000000000000000000),
 ( 0.9933953342250436691, 0.8357391271907733676),
 ( 0.9933953342250436691, 0.8357391271907733676),
 ( 1.000000000000000000, 1.000000000000000000) ) ) 
 REPRESENTATION_ITEM ( '' )  SURFACE ( )  );
#12969=ORIENTED_EDGE ( 'NONE', *, *, #6980, .F. ) ;
#12970=AXIS2_PLACEMENT_3D ( 'NONE', #8529, #9766, #18742 ) ;
#12980=CARTESIAN_POINT ( 'NONE',  ( 2.636624412716062071, -14.14563173255412742, -7.605649742760987486 ) ) ;
#12982=CARTESIAN_POINT ( 'NONE',  ( 0.3058872367615230181, 7.578326039752771415, -11.46514199369349818 ) ) ;
#12987=CARTESIAN_POINT ( 'NONE',  ( 2.002547531651519996, 4.532360870844494016, -11.75462648437097180 ) ) ;
#12990=CARTESIAN_POINT ( 'NONE',  ( 3.950837973638675393, -2.591948120961706792, -14.31366178983255466 ) ) ;
#12992=DIRECTION ( 'NONE',  ( -1.000000000000000000, -0.000000000000000000, -0.000000000000000000 ) ) ;
#12994=B_SPLINE_CURVE_WITH_KNOTS ( 'NONE', 3,
 ( #14488, #13151, #5590, #15731, #2723, #2632, #8479, #63, #11443, #17261, #14394, #17457, #8568 ),
 .UNSPECIFIED., .F., .F.,
 ( 4, 3, 3, 3, 4 ),
 ( 2.453269466693398698E-18, 0.0002299780670421020532, 0.0004599561239687888735, 0.0006896788984287890393, 0.0009194956271626411473 ),
 .UNSPECIFIED. ) ;
#12995=CARTESIAN_POINT ( 'NONE',  ( 1.846138399168762101, 6.971848976711159551, -10.30487220521562541 ) ) ;
#12996=CARTESIAN_POINT ( 'NONE',  ( 0.4754618798421167414, 3.583352865732670534, 13.45049478164061263 ) ) ;
#12997=ORIENTED_EDGE ( 'NONE', *, *, #3339, .T. ) ;
#13000=CARTESIAN_POINT ( 'NONE',  ( 1.846138399168762101, -9.815003036200353748, -7.646096044340000120 ) ) ;
#13003=CARTESIAN_POINT ( 'NONE',  ( 0.3132635586635977298, -0.5277914263192144961, -13.72732610560089128 ) ) ;
#13005=EDGE_LOOP ( 'NONE', ( #14559, #16914, #17159, #11072 ) ) ;
#13009=LINE ( 'NONE', #1067, #8514 ) ;
#13014=COLOUR_RGB ( '', 0.40784314, 0.44705882, 0.49803922) ;
#13019=CARTESIAN_POINT ( 'NONE',  ( 2.747332970342022840, 16.17136872824898575, -2.409922051470736459 ) ) ;
#13023=AXIS2_PLACEMENT_3D ( 'NONE', #13100, #16358, #17791 ) ;
#13024=ORIENTED_EDGE ( 'NONE', *, *, #9317, .F. ) ;
#13026=CARTESIAN_POINT ( 'NONE',  ( 0.3095370825347224519, -11.38092634279633941, 7.700448427571837229 ) ) ;
#13027=ORIENTED_EDGE ( 'NONE', *, *, #8387, .F. ) ;
#13028=VECTOR ( 'NONE', #18679, 1000.000000000000000 ) ;
#13032=CARTESIAN_POINT ( 'NONE',  ( 1.846138399168762101, -3.446241763652916124, -11.95493567637853971 ) ) ;
#13037=CARTESIAN_POINT ( 'NONE',  ( 0.3151928476913548605, 13.06671852871095574, -4.245853234426248513 ) ) ;
#13058=CARTESIAN_POINT ( 'NONE',  ( 2.636624412714763555, 6.973567714907159321, 14.46769361191226722 ) ) ;
#13064=CARTESIAN_POINT ( 'NONE',  ( 1.918921323896210840, 9.738309537478938793, 7.860085869556105109 ) ) ;
#13066=FACE_OUTER_BOUND ( 'NONE', #12624, .T. ) ;
#13068=EDGE_LOOP ( 'NONE', ( #5374, #3085, #11437, #17353 ) ) ;
#13072=ORIENTED_EDGE ( 'NONE', *, *, #11297, .F. ) ;
#13073=B_SPLINE_CURVE_WITH_KNOTS ( 'NONE', 3,
 ( #17852, #3405, #12018, #15346, #9437, #18224 ),
 .UNSPECIFIED., .F., .F.,
 ( 4, 2, 4 ),
 ( 2.710505431213761085E-19, 0.001657017934710631590, 0.003314035869421263179 ),
 .UNSPECIFIED. ) ;
#13079=CARTESIAN_POINT ( 'NONE',  ( 3.950837973638675393, -10.51028938476210328, -10.05648675950137871 ) ) ;
#13082=ORIENTED_EDGE ( 'NONE', *, *, #15084, .F. ) ;
#13087=( BOUNDED_SURFACE ( )  B_SPLINE_SURFACE ( 3, 1, ( 
 ( #919, #18398 ),
 ( #11156, #14098 ),
 ( #7034, #15717 ),
 ( #9708, #3883 ) ),
 .UNSPECIFIED., .F., .F., .T. ) 
 B_SPLINE_SURFACE_WITH_KNOTS ( ( 4, 4 ),
 ( 2, 2 ),
 ( 0.000000000000000000, 1.000000000000000000 ),
 ( 0.000000000000000000, 1.000000000000000000 ),
 .UNSPECIFIED. ) 
 GEOMETRIC_REPRESENTATION_ITEM ( )  RATIONAL_B_SPLINE_SURFACE ( (
 ( 1.000000000000000000, 1.000000000000000000),
 ( 0.9593108457356467333, 0.9995965569486454649),
 ( 0.9593108457356467333, 0.9995965569486454649),
 ( 1.000000000000000000, 1.000000000000000000) ) ) 
 REPRESENTATION_ITEM ( '' )  SURFACE ( )  );
#13088=CARTESIAN_POINT ( 'NONE',  ( 1.847168016377983335, 11.89018175117595177, 3.666915430942639720 ) ) ;
#13093=EDGE_CURVE ( 'NONE', #2050, #7024, #13073, .T. ) ;
#13098=CARTESIAN_POINT ( 'NONE',  ( 0.4862570985993252548, -12.97920246947875889, -5.003653737315625349 ) ) ;
#13100=CARTESIAN_POINT ( 'NONE',  ( 3.950837973638668288, 0.000000000000000000, 0.000000000000000000 ) ) ;
#13101=ORIENTED_EDGE ( 'NONE', *, *, #15062, .T. ) ;
#13105=CARTESIAN_POINT ( 'NONE',  ( 16.56872352241294521, -0.004907101719995745834, -0.009207754980064182873 ) ) ;
#13109=CARTESIAN_POINT ( 'NONE',  ( 16.56753206892534891, 0.006760771273035115839, -0.006669401563385219701 ) ) ;
#13115=CARTESIAN_POINT ( 'NONE',  ( 3.512766787570772653, -2.682019731918489303, 14.81029789862156143 ) ) ;
#13117=CARTESIAN_POINT ( 'NONE',  ( 16.58200780006414732, -0.008650561019685578876, 0.007066318000004673597 ) ) ;
#13123=( BOUNDED_SURFACE ( )  B_SPLINE_SURFACE ( 3, 1, ( 
 ( #12685, #2109 ),
 ( #12414, #7949 ),
 ( #9460, #13755 ),
 ( #9541, #3624 ) ),
 .UNSPECIFIED., .F., .F., .T. ) 
 B_SPLINE_SURFACE_WITH_KNOTS ( ( 4, 4 ),
 ( 2, 2 ),
 ( 0.000000000000000000, 1.000000000000000000 ),
 ( 0.000000000000000000, 1.000000000000000000 ),
 .UNSPECIFIED. ) 
 GEOMETRIC_REPRESENTATION_ITEM ( )  RATIONAL_B_SPLINE_SURFACE ( (
 ( 1.000000000000000000, 1.000000000000000000),
 ( 0.7792777138730160313, 0.9689936506012927220),
 ( 0.7792777138730160313, 0.9689936506012927220),
 ( 1.000000000000000000, 1.000000000000000000) ) ) 
 REPRESENTATION_ITEM ( '' )  SURFACE ( )  );
#13125=ORIENTED_EDGE ( 'NONE', *, *, #15086, .F. ) ;
#13126=ORIENTED_EDGE ( 'NONE', *, *, #5186, .F. ) ;
#13131=EDGE_CURVE ( 'NONE', #15452, #11172, #4180, .T. ) ;
#13136=CARTESIAN_POINT ( 'NONE',  ( 0.3145729642390363567, -7.825496023201391260, 11.29233589755989797 ) ) ;
#13140=CARTESIAN_POINT ( 'NONE',  ( 16.57778382496167424, 0.01018821665058777630, -0.01092721432668997822 ) ) ;
#13141=CARTESIAN_POINT ( 'NONE',  ( 16.57778382496167424, 0.002851818597093999999, -0.01466529584256785410 ) ) ;
#13145=VERTEX_POINT ( 'NONE', #18042 ) ;
#13146=ORIENTED_EDGE ( 'NONE', *, *, #5514, .T. ) ;
#13148=ADVANCED_FACE ( 'NONE', ( #13820 ), #13593, .F. ) ;
#13150=CARTESIAN_POINT ( 'NONE',  ( 1.959283090834856633, -0.6676170829051342182, -12.53713130127478692 ) ) ;
#13151=CARTESIAN_POINT ( 'NONE',  ( 0.3142014840576500267, 8.382000553815611710, -10.88517824918533883 ) ) ;
#13154=EDGE_CURVE ( 'NONE', #14694, #12032, #8101, .T. ) ;
#13157=CARTESIAN_POINT ( 'NONE',  ( 2.002547531651519996, -3.242439124566736997, 12.17374746633577232 ) ) ;
#13161=CARTESIAN_POINT ( 'NONE',  ( 1.977228804422057840, -3.321884655132009811, 15.04020501276143662 ) ) ;
#13162=CARTESIAN_POINT ( 'NONE',  ( 0.3151930723728431083, -11.07033375389125673, -8.137566970826481949 ) ) ;
#13163=CARTESIAN_POINT ( 'NONE',  ( 0.000000000000000000, 0.000000000000000000, 0.000000000000000000 ) ) ;
#13164=EDGE_LOOP ( 'NONE', ( #4956, #9777, #9602, #8946 ) ) ;
#13183=CARTESIAN_POINT ( 'NONE',  ( 0.3151928476913583022, 13.06684726503526761, 4.245457024760265874 ) ) ;
#13185=CIRCLE ( 'NONE', #8027, 16.06066017081991149 ) ;
#13186=CARTESIAN_POINT ( 'NONE',  ( 1.847247051441592181, 7.448813758297314180, -9.967131402978116839 ) ) ;
#13188=VERTEX_POINT ( 'NONE', #1895 ) ;
#13192=CARTESIAN_POINT ( 'NONE',  ( 0.4384471787762841966, -0.7363690479465361260, -13.84291427302852817 ) ) ;
#13197=FACE_OUTER_BOUND ( 'NONE', #13164, .T. ) ;
#13204=VECTOR ( 'NONE', #12944, 1000.000000000000114 ) ;
#13207=FACE_OUTER_BOUND ( 'NONE', #15778, .T. ) ;
#13209=CARTESIAN_POINT ( 'NONE',  ( 16.56872352241294521, -0.004564908236400030961, 0.009382111268607351909 ) ) ;
#13212=CARTESIAN_POINT ( 'NONE',  ( 16.56753206892534891, 0.006669401563384923931, -0.006760771273036191367 ) ) ;
#13221=EDGE_CURVE ( 'NONE', #13922, #12855, #83, .T. ) ;
#13225=CARTESIAN_POINT ( 'NONE',  ( 0.4754618798421171855, 8.775436892861110394, 10.80499583390516172 ) ) ;
#13228=UNCERTAINTY_MEASURE_WITH_UNIT (LENGTH_MEASURE( 1.000000000000000082E-05 ), #17202, 'distance_accuracy_value', 'NONE');
#13231=CARTESIAN_POINT ( 'NONE',  ( 16.58200780006414732, -0.006043560077721775101, 0.009393638146078504489 ) ) ;
#13234=CARTESIAN_POINT ( 'NONE',  ( 2.747332970342022840, -14.63517873738941866, -7.289199830147261139 ) ) ;
#13236=B_SPLINE_CURVE_WITH_KNOTS ( 'NONE', 3,
 ( #15905, #14466, #1090, #17438, #11332, #14565 ),
 .UNSPECIFIED., .F., .F.,
 ( 4, 2, 4 ),
 ( 2.790109556687801058E-18, 0.0002017457492448093974, 0.0004034914984896159759 ),
 .UNSPECIFIED. ) ;
#13237=CARTESIAN_POINT ( 'NONE',  ( 0.3170788640506440603, 13.11595226728163510, -4.100430649997826471 ) ) ;
#13238=CARTESIAN_POINT ( 'NONE',  ( 2.320521194582656932, -15.64520804578280888, 1.795798718313643683 ) ) ;
#13239=ORIENTED_EDGE ( 'NONE', *, *, #3588, .T. ) ;
#13240=ORIENTED_EDGE ( 'NONE', *, *, #318, .T. ) ;
#13242=ORIENTED_EDGE ( 'NONE', *, *, #15062, .F. ) ;
#13243=CARTESIAN_POINT ( 'NONE',  ( 3.950837973638676281, 6.316429227969464932, 13.10350451991842569 ) ) ;
#13246=ORIENTED_EDGE ( 'NONE', *, *, #11389, .F. ) ;
#13249=CONICAL_SURFACE ( 'NONE', #11728, 14.54644660717763927, 0.8559913436420816257 ) ;
#13252=CARTESIAN_POINT ( 'NONE',  ( 3.950837973638675393, 14.31366178983257242, -2.591948120961654833 ) ) ;
#13254=CARTESIAN_POINT ( 'NONE',  ( 2.636624412716062071, -11.10302021258080352, -11.60464335004061454 ) ) ;
#13258=B_SPLINE_CURVE_WITH_KNOTS ( 'NONE', 3,
 ( #1006, #11250, #6845, #9984, #7035, #17069, #12852, #2711, #3884, #11339 ),
 .UNSPECIFIED., .F., .F.,
 ( 4, 3, 3, 4 ),
 ( 0.0004597478348665241538, 0.0004599561239687906082, 0.0006896788984287882803, 0.0009194956271626397379 ),
 .UNSPECIFIED. ) ;
#13272=CARTESIAN_POINT ( 'NONE',  ( 1.846822687350026193, -4.121816957446279517, 11.74004266906802663 ) ) ;
#13273=EDGE_CURVE ( 'NONE', #4376, #6482, #9194, .T. ) ;
#13276=B_SPLINE_CURVE_WITH_KNOTS ( 'NONE', 3,
 ( #9571, #4024, #15772, #8518, #16262, #5824 ),
 .UNSPECIFIED., .F., .F.,
 ( 4, 2, 4 ),
 ( 8.673617379884035472E-19, 0.001500839035891552223, 0.003001678071783103578 ),
 .UNSPECIFIED. ) ;
#13279=AXIS2_PLACEMENT_3D ( 'NONE', #7709, #9750, #12094 ) ;
#13284=CARTESIAN_POINT ( 'NONE',  ( 1.847426409206449405, 0.01438352405959898543, -12.44303504652077841 ) ) ;
#13285=ORIENTED_EDGE ( 'NONE', *, *, #11491, .F. ) ;
#13286=CARTESIAN_POINT ( 'NONE',  ( 1.562796894703937678, 0.000000000000000000, 0.000000000000000000 ) ) ;
#13296=CARTESIAN_POINT ( 'NONE',  ( 16.56679352167444819, 0.004277682826582259769, -0.008252760440870513317 ) ) ;
#13299=CARTESIAN_POINT ( 'NONE',  ( 0.3132642857406504611, -7.641821025099783782, -11.41580579227785464 ) ) ;
#13301=ORIENTED_EDGE ( 'NONE', *, *, #962, .F. ) ;
#13306=CARTESIAN_POINT ( 'NONE',  ( 2.123976203522053741, -15.26039569100257509, -3.347755036806064677 ) ) ;
#13307=CARTESIAN_POINT ( 'NONE',  ( 2.697797270744668019, 11.26906156738836984, -7.053988368581739721 ) ) ;
#13310=VERTEX_POINT ( 'NONE', #15100 ) ;
#13315=CARTESIAN_POINT ( 'NONE',  ( 0.3151928476913523069, 11.11514699826562946, -8.075884471919630769 ) ) ;
#13326=CARTESIAN_POINT ( 'NONE',  ( 8.522092701127531811, 6.489356537178190720, 2.505958102592644288 ) ) ;
#13331=CARTESIAN_POINT ( 'NONE',  ( 8.522092701127531811, -5.397361180353110299, -4.388629235579637466 ) ) ;
#13342=ORIENTED_EDGE ( 'NONE', *, *, #4635, .T. ) ;
#13352=CARTESIAN_POINT ( 'NONE',  ( 0.3137051932979757485, -11.37800749014125223, -7.698472063774596030 ) ) ;
#13355=CARTESIAN_POINT ( 'NONE',  ( 0.3151926232592457966, 8.137833541809381899, 11.07013665200797625 ) ) ;
#13356=CARTESIAN_POINT ( 'NONE',  ( 3.950837973638676281, 13.10350451991840615, 6.316429227969512894 ) ) ;
#13357=LINE ( 'NONE', #174, #12935 ) ;
#13358=CARTESIAN_POINT ( 'NONE',  ( 2.636624412716902288, 7.605649742760546950, -14.14563173255513995 ) ) ;
#13360=VECTOR ( 'NONE', #2434, 1000.000000000000227 ) ;
#13362=VERTEX_POINT ( 'NONE', #2731 ) ;
#13364=ADVANCED_FACE ( 'NONE', ( #12783 ), #5057, .F. ) ;
#13366=CARTESIAN_POINT ( 'NONE',  ( 1.846138399168762101, -11.95493567637848109, -3.446241763653124401 ) ) ;
#13371=CARTESIAN_POINT ( 'NONE',  ( 3.950837973638675393, 10.51028938476217967, 10.05648675950130233 ) ) ;
#13374=EDGE_CURVE ( 'NONE', #16292, #18099, #18278, .T. ) ;
#13379=CARTESIAN_POINT ( 'NONE',  ( 3.664313757352975376, -14.16986885736091395, -1.627055439596424513 ) ) ;
#13381=ORIENTED_EDGE ( 'NONE', *, *, #17544, .T. ) ;
#13382=ADVANCED_FACE ( 'NONE', ( #17091 ), #11338, .T. ) ;
#13384=CARTESIAN_POINT ( 'NONE',  ( 1.847247051441594401, 0.1676840720647037319, -12.44188156437793680 ) ) ;
#13387=ADVANCED_FACE ( 'NONE', ( #8491 ), #15538, .F. ) ;
#13393=CARTESIAN_POINT ( 'NONE',  ( 1.846955891736119293, 3.593597880662512623, -11.91257079808164576 ) ) ;
#13394=DIRECTION ( 'NONE',  ( -0.7561779333270775005, 0.4122479608995705536, 0.5081796452863259761 ) ) ;
#13396=CARTESIAN_POINT ( 'NONE',  ( 2.636624412715384391, -11.60464335004044223, -11.10302021258006278 ) ) ;
#13398=ORIENTED_EDGE ( 'NONE', *, *, #6574, .F. ) ;
#13400=CARTESIAN_POINT ( 'NONE',  ( 1.847461586945732703, -10.04711372545050097, 7.341074796295904648 ) ) ;
#13401=CARTESIAN_POINT ( 'NONE',  ( 0.3151928476913548050, 11.11539186930587242, 8.075547435846990751 ) ) ;
#13402=CARTESIAN_POINT ( 'NONE',  ( 16.56753206892534891, -0.001549402974393209202, 0.009369540855502124857 ) ) ;
#13411=CARTESIAN_POINT ( 'NONE',  ( 0.3151930723728382788, 11.16020735774779027, -8.013866567350774517 ) ) ;
#13423=DIRECTION ( 'NONE',  ( -1.000000000000000000, -0.000000000000000000, -0.000000000000000000 ) ) ;
#13425=CARTESIAN_POINT ( 'NONE',  ( 1.846138399168762101, 0.4167076046095548603, 12.43476674860266762 ) ) ;
#13427=ORIENTED_EDGE ( 'NONE', *, *, #16542, .T. ) ;
#13433=ORIENTED_EDGE ( 'NONE', *, *, #15898, .T. ) ;
#13435=ORIENTED_EDGE ( 'NONE', *, *, #15956, .F. ) ;
#13441=ADVANCED_FACE ( 'NONE', ( #14886 ), #11632, .T. ) ;
#13442=EDGE_CURVE ( 'NONE', #1858, #799, #4360, .T. ) ;
#13448=CARTESIAN_POINT ( 'NONE',  ( 0.3148208552358926493, 8.260375059853341639, 10.97826876274314856 ) ) ;
#13451=DIRECTION ( 'NONE',  ( -1.000000000000000000, -0.000000000000000000, -0.000000000000000000 ) ) ;
#13452=CARTESIAN_POINT ( 'NONE',  ( 0.3151926232592475174, 4.172630140040981317, -13.09050869763088443 ) ) ;
#13465=CARTESIAN_POINT ( 'NONE',  ( 0.4862570985993235340, -0.7479633556563419772, 13.89016912371017121 ) ) ;
#13466=CARTESIAN_POINT ( 'NONE',  ( 16.56753206892534891, 0.006760771273036174887, 0.006669401563384942146 ) ) ;
#13471=CARTESIAN_POINT ( 'NONE',  ( 0.3145734862173258373, 12.96846406299306587, 4.535879238194977070 ) ) ;
#13474=ORIENTED_EDGE ( 'NONE', *, *, #3133, .T. ) ;
#13475=CIRCLE ( 'NONE', #10420, 14.54644660717763927 ) ;
#13479=CARTESIAN_POINT ( 'NONE',  ( 0.3137051932979792457, 11.37800749014131263, 7.698472063774513430 ) ) ;
#13484=ORIENTED_EDGE ( 'NONE', *, *, #14122, .F. ) ;
#13485=DIRECTION ( 'NONE',  ( 0.7561779333270775005, 0.5491072561318364187, -0.3559159372837296664 ) ) ;
#13487=CARTESIAN_POINT ( 'NONE',  ( 0.4862570985993235340, -7.559321496869339185, -11.67702470553373750 ) ) ;
#13488=LINE ( 'NONE', #14924, #7192 ) ;
#13490=EDGE_CURVE ( 'NONE', #15958, #13528, #16213, .T. ) ;
#13491=ORIENTED_EDGE ( 'NONE', *, *, #5107, .F. ) ;
#13492=CIRCLE ( 'NONE', #11065, 16.06066017081991149 ) ;
#13495=B_SPLINE_CURVE_WITH_KNOTS ( 'NONE', 3,
 ( #934, #11171, #9902, #18413, #18600, #1569, #17083, #139, #8738, #3899, #8835, #11080, #14657 ),
 .UNSPECIFIED., .F., .F.,
 ( 4, 3, 3, 3, 4 ),
 ( 3.127317220692750759E-18, 0.0002299804304191498290, 0.0004599608082120264186, 0.0006467586077648000654, 0.0008336169836825974228 ),
 .UNSPECIFIED. ) ;
#13496=DIRECTION ( 'NONE',  ( 0.000000000000000000, 0.000000000000000000, 1.000000000000000000 ) ) ;
#13497=CARTESIAN_POINT ( 'NONE',  ( 0.3170788640506440603, -8.200855617524609897, 11.02668139258439162 ) ) ;
#13502=CARTESIAN_POINT ( 'NONE',  ( 3.512766787570759774, -13.55823433651952925, 6.535475144496928124 ) ) ;
#13504=ORIENTED_EDGE ( 'NONE', *, *, #12780, .F. ) ;
#13505=CARTESIAN_POINT ( 'NONE',  ( 0.3148213771069364175, 11.24846294176323447, -7.888490156175093304 ) ) ;
#13510=CARTESIAN_POINT ( 'NONE',  ( 8.438534575730034959, 0.2320579683291088824, -6.862570336891073097 ) ) ;
#13513=CARTESIAN_POINT ( 'NONE',  ( 0.3308579732647023430, -13.25341063505878481, 3.680601586799824076 ) ) ;
#13522=CARTESIAN_POINT ( 'NONE',  ( 2.697797270744668463, 12.33058466479268844, 4.970631985779629503 ) ) ;
#13523=EDGE_CURVE ( 'NONE', #4326, #12620, #3210, .T. ) ;
#13525=FACE_OUTER_BOUND ( 'NONE', #6195, .T. ) ;
#13526=ORIENTED_EDGE ( 'NONE', *, *, #13769, .F. ) ;
#13528=VERTEX_POINT ( 'NONE', #3111 ) ;
#13531=EDGE_CURVE ( 'NONE', #13773, #9066, #8572, .T. ) ;
#13532=CARTESIAN_POINT ( 'NONE',  ( 3.950837973638675393, -2.591948120961706792, -14.31366178983255466 ) ) ;
#13534=CARTESIAN_POINT ( 'NONE',  ( 16.56822296793089322, 0.009385634690642057770, -0.003834730849371914118 ) ) ;
#13537=ORIENTED_EDGE ( 'NONE', *, *, #8544, .T. ) ;
#13539=CARTESIAN_POINT ( 'NONE',  ( 16.57778382496167424, 0.001819584982831895037, 0.01482878558584693578 ) ) ;
#13540=CARTESIAN_POINT ( 'NONE',  ( 0.3145734862173244495, 7.825584895511528138, 11.29227530924448430 ) ) ;
#13548=VERTEX_POINT ( 'NONE', #13358 ) ;
#13551=ORIENTED_EDGE ( 'NONE', *, *, #5157, .F. ) ;
#13552=CARTESIAN_POINT ( 'NONE',  ( 1.846613052777651198, -7.585914669018095857, -9.862487290071081603 ) ) ;
#13559=CARTESIAN_POINT ( 'NONE',  ( 3.512766787570899663, 10.87507422923878586, 10.40533104696127076 ) ) ;
#13562=CARTESIAN_POINT ( 'NONE',  ( 0.4754618798421162973, -3.583352865732575943, -13.45049478164063395 ) ) ;
#13564=CARTESIAN_POINT ( 'NONE',  ( 16.58200780006414732, -0.004047297414157817463, -0.01041078477703986926 ) ) ;
#13567=ORIENTED_EDGE ( 'NONE', *, *, #4292, .F. ) ;
#13571=ORIENTED_EDGE ( 'NONE', *, *, #6196, .T. ) ;
#13574=EDGE_CURVE ( 'NONE', #11775, #6348, #9831, .T. ) ;
#13582=ORIENTED_EDGE ( 'NONE', *, *, #1838, .F. ) ;
#13584=CARTESIAN_POINT ( 'NONE',  ( 0.4385251269669942498, -10.76637725024245462, -8.732456510146192841 ) ) ;
#13592=CARTESIAN_POINT ( 'NONE',  ( 1.846138399168762101, 12.43476674860266584, 0.4167076046095977149 ) ) ;
#13593=( BOUNDED_SURFACE ( )  B_SPLINE_SURFACE ( 3, 1, ( 
 ( #6290, #13736 ),
 ( #10589, #9521 ),
 ( #13539, #458 ),
 ( #4757, #10779 ) ),
 .UNSPECIFIED., .F., .F., .T. ) 
 B_SPLINE_SURFACE_WITH_KNOTS ( ( 4, 4 ),
 ( 2, 2 ),
 ( 0.000000000000000000, 1.000000000000000000 ),
 ( 0.000000000000000000, 1.000000000000000000 ),
 .UNSPECIFIED. ) 
 GEOMETRIC_REPRESENTATION_ITEM ( )  RATIONAL_B_SPLINE_SURFACE ( (
 ( 1.000000000000000000, 1.000000000000000000),
 ( 0.7792777138730160313, 0.9689936506012927220),
 ( 0.7792777138730160313, 0.9689936506012927220),
 ( 1.000000000000000000, 1.000000000000000000) ) ) 
 REPRESENTATION_ITEM ( '' )  SURFACE ( )  );
#13598=B_SPLINE_CURVE_WITH_KNOTS ( 'NONE', 3,
 ( #713, #5193, #5009, #12277, #5104, #15045 ),
 .UNSPECIFIED., .F., .F.,
 ( 4, 2, 4 ),
 ( 4.240893905418535831E-17, 0.0002014099069817285406, 0.0004028198139634146346 ),
 .UNSPECIFIED. ) ;
#13604=ORIENTED_EDGE ( 'NONE', *, *, #12565, .T. ) ;
#13608=ORIENTED_EDGE ( 'NONE', *, *, #3211, .F. ) ;
#13614=CARTESIAN_POINT ( 'NONE',  ( 16.56679352167444819, 0.001518074900130650254, -0.009170718284672547266 ) ) ;
#13618=CARTESIAN_POINT ( 'NONE',  ( 2.747332970342022840, -2.409922051470793747, 16.17136872824897864 ) ) ;
#13620=CARTESIAN_POINT ( 'NONE',  ( 3.950837973638668288, 14.41405733518061716, 1.958075594453843493 ) ) ;
#13622=ORIENTED_EDGE ( 'NONE', *, *, #14005, .F. ) ;
#13623=CARTESIAN_POINT ( 'NONE',  ( 0.3095370825347233956, -8.444334731363927204, -10.84046130709067590 ) ) ;
#13624=CARTESIAN_POINT ( 'NONE',  ( 2.636624412714242194, 14.46769361191244485, 6.973567714906650394 ) ) ;
#13626=CARTESIAN_POINT ( 'NONE',  ( 1.846955891736118849, -11.91257079808165820, -3.593597880662470878 ) ) ;
#13629=EDGE_LOOP ( 'NONE', ( #17701, #13126, #4237, #4476 ) ) ;
#13632=ORIENTED_EDGE ( 'NONE', *, *, #10826, .T. ) ;
#13637=CARTESIAN_POINT ( 'NONE',  ( 0.3151926232592501265, 4.318679262939624230, 13.04305446098357635 ) ) ;
#13638=CARTESIAN_POINT ( 'NONE',  ( 1.562796894703937678, 0.000000000000000000, 0.000000000000000000 ) ) ;
#13640=CARTESIAN_POINT ( 'NONE',  ( 16.56782317627811096, 0.009228812961909594811, 0.003357783021327272015 ) ) ;
#13641=CARTESIAN_POINT ( 'NONE',  ( 1.959283090834855745, -12.53713130127478337, 0.6676170829051779609 ) ) ;
#13644=CARTESIAN_POINT ( 'NONE',  ( 3.074695600507708182, 10.75417554975745205, 11.23985886659407463 ) ) ;
#13645=CARTESIAN_POINT ( 'NONE',  ( 1.847372867223024295, -11.86627781945711568, 3.744745203533932365 ) ) ;
#13647=EDGE_CURVE ( 'NONE', #15590, #17568, #277, .T. ) ;
#13649=CARTESIAN_POINT ( 'NONE',  ( 2.747332970342022840, -2.705255688517959722, 16.12459247543625551 ) ) ;
#13650=CARTESIAN_POINT ( 'NONE',  ( 1.959212340397945562, -11.71715421693495074, -4.509090217468642692 ) ) ;
#13651=DIRECTION ( 'NONE',  ( -1.000000000000000000, -0.000000000000000000, -0.000000000000000000 ) ) ;
#13655=ORIENTED_EDGE ( 'NONE', *, *, #14692, .T. ) ;
#13660=ORIENTED_EDGE ( 'NONE', *, *, #14666, .F. ) ;
#13661=CARTESIAN_POINT ( 'NONE',  ( 0.3137051932979792457, -13.73004976592201842, -0.4596302728641207813 ) ) ;
#13665=CARTESIAN_POINT ( 'NONE',  ( 3.074695600507264537, -13.70113613813205689, 7.366518011945889732 ) ) ;
#13666=CARTESIAN_POINT ( 'NONE',  ( 0.8740779401508622648, 0.8420120399581700887, 14.27348745891572968 ) ) ;
#13669=CARTESIAN_POINT ( 'NONE',  ( 0.3095370825347234511, -3.806662003783320980, -13.20347358821918426 ) ) ;
#13672=CARTESIAN_POINT ( 'NONE',  ( 16.56782317627811096, -0.007739510688078479403, 0.006045301465876602373 ) ) ;
#13674=CARTESIAN_POINT ( 'NONE',  ( 2.697797270744668019, -0.9169917281808188658, 13.26309265156976913 ) ) ;
#13678=DIRECTION ( 'NONE',  ( -1.000000000000000000, -0.000000000000000000, -0.000000000000000000 ) ) ;
#13685=ORIENTED_EDGE ( 'NONE', *, *, #17591, .T. ) ;
#13689=CARTESIAN_POINT ( 'NONE',  ( 2.636624412714236865, 15.91454522070173638, 2.161493821596668585 ) ) ;
#13691=EDGE_CURVE ( 'NONE', #13818, #5518, #9991, .T. ) ;
#13699=CARTESIAN_POINT ( 'NONE',  ( 0.3720661004400037664, 10.73619472937702213, 8.694226082900630814 ) ) ;
#13702=CARTESIAN_POINT ( 'NONE',  ( 1.977436885025426250, 7.806953934146316776, 13.27782258181756880 ) ) ;
#13705=ORIENTED_EDGE ( 'NONE', *, *, #15715, .T. ) ;
#13706=CARTESIAN_POINT ( 'NONE',  ( 0.3137051932979775248, 10.83767969834815581, -8.442169467526731808 ) ) ;
#13708=CARTESIAN_POINT ( 'NONE',  ( 0.3095370825347233956, 11.38092634279628967, 7.700448427571912724 ) ) ;
#13714=CARTESIAN_POINT ( 'NONE',  ( 8.438534575730034959, -6.598402093327893958, 1.899950616255162483 ) ) ;
#13719=CARTESIAN_POINT ( 'NONE',  ( 3.664313757352970047, -9.645155442698829518, 10.50730552161229880 ) ) ;
#13720=DIRECTION ( 'NONE',  ( -0.7635533937278214944, -0.3966532189476559833, -0.5095610256143900951 ) ) ;
#13721=CARTESIAN_POINT ( 'NONE',  ( 1.977228804422632713, -13.27756617201330336, -7.806978995470745808 ) ) ;
#13722=CARTESIAN_POINT ( 'NONE',  ( 0.3132635586635976188, -7.641727604903970850, 11.41586812343486912 ) ) ;
#13736=CARTESIAN_POINT ( 'NONE',  ( 0.4754618798421167414, 13.89949764182682657, 0.7484603771384882309 ) ) ;
#13739=CARTESIAN_POINT ( 'NONE',  ( 1.254255976358044311, -7.789651112956927470, -12.44256109021856105 ) ) ;
#13740=DIRECTION ( 'NONE',  ( -1.000000000000000000, -0.000000000000000000, -0.000000000000000000 ) ) ;
#13746=ORIENTED_EDGE ( 'NONE', *, *, #10451, .T. ) ;
#13751=CARTESIAN_POINT ( 'NONE',  ( 3.074695600507349358, 10.75417554975707368, -11.23985886659415279 ) ) ;
#13754=CARTESIAN_POINT ( 'NONE',  ( 1.342453679581834924, -11.38190519890846453, -9.456403821038923851 ) ) ;
#13755=CARTESIAN_POINT ( 'NONE',  ( 2.123976203522053297, -15.26039569100261950, 3.347755036805843076 ) ) ;
#13757=CARTESIAN_POINT ( 'NONE',  ( 16.56753206892534891, -0.009369540855502119653, -0.001549402974393242162 ) ) ;
#13762=VERTEX_POINT ( 'NONE', #14298 ) ;
#13767=EDGE_CURVE ( 'NONE', #6138, #4723, #2354, .T. ) ;
#13769=EDGE_CURVE ( 'NONE', #10942, #9252, #4166, .T. ) ;
#13773=VERTEX_POINT ( 'NONE', #8196 ) ;
#13775=CARTESIAN_POINT ( 'NONE',  ( 2.002547531651519996, 6.845637710436341727, -10.57595306287284842 ) ) ;
#13789=EDGE_CURVE ( 'NONE', #11533, #1561, #13258, .T. ) ;
#13794=LINE ( 'NONE', #18436, #10240 ) ;
#13795=FACE_OUTER_BOUND ( 'NONE', #14366, .T. ) ;
#13799=FACE_OUTER_BOUND ( 'NONE', #636, .T. ) ;
#13801=CARTESIAN_POINT ( 'NONE',  ( 1.959212340397942675, 10.53510106265292023, -6.829000156128068433 ) ) ;
#13804=CARTESIAN_POINT ( 'NONE',  ( 3.950837973638668288, 14.41405733518061538, -1.958075594453841273 ) ) ;
#13805=CARTESIAN_POINT ( 'NONE',  ( 1.846138399168762101, 12.43476674860266584, 0.4167076046095977149 ) ) ;
#13810=ADVANCED_FACE ( 'NONE', ( #15816 ), #18123, .F. ) ;
#13812=EDGE_LOOP ( 'NONE', ( #6252, #4030, #13027, #2601 ) ) ;
#13815=CARTESIAN_POINT ( 'NONE',  ( 0.3132635586635977853, 12.89236642382228126, -4.743936529203109487 ) ) ;
#13818=VERTEX_POINT ( 'NONE', #18675 ) ;
#13819=CARTESIAN_POINT ( 'NONE',  ( 2.002547531651519996, -12.57989064830759141, -0.6781519942173057647 ) ) ;
#13820=FACE_OUTER_BOUND ( 'NONE', #15159, .T. ) ;
#13824=CARTESIAN_POINT ( 'NONE',  ( 0.3132642857406526260, 8.495623922778223758, -10.79548167658025193 ) ) ;
#13826=CIRCLE ( 'NONE', #7118, 5.000000000000000000 ) ;
#13832=ADVANCED_FACE ( 'NONE', ( #11430 ), #15643, .F. ) ;
#13837=CARTESIAN_POINT ( 'NONE',  ( 16.56872352241294521, 0.001442253899401220278, -0.01033355228142500415 ) ) ;
#13839=CARTESIAN_POINT ( 'NONE',  ( 8.522092701127531811, 1.786985377232127137, -6.722964936702079619 ) ) ;
#13840=B_SPLINE_CURVE_WITH_KNOTS ( 'NONE', 3,
 ( #17361, #5884, #8482, #1404, #14311, #11727 ),
 .UNSPECIFIED., .F., .F.,
 ( 4, 2, 4 ),
 ( 2.239080928920849783E-18, 0.0002017457492448096685, 0.0004034914984896170601 ),
 .UNSPECIFIED. ) ;
#13841=VECTOR ( 'NONE', #11208, 1000.000000000000114 ) ;
#13844=CARTESIAN_POINT ( 'NONE',  ( 1.918921323896325415, -7.860085869556248994, 9.738309537478970768 ) ) ;
#13849=ORIENTED_EDGE ( 'NONE', *, *, #3155, .T. ) ;
#13850=DIRECTION ( 'NONE',  ( 0.000000000000000000, 0.000000000000000000, 1.000000000000000000 ) ) ;
#13858=EDGE_CURVE ( 'NONE', #3595, #8004, #15524, .T. ) ;
#13868=CARTESIAN_POINT ( 'NONE',  ( 8.438534575730034959, -2.341351102130233119, -6.454982381540311565 ) ) ;
#13869=CARTESIAN_POINT ( 'NONE',  ( 3.950837973638668288, 0.000000000000000000, 0.000000000000000000 ) ) ;
#13870=DIRECTION ( 'NONE',  ( -0.7561779333270775005, 0.03481510524964793324, 0.6534392409364820908 ) ) ;
#13876=CARTESIAN_POINT ( 'NONE',  ( 16.56782317627811096, 0.006045301465876368185, -0.007739510688079533247 ) ) ;
#13882=CARTESIAN_POINT ( 'NONE',  ( 16.56782317627811096, -0.003357783021327886107, -0.009228812961908644183 ) ) ;
#13885=CARTESIAN_POINT ( 'NONE',  ( 0.4862570985993235340, 3.580942890621860109, -13.44146924561377254 ) ) ;
#13894=CARTESIAN_POINT ( 'NONE',  ( 8.438534575730034959, -5.688336279099072357, 3.845978796786017284 ) ) ;
#13895=AXIS2_PLACEMENT_3D ( 'NONE', #15302, #18270, #2214 ) ;
#13897=CARTESIAN_POINT ( 'NONE',  ( 2.002547531651519996, -7.942910686618240845, 9.778737580845669797 ) ) ;
#13899=CARTESIAN_POINT ( 'NONE',  ( 0.4384471787762820871, -13.39294437382615399, -3.577367180593688634 ) ) ;
#13903=ORIENTED_EDGE ( 'NONE', *, *, #11831, .F. ) ;
#13918=CARTESIAN_POINT ( 'NONE',  ( 1.861706995891668770, 7.751853334747318414, 9.751699138048461890 ) ) ;
#13919=LINE ( 'NONE', #7931, #16700 ) ;
#13922=VERTEX_POINT ( 'NONE', #8930 ) ;
#13927=( BOUNDED_SURFACE ( )  B_SPLINE_SURFACE ( 3, 1, ( 
 ( #14371, #1276 ),
 ( #17335, #4252 ),
 ( #11797, #4629 ),
 ( #14946, #3173 ) ),
 .UNSPECIFIED., .F., .F., .T. ) 
 B_SPLINE_SURFACE_WITH_KNOTS ( ( 4, 4 ),
 ( 2, 2 ),
 ( 0.000000000000000000, 1.000000000000000000 ),
 ( 0.000000000000000000, 1.000000000000000000 ),
 .UNSPECIFIED. ) 
 GEOMETRIC_REPRESENTATION_ITEM ( )  RATIONAL_B_SPLINE_SURFACE ( (
 ( 1.000000000000000000, 1.000000000000000000),
 ( 0.9933953342250436691, 0.8357391271907733676),
 ( 0.9933953342250436691, 0.8357391271907733676),
 ( 1.000000000000000000, 1.000000000000000000) ) ) 
 REPRESENTATION_ITEM ( '' )  SURFACE ( )  );
#13929=CARTESIAN_POINT ( 'NONE',  ( 3.950837973638668288, 0.000000000000000000, 0.000000000000000000 ) ) ;
#13930=FACE_OUTER_BOUND ( 'NONE', #3098, .T. ) ;
#13933=CARTESIAN_POINT ( 'NONE',  ( 2.747332970342022840, -11.66639548242798696, -11.45495994260730654 ) ) ;
#13942=CARTESIAN_POINT ( 'NONE',  ( 0.3142014840576536905, 10.88517824918543297, 8.382000553815492694 ) ) ;
#13952=EDGE_CURVE ( 'NONE', #15103, #11694, #14758, .T. ) ;
#13956=B_SPLINE_CURVE_WITH_KNOTS ( 'NONE', 3,
 ( #13624, #3676, #3769, #10669, #18116, #5016 ),
 .UNSPECIFIED., .F., .F.,
 ( 4, 2, 4 ),
 ( 0.000000000000000000, 0.001656992708822033113, 0.003313985417644066227 ),
 .UNSPECIFIED. ) ;
#13959=CARTESIAN_POINT ( 'NONE',  ( 0.3307726912345197445, 13.74203354050372106, -0.5948952607473121379 ) ) ;
#13962=CARTESIAN_POINT ( 'NONE',  ( 3.074695600507237891, -15.41438262616227739, 2.093687500611889352 ) ) ;
#13963=( NAMED_UNIT ( * ) PLANE_ANGLE_UNIT ( ) SI_UNIT ( $, .RADIAN. ) );
#13968=CARTESIAN_POINT ( 'NONE',  ( 3.950837973638675393, -13.10350451991845055, 6.316429227969417859 ) ) ;
#13972=CARTESIAN_POINT ( 'NONE',  ( 16.56822296793089322, -0.008619100080559813359, -0.005339139727952636229 ) ) ;
#13975=EDGE_CURVE ( 'NONE', #9622, #14131, #11243, .T. ) ;
#13977=ORIENTED_EDGE ( 'NONE', *, *, #2888, .F. ) ;
#13978=CARTESIAN_POINT ( 'NONE',  ( 1.959283090834838870, -9.750336807931205385, 7.909254450748972154 ) ) ;
#13979=CARTESIAN_POINT ( 'NONE',  ( 2.636624412715137922, -6.973567714907947135, 14.46769361191283920 ) ) ;
#13980=ORIENTED_EDGE ( 'NONE', *, *, #5054, .T. ) ;
#13986=DIRECTION ( 'NONE',  ( 0.000000000000000000, 0.000000000000000000, 1.000000000000000000 ) ) ;
#13998=EDGE_CURVE ( 'NONE', #698, #16167, #18204, .T. ) ;
#13999=ORIENTED_EDGE ( 'NONE', *, *, #13093, .F. ) ;
#14000=B_SPLINE_CURVE_WITH_KNOTS ( 'NONE', 3,
 ( #16371, #4803, #10534, #16562, #3450, #1841, #9284, #15116, #2034, #9000, #18084, #16645, #3253 ),
 .UNSPECIFIED., .F., .F.,
 ( 4, 3, 3, 3, 4 ),
 ( 3.198396408832238080E-18, 0.0002299780670421061189, 0.0004599561239687905540, 0.0006896788984287883888, 0.0009194956271626399547 ),
 .UNSPECIFIED. ) ;
#14002=ORIENTED_EDGE ( 'NONE', *, *, #13523, .T. ) ;
#14005=EDGE_CURVE ( 'NONE', #16346, #16292, #10734, .T. ) ;
#14011=CARTESIAN_POINT ( 'NONE',  ( 0.4384471787762852513, 7.540925784514715957, -11.63197976518319798 ) ) ;
#14014=CARTESIAN_POINT ( 'NONE',  ( 16.56753206892534891, 0.006760771273036169683, 0.006669401563384943880 ) ) ;
#14015=CARTESIAN_POINT ( 'NONE',  ( 16.56872352241294521, 0.001442253899401802278, 0.01033355228142402403 ) ) ;
#14017=ORIENTED_EDGE ( 'NONE', *, *, #2062, .F. ) ;
#14025=DIRECTION ( 'NONE',  ( -0.7635533937278216055, 0.6453904417649387604, -0.02138673900302117195 ) ) ;
#14028=CARTESIAN_POINT ( 'NONE',  ( 2.123976203522053297, -13.47898556379318435, 7.899625852120161440 ) ) ;
#14040=CARTESIAN_POINT ( 'NONE',  ( 0.3142011359265333148, 11.33549115679423736, 7.762194356530812023 ) ) ;
#14045=B_SPLINE_CURVE_WITH_KNOTS ( 'NONE', 3,
 ( #8192, #8280, #1003, #6840, #18491, #14191 ),
 .UNSPECIFIED., .F., .F.,
 ( 4, 2, 4 ),
 ( 4.336808689942017736E-19, 0.001500839035891552006, 0.003001678071783103578 ),
 .UNSPECIFIED. ) ;
#14046=FACE_OUTER_BOUND ( 'NONE', #7040, .T. ) ;
#14048=EDGE_CURVE ( 'NONE', #4379, #14416, #1873, .T. ) ;
#14057=DIRECTION ( 'NONE',  ( 0.000000000000000000, 0.000000000000000000, 1.000000000000000000 ) ) ;
#14060=SURFACE_STYLE_USAGE ( .BOTH. , #15396 ) ;
#14064=ORIENTED_EDGE ( 'NONE', *, *, #12164, .T. ) ;
#14066=ORIENTED_EDGE ( 'NONE', *, *, #1455, .F. ) ;
#14070=ORIENTED_EDGE ( 'NONE', *, *, #6862, .F. ) ;
#14072=CARTESIAN_POINT ( 'NONE',  ( 0.3142014840576518031, 0.3830336514510798707, -13.73311050063163563 ) ) ;
#14073=VERTEX_POINT ( 'NONE', #718 ) ;
#14075=CARTESIAN_POINT ( 'NONE',  ( 1.977228804422745068, 3.321884655131805975, -15.04020501276218091 ) ) ;
#14078=CARTESIAN_POINT ( 'NONE',  ( 0.3095370825347234511, -11.38092634279634119, 7.700448427571834564 ) ) ;
#14082=CARTESIAN_POINT ( 'NONE',  ( 1.846138399168762101, 7.646096044340033870, -9.815003036200328879 ) ) ;
#14084=CARTESIAN_POINT ( 'NONE',  ( 1.847247051441591958, -3.685275815977108405, -11.88474976472816103 ) ) ;
#14085=CARTESIAN_POINT ( 'NONE',  ( 0.3170788640506441158, 4.392045232375811459, 13.02120094575829867 ) ) ;
#14088=ORIENTED_EDGE ( 'NONE', *, *, #14048, .T. ) ;
#14090=ORIENTED_EDGE ( 'NONE', *, *, #6909, .T. ) ;
#14093=CARTESIAN_POINT ( 'NONE',  ( 1.847168016377982003, -0.1868244120188694568, -12.44137401948661292 ) ) ;
#14098=CARTESIAN_POINT ( 'NONE',  ( 0.3170788640506441158, 13.74111462631963576, -0.1533108587036642600 ) ) ;
#14104=ORIENTED_EDGE ( 'NONE', *, *, #4630, .T. ) ;
#14106=EDGE_CURVE ( 'NONE', #14416, #11694, #11837, .T. ) ;
#14112=CARTESIAN_POINT ( 'NONE',  ( 16.57210152137263393, 0.009075239946108201033, -0.01136813053532078656 ) ) ;
#14114=CARTESIAN_POINT ( 'NONE',  ( 0.3095370825347234511, 8.444334731364163460, -10.84046130709049294 ) ) ;
#14117=CARTESIAN_POINT ( 'NONE',  ( 0.3308579732646998450, 13.74211098745269766, 0.5950689966504839612 ) ) ;
#14119=CARTESIAN_POINT ( 'NONE',  ( 1.846138399168762101, 11.95493567637855392, -3.446241763652874379 ) ) ;
#14121=CARTESIAN_POINT ( 'NONE',  ( 0.3132642857406527370, 4.743831191224565202, -12.89240536501341161 ) ) ;
#14122=EDGE_CURVE ( 'NONE', #11616, #7718, #18473, .T. ) ;
#14127=ORIENTED_EDGE ( 'NONE', *, *, #11831, .T. ) ;
#14129=DIRECTION ( 'NONE',  ( 0.000000000000000000, 0.000000000000000000, 1.000000000000000000 ) ) ;
#14131=VERTEX_POINT ( 'NONE', #6651 ) ;
#14145=CARTESIAN_POINT ( 'NONE',  ( 0.4862570985993235340, 0.7479633556564388996, -13.89016912371016765 ) ) ;
#14152=CARTESIAN_POINT ( 'NONE',  ( 2.636624412716061627, -7.605649742761058540, -14.14563173255469408 ) ) ;
#14157=CARTESIAN_POINT ( 'NONE',  ( 1.846138399168762101, -9.815003036200465658, 7.646096044339859787 ) ) ;
#14160=CARTESIAN_POINT ( 'NONE',  ( 0.3137051932979792457, 4.679953077377485116, 12.91601973349272114 ) ) ;
#14164=CARTESIAN_POINT ( 'NONE',  ( 0.3137051932979792457, 11.37800749014142276, -7.698472063774345564 ) ) ;
#14172=CARTESIAN_POINT ( 'NONE',  ( 1.847380140988743591, -3.949801494731685292, -11.79969976631075390 ) ) ;
#14174=CARTESIAN_POINT ( 'NONE',  ( 0.3095370825347224519, 3.806662003783413351, 13.20347358821915940 ) ) ;
#14176=EDGE_CURVE ( 'NONE', #8361, #3320, #15793, .T. ) ;
#14177=EDGE_LOOP ( 'NONE', ( #15655, #17579, #16638, #1648 ) ) ;
#14179=CARTESIAN_POINT ( 'NONE',  ( 1.918918678667045130, 6.832809802519163256, -10.48466773720554279 ) ) ;
#14180=EDGE_CURVE ( 'NONE', #209, #2120, #16654, .T. ) ;
#14188=CARTESIAN_POINT ( 'NONE',  ( 1.562796894703937678, 6.799999999999999822, -1.500000000000000000 ) ) ;
#14191=CARTESIAN_POINT ( 'NONE',  ( 3.950837973638675393, 6.888253895133292559, 12.81214529934977797 ) ) ;
#14195=LINE ( 'NONE', #12760, #13204 ) ;
#14199=CARTESIAN_POINT ( 'NONE',  ( 8.522092701127531811, 6.946128462138595694, -0.3779863304871462493 ) ) ;
#14210=CONICAL_SURFACE ( 'NONE', #1701, 14.54644660717763927, 0.8559913436420816257 ) ;
#14222=CARTESIAN_POINT ( 'NONE',  ( 2.320521194581858460, 15.43440938316986610, 3.126729093672275805 ) ) ;
#14224=CARTESIAN_POINT ( 'NONE',  ( 0.3058872367615230181, -7.578326039752686150, 11.46514199369355325 ) ) ;
#14227=ORIENTED_EDGE ( 'NONE', *, *, #4799, .T. ) ;
#14230=CARTESIAN_POINT ( 'NONE',  ( 0.3307726912345222980, 4.812300915532974344, 12.88561780039860416 ) ) ;
#14231=DIRECTION ( 'NONE',  ( -1.000000000000000000, 0.000000000000000000, 0.000000000000000000 ) ) ;
#14232=EDGE_CURVE ( 'NONE', #3195, #9890, #12322, .T. ) ;
#14233=VERTEX_POINT ( 'NONE', #12923 ) ;
#14235=CARTESIAN_POINT ( 'NONE',  ( 1.846822687350019754, -12.43915556955403545, -0.2922081769261452022 ) ) ;
#14236=CARTESIAN_POINT ( 'NONE',  ( 16.56872352241294521, -0.01033355228142402750, 0.001442253899401767583 ) ) ;
#14244=SHAPE_REPRESENTATION ( 'straight miter gear_iso_ISO - Straight miter gear 1.5M20T 20PA 2FW ---20O10H16.576MD10.0S1', ( #2030 ), #8454 ) ;
#14245=( BOUNDED_SURFACE ( )  B_SPLINE_SURFACE ( 3, 1, ( 
 ( #10722, #500 ),
 ( #3348, #307 ),
 ( #17989, #597 ),
 ( #4895, #12250 ) ),
 .UNSPECIFIED., .F., .F., .T. ) 
 B_SPLINE_SURFACE_WITH_KNOTS ( ( 4, 4 ),
 ( 2, 2 ),
 ( 0.000000000000000000, 1.000000000000000000 ),
 ( 0.000000000000000000, 1.000000000000000000 ),
 .UNSPECIFIED. ) 
 GEOMETRIC_REPRESENTATION_ITEM ( )  RATIONAL_B_SPLINE_SURFACE ( (
 ( 1.000000000000000000, 1.000000000000000000),
 ( 0.9593108457356467333, 0.9995965569486454649),
 ( 0.9593108457356467333, 0.9995965569486454649),
 ( 1.000000000000000000, 1.000000000000000000) ) ) 
 REPRESENTATION_ITEM ( '' )  SURFACE ( )  );
#14251=CARTESIAN_POINT ( 'NONE',  ( 1.977228804423231345, 7.806978995470744032, -13.27756617201399969 ) ) ;
#14254=CARTESIAN_POINT ( 'NONE',  ( 16.57210152137263393, -0.01453130299868639515, 0.0006600038696349324685 ) ) ;
#14256=CARTESIAN_POINT ( 'NONE',  ( 16.56872352241294521, -0.004907101719994693724, 0.009207754980063731845 ) ) ;
#14260=CARTESIAN_POINT ( 'NONE',  ( 0.4754618798421162973, -5.007009103465343003, 12.98792082933642789 ) ) ;
#14261=AXIS2_PLACEMENT_3D ( 'NONE', #1854, #9015, #6056 ) ;
#14262=CARTESIAN_POINT ( 'NONE',  ( 1.845756295923357326, 12.43231724724606835, -0.4783934145702458673 ) ) ;
#14265=CARTESIAN_POINT ( 'NONE',  ( 0.3137051932979757485, -8.442169467526770887, -10.83767969834812561 ) ) ;
#14266=ADVANCED_FACE ( 'NONE', ( #13207 ), #6672, .T. ) ;
#14267=ADVANCED_FACE ( 'NONE', ( #16177 ), #5644, .F. ) ;
#14269=LINE ( 'NONE', #7197, #17997 ) ;
#14275=CARTESIAN_POINT ( 'NONE',  ( 1.959212340397967766, -0.6675998551412658522, 12.53706137681888677 ) ) ;
#14276=ADVANCED_FACE ( 'NONE', ( #11596 ), #554, .F. ) ;
#14278=CARTESIAN_POINT ( 'NONE',  ( 2.636624412715093513, -14.14563173255330142, 7.605649742761597665 ) ) ;
#14279=CARTESIAN_POINT ( 'NONE',  ( 16.56822296793089322, -0.005339139727952984908, -0.008619100080558656299 ) ) ;
#14282=CARTESIAN_POINT ( 'NONE',  ( 2.002547531651519996, -7.942910686618100513, -9.778737580845787036 ) ) ;
#14286=DIRECTION ( 'NONE',  ( -1.000000000000000000, -0.000000000000000000, -0.000000000000000000 ) ) ;
#14287=VERTEX_POINT ( 'NONE', #7300 ) ;
#14288=CONICAL_SURFACE ( 'NONE', #16995, 14.54644660717763927, 0.8559913436420816257 ) ;
#14290=EDGE_CURVE ( 'NONE', #9252, #4800, #15722, .T. ) ;
#14295=AXIS2_PLACEMENT_3D ( 'NONE', #6904, #10943, #2146 ) ;
#14298=CARTESIAN_POINT ( 'NONE',  ( 2.002547531651519996, 10.57595306287302250, -6.845637710436074386 ) ) ;
#14304=ORIENTED_EDGE ( 'NONE', *, *, #1941, .T. ) ;
#14308=CARTESIAN_POINT ( 'NONE',  ( 3.074695600508242421, -2.093687500613561348, -15.41438262616270194 ) ) ;
#14311=CARTESIAN_POINT ( 'NONE',  ( 0.4384471787762818096, 0.7363690479466327155, 13.84291427302852462 ) ) ;
#14316=CARTESIAN_POINT ( 'NONE',  ( 3.950837973638668288, 0.000000000000000000, 0.000000000000000000 ) ) ;
#14317=CARTESIAN_POINT ( 'NONE',  ( 0.000000000000000000, 0.000000000000000000, 0.000000000000000000 ) ) ;
#14324=CARTESIAN_POINT ( 'NONE',  ( 16.56782317627811096, -0.003357783021327304974, 0.009228812961909584403 ) ) ;
#14325=EDGE_CURVE ( 'NONE', #1370, #13362, #5697, .T. ) ;
#14327=CARTESIAN_POINT ( 'NONE',  ( 0.3095370825347233956, -13.20347358821911854, -3.806662003783550574 ) ) ;
#14328=ORIENTED_EDGE ( 'NONE', *, *, #3042, .T. ) ;
#14331=CARTESIAN_POINT ( 'NONE',  ( 1.918918678667048461, -12.08296592096905187, -3.258447776119960615 ) ) ;
#14344=ORIENTED_EDGE ( 'NONE', *, *, #16255, .T. ) ;
#14345=CARTESIAN_POINT ( 'NONE',  ( 2.320521194582656932, -14.32454473829943886, 6.542541239685230714 ) ) ;
#14351=VECTOR ( 'NONE', #17805, 1000.000000000000000 ) ;
#14352=CARTESIAN_POINT ( 'NONE',  ( 0.3132635586635994507, -3.740017578711855695, 13.21855946425835882 ) ) ;
#14353=CARTESIAN_POINT ( 'NONE',  ( 0.3145729642390390768, -10.93201268464378373, 8.321438378985218876 ) ) ;
#14357=DIRECTION ( 'NONE',  ( -1.000000000000000000, 0.000000000000000000, 0.000000000000000000 ) ) ;
#14364=CARTESIAN_POINT ( 'NONE',  ( 8.522092701127531811, 3.777034505568607425, -5.841710761610089619 ) ) ;
#14365=CARTESIAN_POINT ( 'NONE',  ( 1.959283090834841090, -7.909254450748933962, -9.750336807931228478 ) ) ;
#14366=EDGE_LOOP ( 'NONE', ( #9736, #2200, #611, #12563 ) ) ;
#14369=CARTESIAN_POINT ( 'NONE',  ( 1.847426409206446518, -0.01438352405999345808, 12.44303504652078018 ) ) ;
#14371=CARTESIAN_POINT ( 'NONE',  ( 16.56753206892534891, 0.001549402974394163733, 0.009369540855502535986 ) ) ;
#14372=ORIENTED_EDGE ( 'NONE', *, *, #5905, .F. ) ;
#14377=CARTESIAN_POINT ( 'NONE',  ( 1.846138399168762989, 4.238866729160403857, 11.69739621335923729 ) ) ;
#14384=EDGE_CURVE ( 'NONE', #8099, #3320, #3652, .T. ) ;
#14385=ORIENTED_EDGE ( 'NONE', *, *, #14897, .F. ) ;
#14386=EDGE_CURVE ( 'NONE', #7547, #2319, #18248, .T. ) ;
#14389=VERTEX_POINT ( 'NONE', #2375 ) ;
#14394=CARTESIAN_POINT ( 'NONE',  ( 0.3145729642390366343, 7.825496023201474749, -11.29233589755984113 ) ) ;
#14400=CARTESIAN_POINT ( 'NONE',  ( 2.002547531651519996, -10.57595306287296921, 6.845637710436153434 ) ) ;
#14401=CARTESIAN_POINT ( 'NONE',  ( 0.3095370825347233956, -7.700448427571951804, 11.38092634279625948 ) ) ;
#14404=ORIENTED_EDGE ( 'NONE', *, *, #16792, .T. ) ;
#14406=CARTESIAN_POINT ( 'NONE',  ( 16.56753206892534891, -0.004253784598196239108, 0.008490833999798910042 ) ) ;
#14409=ORIENTED_EDGE ( 'NONE', *, *, #14557, .T. ) ;
#14414=FACE_OUTER_BOUND ( 'NONE', #7649, .T. ) ;
#14415=CARTESIAN_POINT ( 'NONE',  ( 16.57210152137263393, 0.005118120558001911478, 0.01361613799508963087 ) ) ;
#14416=VERTEX_POINT ( 'NONE', #11974 ) ;
#14417=CARTESIAN_POINT ( 'NONE',  ( 8.522092701127531811, 6.946128462138595694, 0.3779863304871469154 ) ) ;
#14418=VECTOR ( 'NONE', #856, 1000.000000000000000 ) ;
#14420=B_SPLINE_CURVE_WITH_KNOTS ( 'NONE', 3,
 ( #16040, #4294, #2656, #12885, #15753, #1424 ),
 .UNSPECIFIED., .F., .F.,
 ( 4, 2, 4 ),
 ( 4.003426615173598157E-17, 0.0002014099069817276190, 0.0004028198139634152309 ),
 .UNSPECIFIED. ) ;
#14423=B_SPLINE_CURVE_WITH_KNOTS ( 'NONE', 3,
 ( #9755, #17033, #16841, #15583, #2310, #2482 ),
 .UNSPECIFIED., .F., .F.,
 ( 4, 2, 4 ),
 ( 0.000000000000000000, 0.001657017934712276541, 0.003314035869424553082 ),
 .UNSPECIFIED. ) ;
#14424=( BOUNDED_SURFACE ( )  B_SPLINE_SURFACE ( 3, 1, ( 
 ( #1225, #5520 ),
 ( #11371, #17185 ),
 ( #4101, #9921 ),
 ( #11006, #5436 ) ),
 .UNSPECIFIED., .F., .F., .T. ) 
 B_SPLINE_SURFACE_WITH_KNOTS ( ( 4, 4 ),
 ( 2, 2 ),
 ( 0.000000000000000000, 1.000000000000000000 ),
 ( 0.000000000000000000, 1.000000000000000000 ),
 .UNSPECIFIED. ) 
 GEOMETRIC_REPRESENTATION_ITEM ( )  RATIONAL_B_SPLINE_SURFACE ( (
 ( 1.000000000000000000, 1.000000000000000000),
 ( 0.9933953342250438912, 0.8357391271907739227),
 ( 0.9933953342250438912, 0.8357391271907739227),
 ( 1.000000000000000000, 1.000000000000000000) ) ) 
 REPRESENTATION_ITEM ( '' )  SURFACE ( )  );
#14431=EDGE_CURVE ( 'NONE', #16551, #15433, #574, .T. ) ;
#14432=CARTESIAN_POINT ( 'NONE',  ( 3.950837973638677170, 10.51028938476232355, -10.05648675950114956 ) ) ;
#14435=CARTESIAN_POINT ( 'NONE',  ( 0.3170788640506440603, 0.1533108587038062576, -13.74111462631963398 ) ) ;
#14441=CARTESIAN_POINT ( 'NONE',  ( 0.4862570985993252548, 10.79774104611373353, 8.769551628660776643 ) ) ;
#14442=ORIENTED_EDGE ( 'NONE', *, *, #16232, .T. ) ;
#14444=CARTESIAN_POINT ( 'NONE',  ( 16.56872352241294521, 0.01033355228142499721, 0.001442253899401261912 ) ) ;
#14449=EDGE_CURVE ( 'NONE', #16063, #12518, #16053, .T. ) ;
#14451=CARTESIAN_POINT ( 'NONE',  ( 16.56872352241294521, -0.004564908236400030961, 0.009382111268607351909 ) ) ;
#14454=DIRECTION ( 'NONE',  ( 0.000000000000000000, 0.000000000000000000, 1.000000000000000000 ) ) ;
#14455=CARTESIAN_POINT ( 'NONE',  ( 2.697797270744668019, -7.053988368581781465, -11.26906156738834675 ) ) ;
#14457=CARTESIAN_POINT ( 'NONE',  ( 16.56872352241294521, 0.009382111268606257298, -0.004564908236400254740 ) ) ;
#14459=ORIENTED_EDGE ( 'NONE', *, *, #15921, .T. ) ;
#14464=FACE_OUTER_BOUND ( 'NONE', #12906, .T. ) ;
#14465=VERTEX_POINT ( 'NONE', #8492 ) ;
#14466=CARTESIAN_POINT ( 'NONE',  ( 0.3132635586635996727, 13.21855946425836592, 3.740017578711807289 ) ) ;
#14472=CARTESIAN_POINT ( 'NONE',  ( 0.8740764193767192047, -0.8420116711622469552, 14.27348595579779911 ) ) ;
#14475=CARTESIAN_POINT ( 'NONE',  ( 0.3145729642390355241, -12.96842777670210189, 4.535980493005037140 ) ) ;
#14479=CIRCLE ( 'NONE', #15109, 14.54644660717763927 ) ;
#14482=ORIENTED_EDGE ( 'NONE', *, *, #7744, .F. ) ;
#14483=VERTEX_POINT ( 'NONE', #9732 ) ;
#14486=CIRCLE ( 'NONE', #6267, 14.54644660717763927 ) ;
#14487=CARTESIAN_POINT ( 'NONE',  ( 1.918918678667071775, -0.6348738215464356793, -12.49849921341423986 ) ) ;
#14488=CARTESIAN_POINT ( 'NONE',  ( 0.3137051932979792457, 8.442169467527008919, -10.83767969834794087 ) ) ;
#14493=EDGE_CURVE ( 'NONE', #8310, #12927, #17272, .T. ) ;
#14494=FACE_OUTER_BOUND ( 'NONE', #10606, .T. ) ;
#14496=CARTESIAN_POINT ( 'NONE',  ( 1.861706995891668326, -3.332865258614060355, 12.00328602385079257 ) ) ;
#14500=CARTESIAN_POINT ( 'NONE',  ( 1.845755665168035575, 9.776700214454821847, 7.694641135843453661 ) ) ;
#14503=ORIENTED_EDGE ( 'NONE', *, *, #6315, .T. ) ;
#14507=ORIENTED_EDGE ( 'NONE', *, *, #14652, .F. ) ;
#14509=DIRECTION ( 'NONE',  ( -1.000000000000000000, -0.000000000000000000, -0.000000000000000000 ) ) ;
#14511=CARTESIAN_POINT ( 'NONE',  ( 2.353870697619111496, 3.268530966681629568, 12.53036919722785925 ) ) ;
#14513=DIRECTION ( 'NONE',  ( -1.000000000000000000, -0.000000000000000000, -0.000000000000000000 ) ) ;
#14515=ORIENTED_EDGE ( 'NONE', *, *, #14325, .T. ) ;
#14517=CARTESIAN_POINT ( 'NONE',  ( 2.353870697619111940, 10.00946331859664085, 8.216087327472971324 ) ) ;
#14524=CARTESIAN_POINT ( 'NONE',  ( 2.636624412714994037, -14.46769361191274328, -6.973567714907344950 ) ) ;
#14526=CARTESIAN_POINT ( 'NONE',  ( 2.320520222537155064, -14.32454429810361951, -6.542539914240126819 ) ) ;
#14527=DIRECTION ( 'NONE',  ( 0.7635533937278216055, 0.6071939193889560604, 0.2197766120036526161 ) ) ;
#14528=EDGE_LOOP ( 'NONE', ( #15803, #8448, #6431, #8997 ) ) ;
#14529=LINE ( 'NONE', #12907, #3609 ) ;
#14536=( BOUNDED_SURFACE ( )  B_SPLINE_SURFACE ( 3, 1, ( 
 ( #6981, #6877 ),
 ( #15385, #9818 ),
 ( #12699, #6789 ),
 ( #18532, #14327 ) ),
 .UNSPECIFIED., .F., .F., .T. ) 
 B_SPLINE_SURFACE_WITH_KNOTS ( ( 4, 4 ),
 ( 2, 2 ),
 ( 0.000000000000000000, 1.000000000000000000 ),
 ( 0.000000000000000000, 1.000000000000000000 ),
 .UNSPECIFIED. ) 
 GEOMETRIC_REPRESENTATION_ITEM ( )  RATIONAL_B_SPLINE_SURFACE ( (
 ( 1.000000000000000000, 1.000000000000000000),
 ( 0.9933953342250438912, 0.8357391271907739227),
 ( 0.9933953342250438912, 0.8357391271907739227),
 ( 1.000000000000000000, 1.000000000000000000) ) ) 
 REPRESENTATION_ITEM ( '' )  SURFACE ( )  );
#14541=CARTESIAN_POINT ( 'NONE',  ( 0.3150692679895994996, -4.391039771493759680, 13.01874238516608884 ) ) ;
#14544=( GEOMETRIC_REPRESENTATION_CONTEXT ( 3 ) GLOBAL_UNCERTAINTY_ASSIGNED_CONTEXT ( ( #5379 ) ) GLOBAL_UNIT_ASSIGNED_CONTEXT ( ( #992, #11326, #17330 ) ) REPRESENTATION_CONTEXT ( 'NONE', 'WORKASPACE' ) );
#14546=CARTESIAN_POINT ( 'NONE',  ( 2.636624412714237309, 15.80357026013209953, 2.862162146984226663 ) ) ;
#14547=CARTESIAN_POINT ( 'NONE',  ( 2.747332970342022840, 11.45495994260734918, -11.66639548242795144 ) ) ;
#14555=CARTESIAN_POINT ( 'NONE',  ( 3.950837973638668288, 14.41405733518061716, 1.958075594453843493 ) ) ;
#14557=EDGE_CURVE ( 'NONE', #17234, #257, #9433, .T. ) ;
#14559=ORIENTED_EDGE ( 'NONE', *, *, #18240, .T. ) ;
#14563=VERTEX_POINT ( 'NONE', #1217 ) ;
#14565=CARTESIAN_POINT ( 'NONE',  ( 0.4862570985993252548, 13.44146924561381162, 3.580942890621718888 ) ) ;
#14570=CARTESIAN_POINT ( 'NONE',  ( 1.846138399168762989, 10.30487220521570357, 6.971848976711047641 ) ) ;
#14573=ADVANCED_FACE ( 'NONE', ( #13066 ), #14288, .T. ) ;
#14575=ORIENTED_EDGE ( 'NONE', *, *, #11594, .F. ) ;
#14576=AXIS2_PLACEMENT_3D ( 'NONE', #18113, #542, #15330 ) ;
#14580=ORIENTED_EDGE ( 'NONE', *, *, #3866, .T. ) ;
#14589=CARTESIAN_POINT ( 'NONE',  ( 2.002547531651519996, 3.242439124566649511, 12.17374746633579541 ) ) ;
#14590=DIRECTION ( 'NONE',  ( -1.000000000000000000, -0.000000000000000000, -0.000000000000000000 ) ) ;
#14591=CARTESIAN_POINT ( 'NONE',  ( 2.636624412714236865, 0.000000000000000000, -16.06066017081991149 ) ) ;
#14592=CARTESIAN_POINT ( 'NONE',  ( 0.4862570985993235340, -0.7479633556561480212, -13.89016912371018186 ) ) ;
#14596=ORIENTED_EDGE ( 'NONE', *, *, #7743, .F. ) ;
#14599=EDGE_CURVE ( 'NONE', #6138, #15079, #12179, .T. ) ;
#14602=CARTESIAN_POINT ( 'NONE',  ( 16.56822296793089322, -0.007741272030791128758, 0.006547366384936715959 ) ) ;
#14603=EDGE_LOOP ( 'NONE', ( #7461, #1727, #2627, #7606 ) ) ;
#14604=CARTESIAN_POINT ( 'NONE',  ( 3.950837973638675393, 2.591948120961804936, 14.31366178983254578 ) ) ;
#14607=B_SPLINE_CURVE_WITH_KNOTS ( 'NONE', 3,
 ( #5529, #2664, #2750, #1331, #8597, #17025, #2839, #11379, #6888, #2561, #12710, #18541, #11474 ),
 .UNSPECIFIED., .F., .F.,
 ( 4, 3, 3, 3, 4 ),
 ( 1.897353801849632760E-18, 0.0002299804304191482569, 0.0004599608082120252260, 0.0006467586077648016917, 0.0008336169836825988323 ),
 .UNSPECIFIED. ) ;
#14610=VERTEX_POINT ( 'NONE', #10496 ) ;
#14612=CARTESIAN_POINT ( 'NONE',  ( 0.3151930723728477157, -4.172946285306481151, -13.09040889075574476 ) ) ;
#14614=CARTESIAN_POINT ( 'NONE',  ( 1.847034903785822246, 11.76058231742745797, 4.063013886994747637 ) ) ;
#14615=CARTESIAN_POINT ( 'NONE',  ( 1.846138399168762101, -6.971848976711082280, 10.30487220521567693 ) ) ;
#14624=CARTESIAN_POINT ( 'NONE',  ( 1.918918678667045574, 12.08296592096908384, 3.258447776119875350 ) ) ;
#14627=B_SPLINE_CURVE_WITH_KNOTS ( 'NONE', 3,
 ( #17456, #13150, #14487, #8567, #2904, #14772 ),
 .UNSPECIFIED., .F., .F.,
 ( 4, 2, 4 ),
 ( 5.421010862427522170E-19, 0.0001825746017570583442, 0.0003651492035141161462 ),
 .UNSPECIFIED. ) ;
#14629=B_SPLINE_CURVE_WITH_KNOTS ( 'NONE', 3,
 ( #1650, #16661, #13502, #6536 ),
 .UNSPECIFIED., .F., .F.,
 ( 4, 4 ),
 ( 6.158879127553505933E-17, 0.002004993803842649181 ),
 .UNSPECIFIED. ) ;
#14630=EDGE_CURVE ( 'NONE', #18099, #6002, #3499, .T. ) ;
#14633=CARTESIAN_POINT ( 'NONE',  ( 3.950837973638675393, -13.10350451991845055, 6.316429227969417859 ) ) ;
#14638=CARTESIAN_POINT ( 'NONE',  ( 1.918921323896324083, 4.466082741316370175, -11.69058285425785648 ) ) ;
#14641=CARTESIAN_POINT ( 'NONE',  ( 0.3170788640506440603, -7.952793437297492218, -11.20690911610912543 ) ) ;
#14643=DIRECTION ( 'NONE',  ( -1.000000000000000000, -0.000000000000000000, -0.000000000000000000 ) ) ;
#14648=CARTESIAN_POINT ( 'NONE',  ( 0.3170788640506440603, -13.11595226728160668, 4.100430649997911736 ) ) ;
#14652=EDGE_CURVE ( 'NONE', #8892, #7279, #3737, .T. ) ;
#14653=EDGE_LOOP ( 'NONE', ( #9160, #1273, #9250, #3612 ) ) ;
#14656=CARTESIAN_POINT ( 'NONE',  ( 1.847461586945727152, 10.04711372545055781, -7.341074796295831817 ) ) ;
#14657=CARTESIAN_POINT ( 'NONE',  ( 1.846138399168762101, -7.646096044339961040, 9.815003036200383946 ) ) ;
#14660=B_SPLINE_CURVE_WITH_KNOTS ( 'NONE', 3,
 ( #12817, #14072, #977, #18644, #12626, #5543, #17212 ),
 .UNSPECIFIED., .F., .F.,
 ( 4, 3, 4 ),
 ( 3.198396408832238080E-18, 0.0002299780670421061460, 0.0004597478348665241538 ),
 .UNSPECIFIED. ) ;
#14661=CARTESIAN_POINT ( 'NONE',  ( 0.3145734862173252822, -8.321353293018908914, 10.93207848441430130 ) ) ;
#14664=CARTESIAN_POINT ( 'NONE',  ( 2.636624412714756005, -2.161493821597335607, 15.91454522070219113 ) ) ;
#14666=EDGE_CURVE ( 'NONE', #3191, #10770, #5689, .T. ) ;
#14675=VERTEX_POINT ( 'NONE', #12221 ) ;
#14676=CARTESIAN_POINT ( 'NONE',  ( 2.002547531651519996, 4.532360870844327039, 11.75462648437103752 ) ) ;
#14680=LINE ( 'NONE', #17660, #3181 ) ;
#14681=DIRECTION ( 'NONE',  ( -1.000000000000000000, -0.000000000000000000, -0.000000000000000000 ) ) ;
#14685=DIRECTION ( 'NONE',  ( 0.000000000000000000, 0.000000000000000000, -1.000000000000000000 ) ) ;
#14686=EDGE_CURVE ( 'NONE', #11651, #4800, #3697, .T. ) ;
#14688=CARTESIAN_POINT ( 'NONE',  ( 2.636624412715137478, -2.862162146983530775, 15.80357026013314048 ) ) ;
#14692=EDGE_CURVE ( 'NONE', #11575, #14465, #13919, .T. ) ;
#14694=VERTEX_POINT ( 'NONE', #12486 ) ;
#14697=VERTEX_POINT ( 'NONE', #2179 ) ;
#14700=FACE_OUTER_BOUND ( 'NONE', #8030, .T. ) ;
#14701=AXIS2_PLACEMENT_3D ( 'NONE', #18096, #972, #702 ) ;
#14702=CARTESIAN_POINT ( 'NONE',  ( 16.56872352241294521, -0.001442253899401298341, 0.01033355228142499027 ) ) ;
#14708=CARTESIAN_POINT ( 'NONE',  ( 8.438534575730034959, 6.598402093327880635, 1.899950616255211111 ) ) ;
#14709=ADVANCED_FACE ( 'NONE', ( #4860 ), #12371, .F. ) ;
#14710=CARTESIAN_POINT ( 'NONE',  ( 0.3151930723728440520, 13.04315954105015152, 4.318364831037635021 ) ) ;
#14714=B_SPLINE_CURVE_WITH_KNOTS ( 'NONE', 3,
 ( #3689, #13644, #14972, #5030 ),
 .UNSPECIFIED., .F., .F.,
 ( 4, 4 ),
 ( 3.019714627835872489E-16, 0.002004993803842318283 ),
 .UNSPECIFIED. ) ;
#14718=LINE ( 'NONE', #11579, #1134 ) ;
#14721=CARTESIAN_POINT ( 'NONE',  ( 3.377929128793395908, -7.136734442940921852, 12.02809354424098665 ) ) ;
#14725=CARTESIAN_POINT ( 'NONE',  ( 0.3095370825347224519, -3.806662003783507497, 13.20347358821913275 ) ) ;
#14731=ORIENTED_EDGE ( 'NONE', *, *, #332, .F. ) ;
#14733=FACE_OUTER_BOUND ( 'NONE', #525, .T. ) ;
#14738=ORIENTED_EDGE ( 'NONE', *, *, #6910, .F. ) ;
#14740=CARTESIAN_POINT ( 'NONE',  ( 16.56753206892534891, 0.009369540855502130061, 0.001549402974393180796 ) ) ;
#14742=VERTEX_POINT ( 'NONE', #742 ) ;
#14748=B_SPLINE_CURVE_WITH_KNOTS ( 'NONE', 3,
 ( #11472, #14517, #7076, #10321, #96, #8792 ),
 .UNSPECIFIED., .F., .F.,
 ( 4, 2, 4 ),
 ( 8.673617379884035472E-19, 0.001500839035891548753, 0.003001678071783096639 ),
 .UNSPECIFIED. ) ;
#14750=VECTOR ( 'NONE', #3301, 999.9999999999998863 ) ;
#14751=CARTESIAN_POINT ( 'NONE',  ( 3.074695600507405757, 7.366518011945858646, 13.70113613813188458 ) ) ;
#14758=LINE ( 'NONE', #148, #4833 ) ;
#14771=CARTESIAN_POINT ( 'NONE',  ( 0.3142014840576502488, -7.762239086932773091, -11.33546131209471142 ) ) ;
#14772=CARTESIAN_POINT ( 'NONE',  ( 1.846138399168762101, -0.4167076046094680408, -12.43476674860266940 ) ) ;
#14774=VERTEX_POINT ( 'NONE', #5671 ) ;
#14777=CIRCLE ( 'NONE', #10824, 16.06066017081991149 ) ;
#14778=CARTESIAN_POINT ( 'NONE',  ( 2.636624412716045196, 11.10302021257998994, -11.60464335004042447 ) ) ;
#14780=CARTESIAN_POINT ( 'NONE',  ( 1.977228804422749064, -1.488378900182820264, -15.33060379559159259 ) ) ;
#14782=CARTESIAN_POINT ( 'NONE',  ( 1.846822687350019754, 11.92063725419904152, -3.566003975885565946 ) ) ;
#14785=CARTESIAN_POINT ( 'NONE',  ( 3.950837973638668288, 0.000000000000000000, 0.000000000000000000 ) ) ;
#14787=B_SPLINE_CURVE_WITH_KNOTS ( 'NONE', 3,
 ( #11021, #610, #3654, #2039, #16749, #1946 ),
 .UNSPECIFIED., .F., .F.,
 ( 4, 2, 4 ),
 ( 4.253224384355279651E-17, 0.0002014099069817287574, 0.0004028198139634150141 ),
 .UNSPECIFIED. ) ;
#14789=ORIENTED_EDGE ( 'NONE', *, *, #6704, .T. ) ;
#14792=ORIENTED_EDGE ( 'NONE', *, *, #2510, .T. ) ;
#14793=ORIENTED_EDGE ( 'NONE', *, *, #10826, .F. ) ;
#14797=EDGE_CURVE ( 'NONE', #11439, #16313, #12574, .T. ) ;
#14800=CARTESIAN_POINT ( 'NONE',  ( 0.4862570985993235340, -11.67702470553370553, 7.559321496869385371 ) ) ;
#14801=CARTESIAN_POINT ( 'NONE',  ( 2.636624412716062071, -11.10302021258080352, -11.60464335004061454 ) ) ;
#14802=FACE_OUTER_BOUND ( 'NONE', #12752, .T. ) ;
#14803=ORIENTED_EDGE ( 'NONE', *, *, #2609, .T. ) ;
#14804=CARTESIAN_POINT ( 'NONE',  ( 1.847034903785829574, -4.063013886994788493, 11.76058231742743665 ) ) ;
#14807=CARTESIAN_POINT ( 'NONE',  ( 16.56822296793089322, -0.009385634690641594599, -0.003834730849370937035 ) ) ;
#14808=DIRECTION ( 'NONE',  ( -0.7635533937278214944, 0.6204116510013479857, 0.1790966170213943998 ) ) ;
#14809=CIRCLE ( 'NONE', #13895, 16.06066017081991149 ) ;
#14813=CARTESIAN_POINT ( 'NONE',  ( 1.846822687350019754, 7.547953575784267066, -9.891732594446496662 ) ) ;
#14819=CARTESIAN_POINT ( 'NONE',  ( 0.3095370825347233956, 13.73357284481724783, -0.4597470195090692657 ) ) ;
#14820=( BOUNDED_SURFACE ( )  B_SPLINE_SURFACE ( 3, 1, ( 
 ( #18752, #3864 ),
 ( #8179, #14085 ),
 ( #11507, #15517 ),
 ( #15426, #14174 ) ),
 .UNSPECIFIED., .F., .F., .T. ) 
 B_SPLINE_SURFACE_WITH_KNOTS ( ( 4, 4 ),
 ( 2, 2 ),
 ( 0.000000000000000000, 1.000000000000000000 ),
 ( 0.000000000000000000, 1.000000000000000000 ),
 .UNSPECIFIED. ) 
 GEOMETRIC_REPRESENTATION_ITEM ( )  RATIONAL_B_SPLINE_SURFACE ( (
 ( 1.000000000000000000, 1.000000000000000000),
 ( 0.9593108457356467333, 0.9995965569486454649),
 ( 0.9593108457356467333, 0.9995965569486454649),
 ( 1.000000000000000000, 1.000000000000000000) ) ) 
 REPRESENTATION_ITEM ( '' )  SURFACE ( )  );
#14821=EDGE_CURVE ( 'NONE', #4379, #9019, #6848, .T. ) ;
#14826=ORIENTED_EDGE ( 'NONE', *, *, #5587, .T. ) ;
#14829=CARTESIAN_POINT ( 'NONE',  ( 1.861628059977342708, 11.66985327793199190, 4.358833901513087916 ) ) ;
#14832=CARTESIAN_POINT ( 'NONE',  ( 1.847247051441591514, -10.16425585218606109, 7.177495230324669961 ) ) ;
#14836=CARTESIAN_POINT ( 'NONE',  ( 1.342453679581834924, -14.34050741580204402, -3.649820028552883233 ) ) ;
#14837=CARTESIAN_POINT ( 'NONE',  ( 3.664313757352978485, 12.42002390572636372, -7.012524439851359759 ) ) ;
#14840=CARTESIAN_POINT ( 'NONE',  ( 1.846138399168762101, 7.646096044339892650, 9.815003036200437236 ) ) ;
#14841=CARTESIAN_POINT ( 'NONE',  ( 3.950837973638676281, 14.31366178983253512, 2.591948120961855118 ) ) ;
#14842=ORIENTED_EDGE ( 'NONE', *, *, #5440, .F. ) ;
#14845=ADVANCED_FACE ( 'NONE', ( #3975 ), #12967, .F. ) ;
#14848=ORIENTED_EDGE ( 'NONE', *, *, #16253, .F. ) ;
#14859=FACE_OUTER_BOUND ( 'NONE', #7155, .T. ) ;
#14869=CARTESIAN_POINT ( 'NONE',  ( 0.3095370825347234511, 11.38092634279639803, -7.700448427571746635 ) ) ;
#14872=EDGE_LOOP ( 'NONE', ( #14731, #13582, #17334, #18884 ) ) ;
#14874=EDGE_CURVE ( 'NONE', #5775, #15079, #2436, .T. ) ;
#14877=CARTESIAN_POINT ( 'NONE',  ( 0.3058872367615230181, 10.75034008168928068, -8.562166468153600718 ) ) ;
#14878=B_SPLINE_CURVE_WITH_KNOTS ( 'NONE', 3,
 ( #7569, #17487, #3336, #16052, #13379, #17882 ),
 .UNSPECIFIED., .F., .F.,
 ( 4, 2, 4 ),
 ( 0.000000000000000000, 0.001500839035891551139, 0.003001678071783102277 ),
 .UNSPECIFIED. ) ;
#14886=FACE_OUTER_BOUND ( 'NONE', #2608, .T. ) ;
#14889=AXIS2_PLACEMENT_3D ( 'NONE', #10693, #13651, #12220 ) ;
#14895=DIRECTION ( 'NONE',  ( -0.7561779333270775005, -0.5081796452863273084, 0.4122479608995688327 ) ) ;
#14897=EDGE_CURVE ( 'NONE', #18099, #4894, #15720, .T. ) ;
#14898=CARTESIAN_POINT ( 'NONE',  ( 2.002547531651519996, -9.778737580845755062, 7.942910686618138705 ) ) ;
#14900=CARTESIAN_POINT ( 'NONE',  ( 1.977228804421969688, 1.488378900182327991, 15.33060379559086073 ) ) ;
#14908=CARTESIAN_POINT ( 'NONE',  ( 0.3170788640506441158, -4.392045232375722641, -13.02120094575832709 ) ) ;
#14912=CARTESIAN_POINT ( 'NONE',  ( 0.3137051932979775248, 0.4596302728639756197, 13.73004976592202198 ) ) ;
#14913=VERTEX_POINT ( 'NONE', #7229 ) ;
#14916=B_SPLINE_CURVE_WITH_KNOTS ( 'NONE', 3,
 ( #16510, #15063, #17041, #5279, #18558, #6730 ),
 .UNSPECIFIED., .F., .F.,
 ( 4, 2, 4 ),
 ( 4.083989690778167730E-17, 0.0002014099069817300042, 0.0004028198139634191341 ),
 .UNSPECIFIED. ) ;
#14921=DIRECTION ( 'NONE',  ( -0.7635533937278214944, -0.1790966170213966202, 0.6204116510013472086 ) ) ;
#14924=CARTESIAN_POINT ( 'NONE',  ( 8.522092701127531811, -1.786985377231985694, -6.722964936702116034 ) ) ;
#14929=CARTESIAN_POINT ( 'NONE',  ( 2.002547531651519996, 12.57989064830759496, 0.6781519942172178350 ) ) ;
#14930=CARTESIAN_POINT ( 'NONE',  ( 0.3145734862173260038, 10.93207848441433683, 8.321353293018871611 ) ) ;
#14931=( BOUNDED_SURFACE ( )  B_SPLINE_SURFACE ( 3, 1, ( 
 ( #13209, #7492 ),
 ( #3164, #10157 ),
 ( #15981, #5942 ),
 ( #11787, #4528 ) ),
 .UNSPECIFIED., .F., .F., .T. ) 
 B_SPLINE_SURFACE_WITH_KNOTS ( ( 4, 4 ),
 ( 2, 2 ),
 ( 0.000000000000000000, 1.000000000000000000 ),
 ( 0.000000000000000000, 1.000000000000000000 ),
 .UNSPECIFIED. ) 
 GEOMETRIC_REPRESENTATION_ITEM ( )  RATIONAL_B_SPLINE_SURFACE ( (
 ( 1.000000000000000000, 1.000000000000000000),
 ( 0.7792777138730160313, 0.9689936506012927220),
 ( 0.7792777138730160313, 0.9689936506012927220),
 ( 1.000000000000000000, 1.000000000000000000) ) ) 
 REPRESENTATION_ITEM ( '' )  SURFACE ( )  );
#14933=CARTESIAN_POINT ( 'NONE',  ( 2.002547531651519996, 10.57595306287302250, -6.845637710436074386 ) ) ;
#14934=ORIENTED_EDGE ( 'NONE', *, *, #5054, .F. ) ;
#14938=VERTEX_POINT ( 'NONE', #4740 ) ;
#14945=VERTEX_POINT ( 'NONE', #6077 ) ;
#14946=CARTESIAN_POINT ( 'NONE',  ( 16.56872352241294521, 0.004907101719995680782, 0.009207754980064214098 ) ) ;
#14948=CARTESIAN_POINT ( 'NONE',  ( 8.522092701127531811, 6.722964936702098271, 1.786985377232055860 ) ) ;
#14957=CARTESIAN_POINT ( 'NONE',  ( 0.3132635586635958425, -12.89236642382225462, 4.743936529203192087 ) ) ;
#14958=CARTESIAN_POINT ( 'NONE',  ( 1.847247051441594179, -11.78111530882020297, -4.004229874809150047 ) ) ;
#14960=B_SPLINE_CURVE_WITH_KNOTS ( 'NONE', 3,
 ( #10369, #10078, #8839, #15907, #17341, #18866 ),
 .UNSPECIFIED., .F., .F.,
 ( 4, 2, 4 ),
 ( 3.671973638477265170E-17, 0.0001825746017570593200, 0.0003651492035140796086 ),
 .UNSPECIFIED. ) ;
#14961=ORIENTED_EDGE ( 'NONE', *, *, #10375, .T. ) ;
#14963=ORIENTED_EDGE ( 'NONE', *, *, #6830, .T. ) ;
#14965=CARTESIAN_POINT ( 'NONE',  ( 2.002547531651519996, -9.778737580845639599, -7.942910686618280813 ) ) ;
#14966=CARTESIAN_POINT ( 'NONE',  ( 2.636624412714134280, 2.862162146984768896, 15.80357026013147426 ) ) ;
#14967=( BOUNDED_SURFACE ( )  B_SPLINE_SURFACE ( 3, 1, ( 
 ( #10947, #627 ),
 ( #2492, #9682 ),
 ( #980, #16764 ),
 ( #12457, #11036 ) ),
 .UNSPECIFIED., .F., .F., .T. ) 
 B_SPLINE_SURFACE_WITH_KNOTS ( ( 4, 4 ),
 ( 2, 2 ),
 ( 0.000000000000000000, 1.000000000000000000 ),
 ( 0.000000000000000000, 1.000000000000000000 ),
 .UNSPECIFIED. ) 
 GEOMETRIC_REPRESENTATION_ITEM ( )  RATIONAL_B_SPLINE_SURFACE ( (
 ( 1.000000000000000000, 1.000000000000000000),
 ( 0.7792777138730158093, 0.9689936506012928330),
 ( 0.7792777138730158093, 0.9689936506012928330),
 ( 1.000000000000000000, 1.000000000000000000) ) ) 
 REPRESENTATION_ITEM ( '' )  SURFACE ( )  );
#14971=CARTESIAN_POINT ( 'NONE',  ( 1.846138399168762101, -12.43476674860266940, 0.4167076046095114505 ) ) ;
#14972=CARTESIAN_POINT ( 'NONE',  ( 3.512766787570837490, 10.40533104696128497, 10.87507422923887646 ) ) ;
#14974=CARTESIAN_POINT ( 'NONE',  ( 0.3151930723728398331, 8.013866567350898862, 11.16020735774769435 ) ) ;
#14984=EDGE_LOOP ( 'NONE', ( #13655, #10318, #9620, #18460 ) ) ;
#14985=VERTEX_POINT ( 'NONE', #11811 ) ;
#14990=CARTESIAN_POINT ( 'NONE',  ( 2.636624412717099908, 15.80357026013547816, -2.862162146981609201 ) ) ;
#14994=CARTESIAN_POINT ( 'NONE',  ( 1.847372867223022963, -3.945260592619128204, 11.80112642014553614 ) ) ;
#14995=B_SPLINE_CURVE_WITH_KNOTS ( 'NONE', 3,
 ( #5240, #6687, #18330, #6499, #16997, #3902 ),
 .UNSPECIFIED., .F., .F.,
 ( 4, 2, 4 ),
 ( 5.421010862427522170E-19, 0.0001825746017570577750, 0.0003651492035141150078 ),
 .UNSPECIFIED. ) ;
#14996=CARTESIAN_POINT ( 'NONE',  ( 0.3137051932979775248, -12.91601973349273891, 4.679953077377436266 ) ) ;
#14998=CARTESIAN_POINT ( 'NONE',  ( 2.747332970342022840, 7.555624153089857131, -14.49942876448584173 ) ) ;
#15008=CARTESIAN_POINT ( 'NONE',  ( 0.3137051932979792457, 12.91601973349270871, 4.679953077377533965 ) ) ;
#15015=ORIENTED_EDGE ( 'NONE', *, *, #16712, .T. ) ;
#15018=CARTESIAN_POINT ( 'NONE',  ( 1.959212340397945118, 4.509090217468684436, -11.71715421693493830 ) ) ;
#15019=CARTESIAN_POINT ( 'NONE',  ( 2.320520222537495680, -11.60169517779343096, -10.64885284335084847 ) ) ;
#15023=ADVANCED_FACE ( 'NONE', ( #343 ), #3078, .F. ) ;
#15025=CARTESIAN_POINT ( 'NONE',  ( 0.3148208552358953138, 11.24855514421875569, 7.888357771040743316 ) ) ;
#15028=CARTESIAN_POINT ( 'NONE',  ( 1.845755665166725068, 6.920419570228353301, 10.33920510797145909 ) ) ;
#15029=VERTEX_POINT ( 'NONE', #11047 ) ;
#15030=CARTESIAN_POINT ( 'NONE',  ( 3.512766787570760663, -10.87507422923897238, 10.40533104696129918 ) ) ;
#15031=B_SPLINE_CURVE_WITH_KNOTS ( 'NONE', 3,
 ( #14933, #3062, #13307, #8818, #14837, #17719 ),
 .UNSPECIFIED., .F., .F.,
 ( 4, 2, 4 ),
 ( 0.000000000000000000, 0.001500839035891550054, 0.003001678071783100109 ),
 .UNSPECIFIED. ) ;
#15033=CARTESIAN_POINT ( 'NONE',  ( 3.950837973638677170, 13.10350451991849141, -6.316429227969337923 ) ) ;
#15037=LINE ( 'NONE', #523, #12758 ) ;
#15039=FACE_OUTER_BOUND ( 'NONE', #12450, .T. ) ;
#15044=CARTESIAN_POINT ( 'NONE',  ( 16.56753206892534891, 0.004368917149004243779, -0.008432171035096398468 ) ) ;
#15045=CARTESIAN_POINT ( 'NONE',  ( 0.3137051932979809665, 13.20008686438111312, -3.805684345189650042 ) ) ;
#15047=LINE ( 'NONE', #5263, #2582 ) ;
#15049=( BOUNDED_SURFACE ( )  B_SPLINE_SURFACE ( 3, 1, ( 
 ( #13231, #4351 ),
 ( #10082, #10174 ),
 ( #147, #8841 ),
 ( #3083, #15999 ) ),
 .UNSPECIFIED., .F., .F., .T. ) 
 B_SPLINE_SURFACE_WITH_KNOTS ( ( 4, 4 ),
 ( 2, 2 ),
 ( 0.000000000000000000, 1.000000000000000000 ),
 ( 0.000000000000000000, 1.000000000000000000 ),
 .UNSPECIFIED. ) 
 GEOMETRIC_REPRESENTATION_ITEM ( )  RATIONAL_B_SPLINE_SURFACE ( (
 ( 1.000000000000000000, 1.000000000000000000),
 ( 0.7792777138730158093, 0.9689936506012928330),
 ( 0.7792777138730158093, 0.9689936506012928330),
 ( 1.000000000000000000, 1.000000000000000000) ) ) 
 REPRESENTATION_ITEM ( '' )  SURFACE ( )  );
#15050=CARTESIAN_POINT ( 'NONE',  ( 1.845756295923363322, -10.33914852636099191, -6.920504327368305120 ) ) ;
#15052=LINE ( 'NONE', #9592, #18119 ) ;
#15056=VERTEX_POINT ( 'NONE', #7998 ) ;
#15057=VECTOR ( 'NONE', #9483, 1000.000000000000114 ) ;
#15059=ORIENTED_EDGE ( 'NONE', *, *, #5811, .T. ) ;
#15061=VERTEX_POINT ( 'NONE', #1970 ) ;
#15062=EDGE_CURVE ( 'NONE', #12290, #12155, #6271, .T. ) ;
#15063=CARTESIAN_POINT ( 'NONE',  ( 0.4385251269669976359, -4.978066129061780032, 12.93791070501032436 ) ) ;
#15070=CARTESIAN_POINT ( 'NONE',  ( 2.705023505549863483, -3.294610156755986452, 12.88681800078731321 ) ) ;
#15071=AXIS2_PLACEMENT_3D ( 'NONE', #3061, #14643, #1554 ) ;
#15072=FACE_OUTER_BOUND ( 'NONE', #6297, .T. ) ;
#15075=CARTESIAN_POINT ( 'NONE',  ( 0.4862570985993235340, -7.559321496869339185, -11.67702470553373750 ) ) ;
#15079=VERTEX_POINT ( 'NONE', #12467 ) ;
#15083=CARTESIAN_POINT ( 'NONE',  ( 1.846138399168762101, -6.971848976710933954, -10.30487220521577818 ) ) ;
#15084=EDGE_CURVE ( 'NONE', #8361, #11620, #3700, .T. ) ;
#15085=EDGE_CURVE ( 'NONE', #4150, #15496, #18522, .T. ) ;
#15086=EDGE_CURVE ( 'NONE', #2621, #9990, #16710, .T. ) ;
#15098=CARTESIAN_POINT ( 'NONE',  ( 16.56822296793089322, -0.008619100080558715279, 0.005339139727952894703 ) ) ;
#15099=CARTESIAN_POINT ( 'NONE',  ( 0.4754618798421167414, 12.98792082933644743, 5.007009103465293265 ) ) ;
#15100=CARTESIAN_POINT ( 'NONE',  ( 2.002547531651519996, -3.242439124566566910, -12.17374746633581495 ) ) ;
#15103=VERTEX_POINT ( 'NONE', #439 ) ;
#15104=CARTESIAN_POINT ( 'NONE',  ( 16.57210152137263393, 0.01453130299868640209, -0.0006600038696348341314 ) ) ;
#15107=CARTESIAN_POINT ( 'NONE',  ( 3.377929128793397684, -10.50432311212909475, 9.234024516648283054 ) ) ;
#15109=AXIS2_PLACEMENT_3D ( 'NONE', #16143, #11939, #3422 ) ;
#15116=CARTESIAN_POINT ( 'NONE',  ( 0.3151926232592509591, 13.73922722301401400, -0.07678256780562460471 ) ) ;
#15124=ORIENTED_EDGE ( 'NONE', *, *, #14666, .T. ) ;
#15125=B_SPLINE_CURVE_WITH_KNOTS ( 'NONE', 3,
 ( #16422, #3006, #6286, #10685 ),
 .UNSPECIFIED., .F., .F.,
 ( 4, 4 ),
 ( 1.330347433792404293E-17, 0.003005512676784847462 ),
 .UNSPECIFIED. ) ;
#15126=EDGE_CURVE ( 'NONE', #8563, #17236, #13956, .T. ) ;
#15129=CARTESIAN_POINT ( 'NONE',  ( 0.3095370825347233956, -0.4597470195089253808, -13.73357284481725316 ) ) ;
#15130=EDGE_LOOP ( 'NONE', ( #1757, #16492, #18048, #6878 ) ) ;
#15134=CARTESIAN_POINT ( 'NONE',  ( 2.636624412715138366, -15.91454522070249311, -2.161493821597819665 ) ) ;
#15137=ORIENTED_EDGE ( 'NONE', *, *, #16443, .F. ) ;
#15140=CARTESIAN_POINT ( 'NONE',  ( 3.950837973638676281, 12.81214529934975310, 6.888253895133341409 ) ) ;
#15159=EDGE_LOOP ( 'NONE', ( #2866, #9762, #5229, #1805 ) ) ;
#15161=ORIENTED_EDGE ( 'NONE', *, *, #2636, .T. ) ;
#15163=B_SPLINE_CURVE_WITH_KNOTS ( 'NONE', 3,
 ( #17947, #14771, #10582, #4847, #258, #16012, #7630, #6181, #11309, #15683, #11122, #3849, #14265 ),
 .UNSPECIFIED., .F., .F.,
 ( 4, 3, 3, 3, 4 ),
 ( 2.453269466693398698E-18, 0.0002299780670421062274, 0.0004599561239687902829, 0.0006896788984287884972, 0.0009194956271626412558 ),
 .UNSPECIFIED. ) ;
#15167=CARTESIAN_POINT ( 'NONE',  ( 16.56872352241294521, 0.01033355228142499721, 0.001442253899401261912 ) ) ;
#15176=CARTESIAN_POINT ( 'NONE',  ( 2.636624412717099908, 15.80357026013547816, -2.862162146981609201 ) ) ;
#15179=DIRECTION ( 'NONE',  ( 0.000000000000000000, 0.000000000000000000, 1.000000000000000000 ) ) ;
#15193=CARTESIAN_POINT ( 'NONE',  ( 2.636624412715137922, 2.161493821597615828, 15.91454522070216093 ) ) ;
#15195=CARTESIAN_POINT ( 'NONE',  ( 1.846138399168762989, 9.815003036200414144, 7.646096044339929954 ) ) ;
#15202=B_SPLINE_CURVE_WITH_KNOTS ( 'NONE', 3,
 ( #9462, #15284, #4467, #16129 ),
 .UNSPECIFIED., .F., .F.,
 ( 4, 4 ),
 ( 9.204257061898183523E-17, 0.002004993803842712065 ),
 .UNSPECIFIED. ) ;
#15215=CARTESIAN_POINT ( 'NONE',  ( 3.950837973638675393, 6.888253895133479965, -12.81214529934967672 ) ) ;
#15217=CARTESIAN_POINT ( 'NONE',  ( 0.4862570985993235340, 13.89016912371017476, 0.7479633556562934604 ) ) ;
#15220=ADVANCED_FACE ( 'NONE', ( #9774 ), #14820, .F. ) ;
#15225=ORIENTED_EDGE ( 'NONE', *, *, #11190, .F. ) ;
#15226=CARTESIAN_POINT ( 'NONE',  ( 16.56753206892534891, -0.009389754735542259201, -0.001421777558675912110 ) ) ;
#15227=ORIENTED_EDGE ( 'NONE', *, *, #13273, .F. ) ;
#15231=VERTEX_POINT ( 'NONE', #6746 ) ;
#15232=CARTESIAN_POINT ( 'NONE',  ( 0.3142014840576516921, 11.33546131209473806, -7.762239086932731347 ) ) ;
#15244=CARTESIAN_POINT ( 'NONE',  ( 3.950837973638676281, -10.05648675950133963, 10.51028938476214059 ) ) ;
#15248=CARTESIAN_POINT ( 'NONE',  ( 0.4384471787762798112, -7.540925784514636909, 11.63197976518326371 ) ) ;
#15252=VERTEX_POINT ( 'NONE', #11136 ) ;
#15255=ORIENTED_EDGE ( 'NONE', *, *, #7287, .T. ) ;
#15259=ADVANCED_FACE ( 'NONE', ( #4146 ), #2469, .F. ) ;
#15260=CARTESIAN_POINT ( 'NONE',  ( 2.320520222538070776, 1.795797593769018485, -15.64520721754711730 ) ) ;
#15266=CARTESIAN_POINT ( 'NONE',  ( 2.320521194582656044, -11.60169518685945356, 10.64885423995117542 ) ) ;
#15268=CARTESIAN_POINT ( 'NONE',  ( 0.3095370825347233956, -11.38092634279623105, -7.700448427571997101 ) ) ;
#15276=CARTESIAN_POINT ( 'NONE',  ( 3.074695600507765025, 15.30693405987741684, -2.772091048738999142 ) ) ;
#15277=CARTESIAN_POINT ( 'NONE',  ( 16.56753206892534891, 0.008432171035096448775, -0.004368917149005361808 ) ) ;
#15280=CARTESIAN_POINT ( 'NONE',  ( 0.3720661004400037664, 8.694226082900744501, -10.73619472937692620 ) ) ;
#15282=LINE ( 'NONE', #2193, #17204 ) ;
#15284=CARTESIAN_POINT ( 'NONE',  ( 3.074695600507423521, -10.75417554975728329, -11.23985886659437483 ) ) ;
#15297=ORIENTED_EDGE ( 'NONE', *, *, #2619, .F. ) ;
#15302=CARTESIAN_POINT ( 'NONE',  ( 2.636624412714236865, 0.000000000000000000, 0.000000000000000000 ) ) ;
#15305=B_SPLINE_CURVE_WITH_KNOTS ( 'NONE', 3,
 ( #14841, #8728, #4721, #16286 ),
 .UNSPECIFIED., .F., .F.,
 ( 4, 4 ),
 ( 4.336808689942017736E-19, 0.003005512676784827947 ),
 .UNSPECIFIED. ) ;
#15310=CARTESIAN_POINT ( 'NONE',  ( 16.56679352167444819, -0.001390132774594504727, 0.009190982326619714232 ) ) ;
#15317=ORIENTED_EDGE ( 'NONE', *, *, #14897, .T. ) ;
#15321=CARTESIAN_POINT ( 'NONE',  ( 16.56753206892534891, 0.008432171035096382855, 0.004368917149004273269 ) ) ;
#15322=CARTESIAN_POINT ( 'NONE',  ( 0.3720661004400037664, -11.58636699658219982, 7.524064345033424139 ) ) ;
#15329=CARTESIAN_POINT ( 'NONE',  ( 1.861628059977342042, 10.38573835516722355, -6.879051339207178373 ) ) ;
#15330=DIRECTION ( 'NONE',  ( 0.000000000000000000, 0.000000000000000000, 1.000000000000000000 ) ) ;
#15338=ORIENTED_EDGE ( 'NONE', *, *, #4741, .T. ) ;
#15340=VECTOR ( 'NONE', #6738, 1000.000000000000114 ) ;
#15343=EDGE_CURVE ( 'NONE', #15056, #12767, #6210, .T. ) ;
#15345=DIRECTION ( 'NONE',  ( 0.000000000000000000, 0.000000000000000000, 1.000000000000000000 ) ) ;
#15346=CARTESIAN_POINT ( 'NONE',  ( 1.977228804422057840, -7.806978995470733373, 13.27756617201263545 ) ) ;
#15347=CARTESIAN_POINT ( 'NONE',  ( 1.254255976357671942, -5.487601330835209623, 13.61551404021223455 ) ) ;
#15348=DIRECTION ( 'NONE',  ( 0.7071067818211348444, 8.659560554583479511E-17, 0.7071067805519601901 ) ) ;
#15361=FACE_OUTER_BOUND ( 'NONE', #15798, .T. ) ;
#15365=CARTESIAN_POINT ( 'NONE',  ( 16.56782317627811096, -0.0003415813796006971566, 0.009814734722107082768 ) ) ;
#15372=CARTESIAN_POINT ( 'NONE',  ( 0.3137051932979757485, -8.442169467526770887, -10.83767969834812561 ) ) ;
#15376=CARTESIAN_POINT ( 'NONE',  ( 3.950837973638675393, 14.31366178983257242, -2.591948120961654833 ) ) ;
#15378=DIRECTION ( 'NONE',  ( 0.000000000000000000, 0.000000000000000000, 1.000000000000000000 ) ) ;
#15380=CARTESIAN_POINT ( 'NONE',  ( 0.4862570985993252548, 5.003653737315486794, 12.97920246947881395 ) ) ;
#15384=CARTESIAN_POINT ( 'NONE',  ( 3.664313757352971823, 2.831308606787245719, 13.97913389346634183 ) ) ;
#15385=CARTESIAN_POINT ( 'NONE',  ( 16.56822296793089322, 0.005339139727952925060, 0.008619100080558696197 ) ) ;
#15386=EDGE_LOOP ( 'NONE', ( #11621, #15916, #3688, #15647 ) ) ;
#15396=SURFACE_SIDE_STYLE ('',( #1151 ) ) ;
#15397=ADVANCED_FACE ( 'NONE', ( #11599 ), #14931, .F. ) ;
#15398=CARTESIAN_POINT ( 'NONE',  ( 2.002547531651519996, 9.778737580845815458, -7.942910686618064986 ) ) ;
#15400=CARTESIAN_POINT ( 'NONE',  ( 16.56753206892534891, -0.004368917149004301892, 0.008432171035096367243 ) ) ;
#15411=VECTOR ( 'NONE', #18672, 1000.000000000000114 ) ;
#15412=ORIENTED_EDGE ( 'NONE', *, *, #13374, .T. ) ;
#15413=CARTESIAN_POINT ( 'NONE',  ( 1.342453679581834924, -0.9602753779829698022, -14.76648944001040498 ) ) ;
#15415=CARTESIAN_POINT ( 'NONE',  ( 16.56822296793089322, 0.007741272030791082788, 0.006547366384935537215 ) ) ;
#15416=B_SPLINE_CURVE_WITH_KNOTS ( 'NONE', 3,
 ( #12313, #12227, #2184, #3321, #18143, #1808 ),
 .UNSPECIFIED., .F., .F.,
 ( 4, 2, 4 ),
 ( 7.047314121155778821E-19, 0.001657017934712349183, 0.003314035869424697932 ),
 .UNSPECIFIED. ) ;
#15417=CARTESIAN_POINT ( 'NONE',  ( 1.846613052777651198, -10.26230975746754659, -7.035606253495426898 ) ) ;
#15419=CARTESIAN_POINT ( 'NONE',  ( 2.002547531651519996, 11.75462648437101976, 4.532360870844369671 ) ) ;
#15425=CARTESIAN_POINT ( 'NONE',  ( 1.846138399168762101, -3.446241763652916124, -11.95493567637853971 ) ) ;
#15426=CARTESIAN_POINT ( 'NONE',  ( 16.56753206892534891, -0.006760771273036217388, -0.006669401563384900512 ) ) ;
#15432=ORIENTED_EDGE ( 'NONE', *, *, #16712, .F. ) ;
#15433=VERTEX_POINT ( 'NONE', #7975 ) ;
#15434=ORIENTED_EDGE ( 'NONE', *, *, #10347, .T. ) ;
#15440=CARTESIAN_POINT ( 'NONE',  ( 16.57210152137263393, 0.01453130299868522594, 0.0006600038696346533949 ) ) ;
#15445=ORIENTED_EDGE ( 'NONE', *, *, #3459, .F. ) ;
#15449=EDGE_CURVE ( 'NONE', #14774, #2897, #1883, .T. ) ;
#15450=ORIENTED_EDGE ( 'NONE', *, *, #11458, .T. ) ;
#15451=ORIENTED_EDGE ( 'NONE', *, *, #9849, .F. ) ;
#15452=VERTEX_POINT ( 'NONE', #1852 ) ;
#15456=DIRECTION ( 'NONE',  ( 0.7561779333270775005, 0.6322161072786955938, -0.1688126975276531827 ) ) ;
#15459=CIRCLE ( 'NONE', #9055, 16.06066017081991149 ) ;
#15467=CARTESIAN_POINT ( 'NONE',  ( 1.254255976358384705, 12.44256109021893941, -7.789651112956954115 ) ) ;
#15472=ORIENTED_EDGE ( 'NONE', *, *, #5897, .T. ) ;
#15477=CLOSED_SHELL ( 'NONE', ( #3272, #8111, #6657, #17581, #9377, #12700, #17048, #14573, #10181, #13382, #10873, #7444, #9495, #7933, #4393, #13441, #5284, #18634, #14266, #12514, #4827, #6342, #3245, #11400, #17915, #6784, #8368, #11436, #18732, #14267, #13148, #6512, #6758, #11017, #15953, #10552, #15259, #14845, #1535, #12144, #5078, #7308, #15552, #5612, #16602, #17690, #16205, #1592, #8008, #12149, #5394, #4879, #48, #15220, #5101, #10154, #5761, #16120, #9091, #18834, #13810, #6036, #512, #1557, #17378, #1889, #13387, #3292, #5156, #76, #3356, #6679, #16736, #16391, #3365, #4363, #12028, #16482, #16424, #11123, #3820, #3610, #7037, #3381, #12415, #15023, #6678, #8742, #653, #16778, #2081, #14709, #2468, #13364, #5720, #3699, #12188, #2361, #11382, #15584, #12883, #12387, #4281, #11973, #1492, #3678, #5262, #11315, #15709, #13832, #6799, #18417, #7123, #20, #2977, #14276, #4802, #2052, #12641, #18804, #8148, #8136, #16079, #11991, #2622, #15397, #2944, #11480, #5856, #17985, #5660, #2911 ) ) ;
#15479=ORIENTED_EDGE ( 'NONE', *, *, #13221, .F. ) ;
#15482=ORIENTED_EDGE ( 'NONE', *, *, #4981, .F. ) ;
#15483=CARTESIAN_POINT ( 'NONE',  ( 0.8740764193767940338, -9.070946295054064024, 11.05257066464529281 ) ) ;
#15494=ORIENTED_EDGE ( 'NONE', *, *, #10473, .T. ) ;
#15496=VERTEX_POINT ( 'NONE', #10647 ) ;
#15501=VERTEX_POINT ( 'NONE', #10547 ) ;
#15503=CARTESIAN_POINT ( 'NONE',  ( 0.3308579732647032867, 10.76782854710826776, 8.558831104906948539 ) ) ;
#15505=CARTESIAN_POINT ( 'NONE',  ( 3.950837973638676281, -10.05648675950133963, 10.51028938476214059 ) ) ;
#15507=CARTESIAN_POINT ( 'NONE',  ( 0.3058872367615226295, -11.46514199369363318, 7.578326039752564469 ) ) ;
#15509=FACE_OUTER_BOUND ( 'NONE', #9648, .T. ) ;
#15512=B_SPLINE_CURVE_WITH_KNOTS ( 'NONE', 3,
 ( #13425, #5866, #340, #11708, #4547, #10371, #16201 ),
 .UNSPECIFIED., .F., .F.,
 ( 4, 3, 4 ),
 ( 1.843143693225357538E-18, 0.0002299804304191480943, 0.0004168119862255878537 ),
 .UNSPECIFIED. ) ;
#15513=CARTESIAN_POINT ( 'NONE',  ( 16.56822296793089322, 0.006547366384936635295, 0.007741272030791194678 ) ) ;
#15517=CARTESIAN_POINT ( 'NONE',  ( 0.3170788640506440603, 4.100430649997962362, 13.11595226728159425 ) ) ;
#15522=VERTEX_POINT ( 'NONE', #6244 ) ;
#15524=B_SPLINE_CURVE_WITH_KNOTS ( 'NONE', 3,
 ( #10372, #10083, #15912, #10273, #8647, #14570 ),
 .UNSPECIFIED., .F., .F.,
 ( 4, 2, 4 ),
 ( 3.527508043940425264E-17, 0.0001825746017570591031, 0.0003651492035140829697 ),
 .UNSPECIFIED. ) ;
#15535=CARTESIAN_POINT ( 'NONE',  ( 16.56753206892534891, 0.009369540855502130061, 0.001549402974393180796 ) ) ;
#15537=ORIENTED_EDGE ( 'NONE', *, *, #1658, .T. ) ;
#15538=( BOUNDED_SURFACE ( )  B_SPLINE_SURFACE ( 3, 1, ( 
 ( #1028, #3996 ),
 ( #2822, #10007 ),
 ( #6869, #14224 ),
 ( #18699, #14401 ) ),
 .UNSPECIFIED., .F., .F., .T. ) 
 B_SPLINE_SURFACE_WITH_KNOTS ( ( 4, 4 ),
 ( 2, 2 ),
 ( 0.000000000000000000, 1.000000000000000000 ),
 ( 0.000000000000000000, 1.000000000000000000 ),
 .UNSPECIFIED. ) 
 GEOMETRIC_REPRESENTATION_ITEM ( )  RATIONAL_B_SPLINE_SURFACE ( (
 ( 1.000000000000000000, 1.000000000000000000),
 ( 0.9933953342250438912, 0.8357391271907739227),
 ( 0.9933953342250438912, 0.8357391271907739227),
 ( 1.000000000000000000, 1.000000000000000000) ) ) 
 REPRESENTATION_ITEM ( '' )  SURFACE ( )  );
#15540=VECTOR ( 'NONE', #333, 1000.000000000000114 ) ;
#15542=ORIENTED_EDGE ( 'NONE', *, *, #8507, .F. ) ;
#15543=B_SPLINE_CURVE_WITH_KNOTS ( 'NONE', 3,
 ( #4760, #2916, #18893, #13161, #8775, #14688 ),
 .UNSPECIFIED., .F., .F.,
 ( 4, 2, 4 ),
 ( 0.000000000000000000, 0.001657017934710630505, 0.003314035869421261011 ),
 .UNSPECIFIED. ) ;
#15549=ORIENTED_EDGE ( 'NONE', *, *, #6574, .T. ) ;
#15550=FACE_OUTER_BOUND ( 'NONE', #6135, .T. ) ;
#15552=ADVANCED_FACE ( 'NONE', ( #16381 ), #3717, .F. ) ;
#15555=CARTESIAN_POINT ( 'NONE',  ( 1.845755665166724846, -6.920419570228271589, -10.33920510797150882 ) ) ;
#15556=CARTESIAN_POINT ( 'NONE',  ( 0.4384471787762813100, -8.732395932355604629, -10.76632603192796722 ) ) ;
#15558=CARTESIAN_POINT ( 'NONE',  ( 0.3137051932979792457, 4.679953077377670745, -12.91601973349265720 ) ) ;
#15560=VERTEX_POINT ( 'NONE', #12263 ) ;
#15564=CARTESIAN_POINT ( 'NONE',  ( 16.57605080000000086, 0.000000000000000000, 0.000000000000000000 ) ) ;
#15568=CARTESIAN_POINT ( 'NONE',  ( 3.074695600507118431, 2.772091048739504959, -15.30693405987805811 ) ) ;
#15569=VERTEX_POINT ( 'NONE', #18093 ) ;
#15571=CARTESIAN_POINT ( 'NONE',  ( 0.8740764193766769052, -13.83508774436000088, 3.609949042658186169 ) ) ;
#15573=( BOUNDED_SURFACE ( )  B_SPLINE_SURFACE ( 3, 1, ( 
 ( #16096, #15987 ),
 ( #7218, #18859 ),
 ( #33, #11604 ),
 ( #11795, #2881 ) ),
 .UNSPECIFIED., .F., .F., .F. ) 
 B_SPLINE_SURFACE_WITH_KNOTS ( ( 4, 4 ),
 ( 2, 2 ),
 ( 0.000000000000000000, 1.000000000000000000 ),
 ( 0.000000000000000000, 1.000000000000000000 ),
 .UNSPECIFIED. ) 
 GEOMETRIC_REPRESENTATION_ITEM ( )  RATIONAL_B_SPLINE_SURFACE ( (
 ( 1.000000000000000000, 1.000000000000000000),
 ( 0.7792777138730158093, 0.9689936506012928330),
 ( 0.7792777138730158093, 0.9689936506012928330),
 ( 1.000000000000000000, 1.000000000000000000) ) ) 
 REPRESENTATION_ITEM ( '' )  SURFACE ( )  );
#15578=SHAPE_REPRESENTATION_RELATIONSHIP ( 'NONE' , 'NONE' ,  #14244, #6229 ) ;
#15579=CARTESIAN_POINT ( 'NONE',  ( 0.4862570985993235340, 7.559321496869593204, -11.67702470553357053 ) ) ;
#15580=B_SPLINE_CURVE_WITH_KNOTS ( 'NONE', 3,
 ( #688, #402, #6521, #10435 ),
 .UNSPECIFIED., .F., .F.,
 ( 4, 4 ),
 ( 2.851299179213411365E-16, 0.002004993803842618823 ),
 .UNSPECIFIED. ) ;
#15583=CARTESIAN_POINT ( 'NONE',  ( 1.977228804423455610, 11.52787183731216381, -10.21522664410554881 ) ) ;
#15584=ADVANCED_FACE ( 'NONE', ( #15674 ), #7645, .F. ) ;
#15588=CARTESIAN_POINT ( 'NONE',  ( 8.522092701127531811, -4.388629235579615262, 5.397361180353127175 ) ) ;
#15590=VERTEX_POINT ( 'NONE', #14152 ) ;
#15592=CARTESIAN_POINT ( 'NONE',  ( 1.254009781011991898, 3.563484327698415388, -14.24044713813362151 ) ) ;
#15596=EDGE_CURVE ( 'NONE', #4800, #13818, #14423, .T. ) ;
#15597=CARTESIAN_POINT ( 'NONE',  ( 0.3137051932979792457, -10.83767969834809008, 8.442169467526815296 ) ) ;
#15604=CARTESIAN_POINT ( 'NONE',  ( 0.4862570985993235340, -10.79774104611379215, 8.769551628660700260 ) ) ;
#15607=SURFACE_STYLE_FILL_AREA ( #5560 ) ;
#15611=EDGE_LOOP ( 'NONE', ( #12089, #11073, #13604, #971 ) ) ;
#15612=CIRCLE ( 'NONE', #12572, 16.06066017081991149 ) ;
#15613=ORIENTED_EDGE ( 'NONE', *, *, #4755, .F. ) ;
#15618=CARTESIAN_POINT ( 'NONE',  ( 1.846138399168762101, 9.815003036200520725, -7.646096044339786069 ) ) ;
#15621=CARTESIAN_POINT ( 'NONE',  ( 16.56782317627811096, 0.009439921864426468329, 0.002708056627497651414 ) ) ;
#15622=CARTESIAN_POINT ( 'NONE',  ( 16.56872352241294521, -0.009207754980064163791, 0.004907101719995779661 ) ) ;
#15631=CARTESIAN_POINT ( 'NONE',  ( 1.847034903785821136, 10.19974412751574810, -7.126331315909155251 ) ) ;
#15635=CARTESIAN_POINT ( 'NONE',  ( 1.861628059977342931, -12.00316790821103652, 3.332996951203584413 ) ) ;
#15639=AXIS2_PLACEMENT_3D ( 'NONE', #18472, #11132, #3859 ) ;
#15641=CARTESIAN_POINT ( 'NONE',  ( 2.747332970342022840, 14.63517873738947195, 7.289199830147158998 ) ) ;
#15643=( BOUNDED_SURFACE ( )  B_SPLINE_SURFACE ( 3, 1, ( 
 ( #1097, #12761 ),
 ( #18584, #5490 ),
 ( #17154, #4066 ),
 ( #9884, #2991 ) ),
 .UNSPECIFIED., .F., .F., .T. ) 
 B_SPLINE_SURFACE_WITH_KNOTS ( ( 4, 4 ),
 ( 2, 2 ),
 ( 0.000000000000000000, 1.000000000000000000 ),
 ( 0.000000000000000000, 1.000000000000000000 ),
 .UNSPECIFIED. ) 
 GEOMETRIC_REPRESENTATION_ITEM ( )  RATIONAL_B_SPLINE_SURFACE ( (
 ( 1.000000000000000000, 1.000000000000000000),
 ( 0.7792777138730158093, 0.9689936506012928330),
 ( 0.7792777138730158093, 0.9689936506012928330),
 ( 1.000000000000000000, 1.000000000000000000) ) ) 
 REPRESENTATION_ITEM ( '' )  SURFACE ( )  );
#15646=CARTESIAN_POINT ( 'NONE',  ( 0.3137051932979792457, 7.698472063774471685, 11.37800749014133928 ) ) ;
#15647=ORIENTED_EDGE ( 'NONE', *, *, #3890, .F. ) ;
#15649=EDGE_CURVE ( 'NONE', #4326, #16313, #3839, .T. ) ;
#15650=EDGE_CURVE ( 'NONE', #11605, #12470, #16938, .T. ) ;
#15651=EDGE_CURVE ( 'NONE', #15433, #8892, #13276, .T. ) ;
#15655=ORIENTED_EDGE ( 'NONE', *, *, #4826, .F. ) ;
#15656=CARTESIAN_POINT ( 'NONE',  ( 3.950837973638676281, -12.81214529934970336, -6.888253895133431115 ) ) ;
#15657=CARTESIAN_POINT ( 'NONE',  ( 1.847380140988739150, -12.44273713935591097, 0.1101766933248207875 ) ) ;
#15662=DIRECTION ( 'NONE',  ( -1.000000000000000000, -0.000000000000000000, -0.000000000000000000 ) ) ;
#15671=FACE_BOUND ( 'NONE', #2550, .T. ) ;
#15673=ORIENTED_EDGE ( 'NONE', *, *, #5897, .F. ) ;
#15674=FACE_OUTER_BOUND ( 'NONE', #16715, .T. ) ;
#15678=EDGE_CURVE ( 'NONE', #15103, #4379, #12731, .T. ) ;
#15680=( BOUNDED_SURFACE ( )  B_SPLINE_SURFACE ( 3, 1, ( 
 ( #14406, #14869 ),
 ( #14324, #10574 ),
 ( #2650, #7623 ),
 ( #16414, #12104 ) ),
 .UNSPECIFIED., .F., .F., .T. ) 
 B_SPLINE_SURFACE_WITH_KNOTS ( ( 4, 4 ),
 ( 2, 2 ),
 ( 0.000000000000000000, 1.000000000000000000 ),
 ( 0.000000000000000000, 1.000000000000000000 ),
 .UNSPECIFIED. ) 
 GEOMETRIC_REPRESENTATION_ITEM ( )  RATIONAL_B_SPLINE_SURFACE ( (
 ( 1.000000000000000000, 1.000000000000000000),
 ( 0.9933953342250436691, 0.8357391271907733676),
 ( 0.9933953342250436691, 0.8357391271907733676),
 ( 1.000000000000000000, 1.000000000000000000) ) ) 
 REPRESENTATION_ITEM ( '' )  SURFACE ( )  );
#15681=( BOUNDED_SURFACE ( )  B_SPLINE_SURFACE ( 3, 1, ( 
 ( #9245, #6291 ),
 ( #12019, #3406 ),
 ( #4856, #10590 ),
 ( #4661, #1989 ) ),
 .UNSPECIFIED., .F., .F., .T. ) 
 B_SPLINE_SURFACE_WITH_KNOTS ( ( 4, 4 ),
 ( 2, 2 ),
 ( 0.000000000000000000, 1.000000000000000000 ),
 ( 0.000000000000000000, 1.000000000000000000 ),
 .UNSPECIFIED. ) 
 GEOMETRIC_REPRESENTATION_ITEM ( )  RATIONAL_B_SPLINE_SURFACE ( (
 ( 1.000000000000000000, 1.000000000000000000),
 ( 0.9933953342250436691, 0.8357391271907733676),
 ( 0.9933953342250436691, 0.8357391271907733676),
 ( 1.000000000000000000, 1.000000000000000000) ) ) 
 REPRESENTATION_ITEM ( '' )  SURFACE ( )  );
#15683=CARTESIAN_POINT ( 'NONE',  ( 0.3148208552358953138, -8.260375059853256374, -10.97826876274321428 ) ) ;
#15684=CARTESIAN_POINT ( 'NONE',  ( 2.123976203522053297, 1.531817366691969884, -15.54801196254785189 ) ) ;
#15691=ORIENTED_EDGE ( 'NONE', *, *, #3302, .T. ) ;
#15702=ORIENTED_EDGE ( 'NONE', *, *, #4932, .T. ) ;
#15705=ORIENTED_EDGE ( 'NONE', *, *, #13789, .T. ) ;
#15708=CARTESIAN_POINT ( 'NONE',  ( 2.002547531651519996, 0.6781519942173496185, -12.57989064830758785 ) ) ;
#15709=ADVANCED_FACE ( 'NONE', ( #4508 ), #16886, .F. ) ;
#15715=EDGE_CURVE ( 'NONE', #12855, #16968, #14718, .T. ) ;
#15716=CARTESIAN_POINT ( 'NONE',  ( 0.000000000000000000, 0.000000000000000000, 0.000000000000000000 ) ) ;
#15717=CARTESIAN_POINT ( 'NONE',  ( 0.3170788640506440603, 13.74111462631963576, 0.1533108587036622894 ) ) ;
#15720=LINE ( 'NONE', #7038, #10276 ) ;
#15722=B_SPLINE_CURVE_WITH_KNOTS ( 'NONE', 3,
 ( #22, #5841, #17511, #2967, #8816, #1553 ),
 .UNSPECIFIED., .F., .F.,
 ( 4, 2, 4 ),
 ( 3.903127820947815962E-18, 0.0002017457492448081235, 0.0004034914984896123438 ),
 .UNSPECIFIED. ) ;
#15723=ORIENTED_EDGE ( 'NONE', *, *, #3300, .F. ) ;
#15731=CARTESIAN_POINT ( 'NONE',  ( 0.3148213771069372502, 8.260246460850879657, -10.97836617636215628 ) ) ;
#15739=B_SPLINE_CURVE_WITH_KNOTS ( 'NONE', 3,
 ( #9275, #15107, #3818, #771 ),
 .UNSPECIFIED., .F., .F.,
 ( 4, 4 ),
 ( 2.168404344971008868E-17, 0.003005512676784848763 ),
 .UNSPECIFIED. ) ;
#15743=CARTESIAN_POINT ( 'NONE',  ( 0.4862570985993235340, 5.003653737315670647, -12.97920246947874112 ) ) ;
#15745=CARTESIAN_POINT ( 'NONE',  ( 3.950837973638677170, 6.316429227969654114, -13.10350451991833687 ) ) ;
#15746=ORIENTED_EDGE ( 'NONE', *, *, #6920, .T. ) ;
#15753=CARTESIAN_POINT ( 'NONE',  ( 0.3132642857406499615, -3.740125687984641178, -13.21852905223342667 ) ) ;
#15755=CARTESIAN_POINT ( 'NONE',  ( 3.512766787570702487, -10.87507422923887113, -10.40533104696150701 ) ) ;
#15759=CARTESIAN_POINT ( 'NONE',  ( 1.846955891736115962, -3.593597880662430910, 11.91257079808167596 ) ) ;
#15760=CARTESIAN_POINT ( 'NONE',  ( 1.959212340397945562, 3.239239832449027467, 12.12975361829676579 ) ) ;
#15765=EDGE_CURVE ( 'NONE', #8324, #15496, #14529, .T. ) ;
#15769=CARTESIAN_POINT ( 'NONE',  ( 3.950837973638668288, 0.000000000000000000, 0.000000000000000000 ) ) ;
#15772=CARTESIAN_POINT ( 'NONE',  ( 2.697797270744667131, -4.970631985779678352, 12.33058466479267778 ) ) ;
#15773=VERTEX_POINT ( 'NONE', #17304 ) ;
#15775=B_SPLINE_CURVE_WITH_KNOTS ( 'NONE', 3,
 ( #3327, #1910, #9074, #2010 ),
 .UNSPECIFIED., .F., .F.,
 ( 4, 4 ),
 ( 0.000000000000000000, 0.002004993803842881200 ),
 .UNSPECIFIED. ) ;
#15776=CARTESIAN_POINT ( 'NONE',  ( 0.3148213771069381384, -12.99360322443199678, -4.463459503829131592 ) ) ;
#15778=EDGE_LOOP ( 'NONE', ( #4765, #4864, #8408, #10233 ) ) ;
#15786=CARTESIAN_POINT ( 'NONE',  ( 0.3137051932979809665, -3.805684345189881856, 13.20008686438104739 ) ) ;
#15792=EDGE_CURVE ( 'NONE', #14483, #10527, #7581, .T. ) ;
#15793=CIRCLE ( 'NONE', #8791, 14.54644660717763927 ) ;
#15797=CARTESIAN_POINT ( 'NONE',  ( 16.56872352241294521, -0.01027347319884440620, 0.001821578298044753286 ) ) ;
#15798=EDGE_LOOP ( 'NONE', ( #16785, #10309, #15482, #15673 ) ) ;
#15799=CARTESIAN_POINT ( 'NONE',  ( 2.636624412714236865, 0.000000000000000000, 0.000000000000000000 ) ) ;
#15803=ORIENTED_EDGE ( 'NONE', *, *, #14821, .T. ) ;
#15808=CARTESIAN_POINT ( 'NONE',  ( 0.3145734862173233393, 13.15783074029284272, -3.953068532979860272 ) ) ;
#15809=B_SPLINE_CURVE_WITH_KNOTS ( 'NONE', 3,
 ( #2832, #15854, #11652, #7265, #7361, #11373 ),
 .UNSPECIFIED., .F., .F.,
 ( 4, 2, 4 ),
 ( 3.551420023959826846E-17, 0.0001825746017570578021, 0.0003651492035140800965 ),
 .UNSPECIFIED. ) ;
#15816=FACE_OUTER_BOUND ( 'NONE', #3174, .T. ) ;
#15818=B_SPLINE_CURVE_WITH_KNOTS ( 'NONE', 3,
 ( #16355, #17885, #12394, #3788, #15266, #2178 ),
 .UNSPECIFIED., .F., .F.,
 ( 4, 2, 4 ),
 ( 9.215718466126787689E-19, 0.001657017934710630505, 0.003314035869421260144 ),
 .UNSPECIFIED. ) ;
#15819=CARTESIAN_POINT ( 'NONE',  ( 0.3137051932979809665, -13.20008686438108647, 3.805684345189735307 ) ) ;
#15828=CARTESIAN_POINT ( 'NONE',  ( 0.000000000000000000, 0.000000000000000000, 1.500000000000000000 ) ) ;
#15829=CARTESIAN_POINT ( 'NONE',  ( 0.3170788640506441158, 8.200855617524535290, 11.02668139258444846 ) ) ;
#15830=CARTESIAN_POINT ( 'NONE',  ( 2.636624412714292376, 11.60464335004048309, 11.10302021257707850 ) ) ;
#15831=ORIENTED_EDGE ( 'NONE', *, *, #669, .T. ) ;
#15841=CARTESIAN_POINT ( 'NONE',  ( 0.3308579732647040639, 4.812490080619379995, -12.88563776947740358 ) ) ;
#15846=ORIENTED_EDGE ( 'NONE', *, *, #15126, .T. ) ;
#15848=ORIENTED_EDGE ( 'NONE', *, *, #5486, .T. ) ;
#15854=CARTESIAN_POINT ( 'NONE',  ( 1.959283090834838426, 3.239245055717136168, -12.12982544407801555 ) ) ;
#15858=VERTEX_POINT ( 'NONE', #11958 ) ;
#15859=CARTESIAN_POINT ( 'NONE',  ( 1.846138399168762101, 0.4167076046097279440, -12.43476674860266051 ) ) ;
#15861=B_SPLINE_CURVE_WITH_KNOTS ( 'NONE', 3,
 ( #4731, #16299, #3280, #13513, #4543, #240 ),
 .UNSPECIFIED., .F., .F.,
 ( 4, 2, 4 ),
 ( 4.240893905418535831E-17, 0.0002014099069817287303, 0.0004028198139634150141 ),
 .UNSPECIFIED. ) ;
#15862=DIRECTION ( 'NONE',  ( -1.000000000000000000, -0.000000000000000000, -0.000000000000000000 ) ) ;
#15867=CARTESIAN_POINT ( 'NONE',  ( 3.950837973638675393, 10.05648675950126325, 10.51028938476221342 ) ) ;
#15869=CARTESIAN_POINT ( 'NONE',  ( 2.002547531651519996, 6.845637710436190737, 10.57595306287294612 ) ) ;
#15870=ORIENTED_EDGE ( 'NONE', *, *, #6398, .F. ) ;
#15871=CARTESIAN_POINT ( 'NONE',  ( 0.3095370825347224519, 0.4597470195092092093, -13.73357284481724250 ) ) ;
#15872=CARTESIAN_POINT ( 'NONE',  ( 0.3145734862173260038, -12.96846406299303212, -4.535879238195068552 ) ) ;
#15873=EDGE_CURVE ( 'NONE', #17236, #5784, #1631, .T. ) ;
#15879=CARTESIAN_POINT ( 'NONE',  ( 16.56782317627811096, -0.009228812961909619098, -0.003357783021327203059 ) ) ;
#15880=CARTESIAN_POINT ( 'NONE',  ( 0.4862570985993252548, -3.580942890621766406, 13.44146924561379741 ) ) ;
#15882=DIRECTION ( 'NONE',  ( -1.000000000000000000, -0.000000000000000000, -0.000000000000000000 ) ) ;
#15883=VERTEX_POINT ( 'NONE', #7579 ) ;
#15886=CARTESIAN_POINT ( 'NONE',  ( 3.074695600507268978, -2.772091048739378394, 15.30693405987788935 ) ) ;
#15887=CARTESIAN_POINT ( 'NONE',  ( 1.342453679581834924, 9.456403821038962931, -11.38190519890843255 ) ) ;
#15890=FACE_OUTER_BOUND ( 'NONE', #5516, .T. ) ;
#15891=CARTESIAN_POINT ( 'NONE',  ( 3.664313757352976264, -7.012524439851403280, -12.42002390572634418 ) ) ;
#15893=CARTESIAN_POINT ( 'NONE',  ( 0.3058872367615230181, -3.664492643742856881, 13.24582953854924128 ) ) ;
#15894=CARTESIAN_POINT ( 'NONE',  ( 1.959283090834841090, 6.829027319138399221, -10.53516775895152691 ) ) ;
#15898=EDGE_CURVE ( 'NONE', #11694, #8226, #11812, .T. ) ;
#15901=CARTESIAN_POINT ( 'NONE',  ( 1.847421816787902404, -0.02876707915213067360, 12.44300551404155541 ) ) ;
#15902=ORIENTED_EDGE ( 'NONE', *, *, #849, .F. ) ;
#15903=CARTESIAN_POINT ( 'NONE',  ( 2.636624412714236865, 0.000000000000000000, 0.000000000000000000 ) ) ;
#15905=CARTESIAN_POINT ( 'NONE',  ( 0.3137051932979792457, 13.20008686438105983, 3.805684345189833451 ) ) ;
#15907=CARTESIAN_POINT ( 'NONE',  ( 1.861706995891669880, 9.751699138048550708, -7.751853334747211832 ) ) ;
#15912=CARTESIAN_POINT ( 'NONE',  ( 1.918918678667043354, 10.48466773720562273, 6.832809802519053122 ) ) ;
#15916=ORIENTED_EDGE ( 'NONE', *, *, #3677, .F. ) ;
#15919=ORIENTED_EDGE ( 'NONE', *, *, #8416, .T. ) ;
#15921=EDGE_CURVE ( 'NONE', #13362, #10401, #15976, .T. ) ;
#15926=CARTESIAN_POINT ( 'NONE',  ( 8.522092701127531811, 5.841710761610186431, -3.777034505568459100 ) ) ;
#15932=CARTESIAN_POINT ( 'NONE',  ( 0.4862570985993235340, -8.769551628660655851, -10.79774104611382946 ) ) ;
#15933=CARTESIAN_POINT ( 'NONE',  ( 1.846822687350020198, 3.566003975885688515, 11.92063725419900777 ) ) ;
#15934=CARTESIAN_POINT ( 'NONE',  ( 0.4385251269669978580, 4.978066129061869738, -12.93791070501029239 ) ) ;
#15935=DIRECTION ( 'NONE',  ( 0.7561779333270775005, -0.1688126975276555974, -0.6322161072786950387 ) ) ;
#15936=ORIENTED_EDGE ( 'NONE', *, *, #10399, .F. ) ;
#15940=CARTESIAN_POINT ( 'NONE',  ( 0.3058872367615226295, 13.72992299905060065, 0.6080468242581433813 ) ) ;
#15941=ORIENTED_EDGE ( 'NONE', *, *, #3454, .F. ) ;
#15943=EDGE_CURVE ( 'NONE', #2897, #7741, #15739, .T. ) ;
#15950=CARTESIAN_POINT ( 'NONE',  ( 0.3137051932979792457, 13.73004976592202198, 0.4596302728640249136 ) ) ;
#15953=ADVANCED_FACE ( 'NONE', ( #17890 ), #18837, .F. ) ;
#15956=EDGE_CURVE ( 'NONE', #14563, #11376, #2306, .T. ) ;
#15958=VERTEX_POINT ( 'NONE', #9816 ) ;
#15959=DIRECTION ( 'NONE',  ( 1.000000000000000000, 0.000000000000000000, 0.000000000000000000 ) ) ;
#15960=CARTESIAN_POINT ( 'NONE',  ( 1.846524061778019199, 0.3544704288994222074, -12.43723828841088164 ) ) ;
#15961=VERTEX_POINT ( 'NONE', #9644 ) ;
#15968=ORIENTED_EDGE ( 'NONE', *, *, #1748, .F. ) ;
#15969=CARTESIAN_POINT ( 'NONE',  ( 0.3170788640506440603, 13.02120094575828269, 4.392045232375855868 ) ) ;
#15971=CARTESIAN_POINT ( 'NONE',  ( 1.846138399168762101, -9.815003036200353748, -7.646096044340000120 ) ) ;
#15973=VECTOR ( 'NONE', #4118, 1000.000000000000000 ) ;
#15976=B_SPLINE_CURVE_WITH_KNOTS ( 'NONE', 3,
 ( #13479, #304, #17984, #10525, #16360, #3239 ),
 .UNSPECIFIED., .F., .F.,
 ( 4, 2, 4 ),
 ( 2.474737474518078493E-18, 0.0002017457492448081235, 0.0004034914984896138075 ),
 .UNSPECIFIED. ) ;
#15977=DIRECTION ( 'NONE',  ( 0.000000000000000000, 0.000000000000000000, 1.000000000000000000 ) ) ;
#15980=CARTESIAN_POINT ( 'NONE',  ( 16.58200780006414732, -0.0006320991582348829945, 0.01115192838421569070 ) ) ;
#15981=CARTESIAN_POINT ( 'NONE',  ( 16.57778382496167424, 0.006312874906843865194, 0.01354073047775895648 ) ) ;
#15983=CARTESIAN_POINT ( 'NONE',  ( 2.353870697619110608, -10.00946331859657334, -8.216087327473042379 ) ) ;
#15984=CARTESIAN_POINT ( 'NONE',  ( 0.4862570985993235340, -13.89016912371018186, 0.7479633556561964269 ) ) ;
#15985=EDGE_LOOP ( 'NONE', ( #5343, #5930, #9271, #18245 ) ) ;
#15986=ORIENTED_EDGE ( 'NONE', *, *, #17591, .F. ) ;
#15987=CARTESIAN_POINT ( 'NONE',  ( 2.747332970342022840, -11.66639548242815572, 11.45495994260713957 ) ) ;
#15991=CARTESIAN_POINT ( 'NONE',  ( 0.3137051932979792457, -0.4596302728640728752, 13.73004976592201842 ) ) ;
#15999=CARTESIAN_POINT ( 'NONE',  ( 0.4754618798421171855, -13.89949764182683190, 0.7484603771383911974 ) ) ;
#16002=CARTESIAN_POINT ( 'NONE',  ( 0.4385251269669942498, 7.540955776459739468, 11.63205320541525900 ) ) ;
#16012=CARTESIAN_POINT ( 'NONE',  ( 0.3151930723728413319, -8.013866567350813597, -11.16020735774775829 ) ) ;
#16014=CARTESIAN_POINT ( 'NONE',  ( 0.3170788640506440603, 7.952793437297573931, 11.20690911610906326 ) ) ;
#16016=CARTESIAN_POINT ( 'NONE',  ( 3.512766787570810401, -2.025881399556277440, -14.91422000116817159 ) ) ;
#16017=EDGE_LOOP ( 'NONE', ( #12312, #4673, #13146, #10113 ) ) ;
#16023=CARTESIAN_POINT ( 'NONE',  ( 3.950837973638668288, 0.000000000000000000, 0.000000000000000000 ) ) ;
#16026=FACE_OUTER_BOUND ( 'NONE', #604, .T. ) ;
#16038=CARTESIAN_POINT ( 'NONE',  ( 16.56872352241294521, 0.004907101719995680782, 0.009207754980064214098 ) ) ;
#16039=ORIENTED_EDGE ( 'NONE', *, *, #8884, .T. ) ;
#16040=CARTESIAN_POINT ( 'NONE',  ( 0.4862570985993235340, -3.580942890621579444, -13.44146924561384537 ) ) ;
#16043=CARTESIAN_POINT ( 'NONE',  ( 2.002547531651519996, -12.17374746633575988, -3.242439124566779185 ) ) ;
#16045=CARTESIAN_POINT ( 'NONE',  ( 16.57210152137263393, -0.009075239946109120437, -0.01136813053532156892 ) ) ;
#16046=DIRECTION ( 'NONE',  ( 0.7561779333270775005, 0.3559159372837274460, 0.5491072561318377510 ) ) ;
#16052=CARTESIAN_POINT ( 'NONE',  ( 3.353306896162453921, -13.88482890973695660, -1.348936822032970495 ) ) ;
#16053=B_SPLINE_CURVE_WITH_KNOTS ( 'NONE', 3,
 ( #3910, #11364, #7255, #9812 ),
 .UNSPECIFIED., .F., .F.,
 ( 4, 4 ),
 ( 2.298835888684693015E-16, 0.002004993803842571552 ),
 .UNSPECIFIED. ) ;
#16056=EDGE_CURVE ( 'NONE', #9114, #7547, #15459, .T. ) ;
#16058=CARTESIAN_POINT ( 'NONE',  ( 2.705023505549863039, 10.24007717649592841, -8.489131503859667305 ) ) ;
#16059=VERTEX_POINT ( 'NONE', #2735 ) ;
#16063=VERTEX_POINT ( 'NONE', #11814 ) ;
#16068=CARTESIAN_POINT ( 'NONE',  ( 0.3720661004400037664, 7.524064345033464107, 11.58636699658217672 ) ) ;
#16070=EDGE_CURVE ( 'NONE', #620, #18610, #18065, .T. ) ;
#16074=VECTOR ( 'NONE', #13720, 1000.000000000000227 ) ;
#16075=MECHANICAL_DESIGN_GEOMETRIC_PRESENTATION_REPRESENTATION('',(#9957),#14544);
#16076=PRODUCT_DEFINITION ( 'UNKNOWN', '', #10827, #4852 ) ;
#16079=ADVANCED_FACE ( 'NONE', ( #8582 ), #15680, .F. ) ;
#16080=VECTOR ( 'NONE', #10996, 1000.000000000000000 ) ;
#16082=CARTESIAN_POINT ( 'NONE',  ( 3.074695600507159732, -15.30693405987801370, -2.772091048739451669 ) ) ;
#16090=CARTESIAN_POINT ( 'NONE',  ( 1.918918678667047129, 4.466049546133911363, 11.69059232068580556 ) ) ;
#16091=CARTESIAN_POINT ( 'NONE',  ( 1.562796894703937678, 4.769696007084728073, 1.500000000000000000 ) ) ;
#16096=CARTESIAN_POINT ( 'NONE',  ( 16.58200780006414732, 0.0006320991582340733123, 0.01115192838421469670 ) ) ;
#16099=ORIENTED_EDGE ( 'NONE', *, *, #6353, .T. ) ;
#16103=CARTESIAN_POINT ( 'NONE',  ( 0.3170788640506441158, 0.1533108587036162707, 13.74111462631963576 ) ) ;
#16111=CARTESIAN_POINT ( 'NONE',  ( 0.3132642857406501835, 7.641821025099867271, 11.41580579227779779 ) ) ;
#16114=CARTESIAN_POINT ( 'NONE',  ( 16.56872352241294521, 0.007512283835804314455, -0.007240717549633915451 ) ) ;
#16115=EDGE_LOOP ( 'NONE', ( #7897, #10073, #15059, #11893 ) ) ;
#16118=ORIENTED_EDGE ( 'NONE', *, *, #1206, .F. ) ;
#16120=ADVANCED_FACE ( 'NONE', ( #13525 ), #12259, .F. ) ;
#16121=CARTESIAN_POINT ( 'NONE',  ( 1.846138399168762101, -9.815003036200353748, -7.646096044340000120 ) ) ;
#16122=CARTESIAN_POINT ( 'NONE',  ( 1.977228804422746400, -6.152949558601968683, -14.12033626431101041 ) ) ;
#16123=CARTESIAN_POINT ( 'NONE',  ( 0.4862570985993252548, 10.79774104611373353, 8.769551628660776643 ) ) ;
#16129=CARTESIAN_POINT ( 'NONE',  ( 3.950837973638675393, -10.05648675950118509, -10.51028938476228980 ) ) ;
#16130=CARTESIAN_POINT ( 'NONE',  ( 3.074695600507694859, 14.01296402267844066, 6.754521329824622278 ) ) ;
#16131=CARTESIAN_POINT ( 'NONE',  ( 1.846138399168762989, 3.446241763652997836, 11.95493567637851839 ) ) ;
#16132=CARTESIAN_POINT ( 'NONE',  ( 0.3148208552358962020, -11.24855514421869529, -7.888357771040825028 ) ) ;
#16133=CARTESIAN_POINT ( 'NONE',  ( 1.846524061778018977, 7.023652644192272199, 10.27028962889599484 ) ) ;
#16136=EDGE_LOOP ( 'NONE', ( #10479, #15450, #13537, #3845 ) ) ;
#16138=FACE_OUTER_BOUND ( 'NONE', #5299, .T. ) ;
#16140=ORIENTED_EDGE ( 'NONE', *, *, #12102, .F. ) ;
#16143=CARTESIAN_POINT ( 'NONE',  ( 3.950837973638668288, 0.000000000000000000, 0.000000000000000000 ) ) ;
#16144=CARTESIAN_POINT ( 'NONE',  ( 2.320520222537238553, -13.71278186123262799, 7.743191299717230969 ) ) ;
#16145=CARTESIAN_POINT ( 'NONE',  ( 0.3058872367615230181, 4.821066432589326212, 12.87003593440630311 ) ) ;
#16149=CARTESIAN_POINT ( 'NONE',  ( 1.846138399168762989, 3.446241763652997836, 11.95493567637851839 ) ) ;
#16156=CARTESIAN_POINT ( 'NONE',  ( 0.8740764193767259771, -13.31469591265765118, -5.211550415969147920 ) ) ;
#16164=EDGE_LOOP ( 'NONE', ( #11188, #2553, #11494, #5776 ) ) ;
#16167=VERTEX_POINT ( 'NONE', #16866 ) ;
#16168=CARTESIAN_POINT ( 'NONE',  ( 2.002547531651519996, 7.942910686618313676, -9.778737580845612953 ) ) ;
#16174=VERTEX_POINT ( 'NONE', #12469 ) ;
#16176=CARTESIAN_POINT ( 'NONE',  ( 0.3170788640506441158, -8.200855617524453578, -11.02668139258451063 ) ) ;
#16177=FACE_OUTER_BOUND ( 'NONE', #7977, .T. ) ;
#16182=CARTESIAN_POINT ( 'NONE',  ( 3.377929128793398572, 12.84367544717943410, -5.536064832134035996 ) ) ;
#16187=B_SPLINE_CURVE_WITH_KNOTS ( 'NONE', 3,
 ( #4079, #14308, #16016, #3004 ),
 .UNSPECIFIED., .F., .F.,
 ( 4, 4 ),
 ( 3.750785467376078809E-16, 0.002004993803842428438 ),
 .UNSPECIFIED. ) ;
#16190=EDGE_CURVE ( 'NONE', #8004, #13362, #2075, .T. ) ;
#16192=CARTESIAN_POINT ( 'NONE',  ( 1.847168016377981115, 9.955470380986737311, -7.464000291196308368 ) ) ;
#16193=EDGE_CURVE ( 'NONE', #2734, #2050, #6421, .T. ) ;
#16200=LINE ( 'NONE', #13326, #7821 ) ;
#16201=CARTESIAN_POINT ( 'NONE',  ( 1.847426409206450959, -2.029922383240494730E-11, 12.44303504652081038 ) ) ;
#16205=ADVANCED_FACE ( 'NONE', ( #4051 ), #9717, .F. ) ;
#16206=VECTOR ( 'NONE', #16607, 1000.000000000000114 ) ;
#16210=ORIENTED_EDGE ( 'NONE', *, *, #14176, .F. ) ;
#16213=B_SPLINE_CURVE_WITH_KNOTS ( 'NONE', 3,
 ( #4572, #5996, #11925, #17763, #11835, #13162, #75, #9058, #17672, #16132, #4667, #11736, #273 ),
 .UNSPECIFIED., .F., .F.,
 ( 4, 3, 3, 3, 4 ),
 ( 4.906538933386797396E-18, 0.0002299780670421066068, 0.0004599561239687925598, 0.0006896788984287864372, 0.0009194956271626387621 ),
 .UNSPECIFIED. ) ;
#16215=CARTESIAN_POINT ( 'NONE',  ( 2.705023505549864371, 4.909285963184069956, 12.36217802824807421 ) ) ;
#16216=CARTESIAN_POINT ( 'NONE',  ( 16.56753206892534891, -0.008490833999798953410, -0.004253784598196148035 ) ) ;
#16220=CARTESIAN_POINT ( 'NONE',  ( 1.845756295923360435, -12.43231724724606835, 0.4783934145701590479 ) ) ;
#16223=MANIFOLD_SOLID_BREP ( 'Keyway', #15477 ) ;
#16225=CARTESIAN_POINT ( 'NONE',  ( 0.3137051932979757485, 8.442169467526850823, 10.83767969834806166 ) ) ;
#16227=CARTESIAN_POINT ( 'NONE',  ( 1.847372867223030068, 11.86627781945713167, -3.744745203533853317 ) ) ;
#16228=CARTESIAN_POINT ( 'NONE',  ( 1.959212340397916030, 9.750290364083625150, 7.909199412631181758 ) ) ;
#16229=DIRECTION ( 'NONE',  ( -1.000000000000000000, 0.000000000000000000, 0.000000000000000000 ) ) ;
#16230=B_SPLINE_CURVE_WITH_KNOTS ( 'NONE', 3,
 ( #1907, #4868, #18146, #5046, #10898, #752 ),
 .UNSPECIFIED., .F., .F.,
 ( 4, 2, 4 ),
 ( 0.000000000000000000, 0.001656992708824547161, 0.003313985417649093455 ),
 .UNSPECIFIED. ) ;
#16232=EDGE_CURVE ( 'NONE', #1343, #10403, #4139, .T. ) ;
#16233=ORIENTED_EDGE ( 'NONE', *, *, #17987, .T. ) ;
#16238=DIRECTION ( 'NONE',  ( 0.000000000000000000, 0.000000000000000000, 1.000000000000000000 ) ) ;
#16244=CARTESIAN_POINT ( 'NONE',  ( 3.074695600507531434, 11.23985886659412259, 10.75417554975680900 ) ) ;
#16250=B_SPLINE_CURVE_WITH_KNOTS ( 'NONE', 3,
 ( #10727, #405, #14829, #16272, #4805, #7483 ),
 .UNSPECIFIED., .F., .F.,
 ( 4, 2, 4 ),
 ( 8.673617379884035472E-19, 0.0001828790815886939666, 0.0003657581631773870658 ),
 .UNSPECIFIED. ) ;
#16251=CARTESIAN_POINT ( 'NONE',  ( 2.320520222536399668, 3.126729907239529815, 15.43440824796666710 ) ) ;
#16252=CARTESIAN_POINT ( 'NONE',  ( 0.3137051932979792457, 12.91601973349270871, 4.679953077377533965 ) ) ;
#16253=EDGE_CURVE ( 'NONE', #12855, #12290, #3905, .T. ) ;
#16255=EDGE_CURVE ( 'NONE', #7527, #10168, #2785, .T. ) ;
#16262=CARTESIAN_POINT ( 'NONE',  ( 3.664313757352974932, -5.926151963190458893, 12.97355833021538096 ) ) ;
#16264=ORIENTED_EDGE ( 'NONE', *, *, #16911, .T. ) ;
#16267=B_SPLINE_CURVE_WITH_KNOTS ( 'NONE', 3,
 ( #5185, #6811, #11030, #16847 ),
 .UNSPECIFIED., .F., .F.,
 ( 4, 4 ),
 ( 0.000000000000000000, 0.002004993803842541195 ),
 .UNSPECIFIED. ) ;
#16269=ORIENTED_EDGE ( 'NONE', *, *, #4663, .T. ) ;
#16270=CARTESIAN_POINT ( 'NONE',  ( 1.846524061778021419, 4.180439405448487911, -11.71897913237544664 ) ) ;
#16271=CARTESIAN_POINT ( 'NONE',  ( 0.4754618798421167414, -13.89949764182682124, -0.7484603771385852644 ) ) ;
#16272=CARTESIAN_POINT ( 'NONE',  ( 1.918921323896324083, 11.69058285425790977, 4.466082741316246718 ) ) ;
#16275=B_SPLINE_CURVE_WITH_KNOTS ( 'NONE', 3,
 ( #2907, #7142, #2634, #11445 ),
 .UNSPECIFIED., .F., .F.,
 ( 4, 4 ),
 ( 2.076240083260000355E-17, 0.003005512676784849197 ),
 .UNSPECIFIED. ) ;
#16277=CARTESIAN_POINT ( 'NONE',  ( 8.522092701127531811, 6.489356537178224471, -2.505958102592553693 ) ) ;
#16281=CARTESIAN_POINT ( 'NONE',  ( 16.58200780006414732, 0.009393638146078525306, 0.006043560077721743008 ) ) ;
#16285=DIRECTION ( 'NONE',  ( 0.000000000000000000, 0.000000000000000000, 1.000000000000000000 ) ) ;
#16286=CARTESIAN_POINT ( 'NONE',  ( 2.002547531651519996, 12.17374746633578475, 3.242439124566693476 ) ) ;
#16292=VERTEX_POINT ( 'NONE', #11792 ) ;
#16293=EDGE_CURVE ( 'NONE', #11007, #620, #8245, .T. ) ;
#16297=CARTESIAN_POINT ( 'NONE',  ( 0.3145729642390355796, -13.73540280162741212, 0.3065092323350734893 ) ) ;
#16299=CARTESIAN_POINT ( 'NONE',  ( 0.4385251269669947494, -13.39302348765811068, 3.577373010348662508 ) ) ;
#16300=PLANE ( 'NONE',  #10225 ) ;
#16313=VERTEX_POINT ( 'NONE', #16091 ) ;
#16314=ORIENTED_EDGE ( 'NONE', *, *, #12311, .F. ) ;
#16316=CARTESIAN_POINT ( 'NONE',  ( 2.002547531651519996, -12.57989064830759141, -0.6781519942173057647 ) ) ;
#16317=FACE_OUTER_BOUND ( 'NONE', #6343, .T. ) ;
#16327=B_SPLINE_CURVE_WITH_KNOTS ( 'NONE', 3,
 ( #6892, #17486, #7275, #13088, #18821, #18543, #11570, #3491, #5815, #14614, #4391, #10222, #4213 ),
 .UNSPECIFIED., .F., .F.,
 ( 4, 3, 3, 3, 4 ),
 ( 2.168404344971008868E-18, 0.0002299804304191468746, 0.0004599608082120234371, 0.0006467586077648000654, 0.0008336169836825981817 ),
 .UNSPECIFIED. ) ;
#16329=DIRECTION ( 'NONE',  ( -0.7635533937278216055, -0.6453904417649388714, 0.02138673900301666167 ) ) ;
#16333=ORIENTED_EDGE ( 'NONE', *, *, #11407, .F. ) ;
#16338=VECTOR ( 'NONE', #14808, 1000.000000000000000 ) ;
#16339=CARTESIAN_POINT ( 'NONE',  ( 1.847168016377979116, -7.464000291196340342, -9.955470380986712442 ) ) ;
#16340=AXIS2_PLACEMENT_3D ( 'NONE', #12358, #5095, #2051 ) ;
#16341=EDGE_CURVE ( 'NONE', #5432, #14483, #15305, .T. ) ;
#16346=VERTEX_POINT ( 'NONE', #10551 ) ;
#16350=FACE_OUTER_BOUND ( 'NONE', #9716, .T. ) ;
#16352=LINE ( 'NONE', #9083, #14418 ) ;
#16355=CARTESIAN_POINT ( 'NONE',  ( 0.4862570985993235340, -10.79774104611379215, 8.769551628660700260 ) ) ;
#16356=ORIENTED_EDGE ( 'NONE', *, *, #17461, .F. ) ;
#16358=DIRECTION ( 'NONE',  ( -1.000000000000000000, -0.000000000000000000, -0.000000000000000000 ) ) ;
#16360=CARTESIAN_POINT ( 'NONE',  ( 0.4384471787762856398, 11.63197976518328680, 7.540925784514595165 ) ) ;
#16364=ORIENTED_EDGE ( 'NONE', *, *, #6009, .F. ) ;
#16368=VERTEX_POINT ( 'NONE', #8822 ) ;
#16369=LINE ( 'NONE', #3252, #10282 ) ;
#16371=CARTESIAN_POINT ( 'NONE',  ( 0.3137051932979792457, 13.73004976592202198, 0.4596302728640249136 ) ) ;
#16372=CYLINDRICAL_SURFACE ( 'NONE', #5203, 5.000000000000000000 ) ;
#16376=CARTESIAN_POINT ( 'NONE',  ( 0.3151930723728406103, 11.07033375389132246, 8.137566970826403789 ) ) ;
#16379=CARTESIAN_POINT ( 'NONE',  ( 0.3137051932979792457, 13.20008686438105983, 3.805684345189833451 ) ) ;
#16381=FACE_OUTER_BOUND ( 'NONE', #16115, .T. ) ;
#16383=CARTESIAN_POINT ( 'NONE',  ( 0.3137051932979809665, 3.805684345189785933, 13.20008686438107581 ) ) ;
#16388=VERTEX_POINT ( 'NONE', #14555 ) ;
#16390=EDGE_LOOP ( 'NONE', ( #13608, #10162, #17962, #3374 ) ) ;
#16391=ADVANCED_FACE ( 'NONE', ( #1756 ), #1177, .F. ) ;
#16395=CARTESIAN_POINT ( 'NONE',  ( 2.002547531651520885, 10.57595306287292480, 6.845637710436228929 ) ) ;
#16397=CARTESIAN_POINT ( 'NONE',  ( 0.3137051932979757485, 13.73004976592202020, -0.4596302728640235258 ) ) ;
#16398=CARTESIAN_POINT ( 'NONE',  ( 0.3308579732647007887, -8.558831104906994725, 10.76782854710824111 ) ) ;
#16409=AXIS2_PLACEMENT_3D ( 'NONE', #13163, #13740, #15179 ) ;
#16413=DIRECTION ( 'NONE',  ( 0.7561779333270775005, -0.5081796452863246438, -0.4122479608995723299 ) ) ;
#16414=CARTESIAN_POINT ( 'NONE',  ( 16.56872352241294521, -0.001442253899401298341, 0.01033355228142499027 ) ) ;
#16417=VERTEX_POINT ( 'NONE', #10352 ) ;
#16422=CARTESIAN_POINT ( 'NONE',  ( 3.950837973638677170, 1.958075594453790869, 14.41405733518061538 ) ) ;
#16424=ADVANCED_FACE ( 'NONE', ( #8913 ), #17532, .F. ) ;
#16427=CARTESIAN_POINT ( 'NONE',  ( 0.3137051932979792457, 7.698472063774471685, 11.37800749014133928 ) ) ;
#16428=DIRECTION ( 'NONE',  ( 0.000000000000000000, 0.000000000000000000, -1.000000000000000000 ) ) ;
#16429=CARTESIAN_POINT ( 'NONE',  ( 2.320521194581854907, 10.64885423995017355, 11.60169518685927059 ) ) ;
#16437=ORIENTED_EDGE ( 'NONE', *, *, #1398, .F. ) ;
#16442=CARTESIAN_POINT ( 'NONE',  ( 2.636624412716062071, -14.14563173255412742, -7.605649742760987486 ) ) ;
#16443=EDGE_CURVE ( 'NONE', #5049, #471, #14629, .T. ) ;
#16444=CARTESIAN_POINT ( 'NONE',  ( 3.353306896162455697, 1.348936822033017124, -13.88482890973694950 ) ) ;
#16445=ORIENTED_EDGE ( 'NONE', *, *, #8085, .F. ) ;
#16450=CARTESIAN_POINT ( 'NONE',  ( 16.57778382496167424, 0.01092721432668994352, 0.01018821665058780926 ) ) ;
#16452=B_SPLINE_CURVE_WITH_KNOTS ( 'NONE', 3,
 ( #4065, #12666, #9882, #7127, #14011, #9983 ),
 .UNSPECIFIED., .F., .F.,
 ( 4, 2, 4 ),
 ( 1.946286347258496500E-18, 0.0002017457492448080964, 0.0004034914984896142412 ),
 .UNSPECIFIED. ) ;
#16457=FACE_OUTER_BOUND ( 'NONE', #14528, .T. ) ;
#16463=CARTESIAN_POINT ( 'NONE',  ( 3.950837973638675393, -6.888253895133384930, 12.81214529934972823 ) ) ;
#16466=CARTESIAN_POINT ( 'NONE',  ( 3.664313757352975376, 9.645155442698909454, -10.50730552161222597 ) ) ;
#16468=CARTESIAN_POINT ( 'NONE',  ( 1.845755665166724846, 4.296872077620840891, -11.67596932341229987 ) ) ;
#16474=DIRECTION ( 'NONE',  ( -0.7561779333270775005, 0.6106991889125087392, -0.2350349629540122165 ) ) ;
#16482=ADVANCED_FACE ( 'NONE', ( #18189 ), #16923, .F. ) ;
#16483=ORIENTED_EDGE ( 'NONE', *, *, #13154, .F. ) ;
#16486=EDGE_LOOP ( 'NONE', ( #4320, #6634, #2312, #17817 ) ) ;
#16492=ORIENTED_EDGE ( 'NONE', *, *, #7282, .T. ) ;
#16494=CARTESIAN_POINT ( 'NONE',  ( 3.950837973638676281, -1.958075594453890789, 14.41405733518059940 ) ) ;
#16495=CARTESIAN_POINT ( 'NONE',  ( 16.56872352241294521, -0.007512283835805501873, -0.007240717549633963156 ) ) ;
#16499=CARTESIAN_POINT ( 'NONE',  ( 0.3939875929385661668, 3.598491969338414531, -13.34133634968951831 ) ) ;
#16500=CARTESIAN_POINT ( 'NONE',  ( 3.664313757352963830, 12.97355833021539873, 5.926151963190401162 ) ) ;
#16502=EDGE_CURVE ( 'NONE', #9780, #14694, #5709, .T. ) ;
#16504=CARTESIAN_POINT ( 'NONE',  ( 16.56753206892534891, -0.006669401563384969034, 0.006760771273036147132 ) ) ;
#16510=CARTESIAN_POINT ( 'NONE',  ( 0.4862570985993252548, -5.003653737315580052, 12.97920246947877665 ) ) ;
#16511=B_SPLINE_CURVE_WITH_KNOTS ( 'NONE', 3,
 ( #12980, #11286, #4103, #15656 ),
 .UNSPECIFIED., .F., .F.,
 ( 4, 4 ),
 ( 4.459867448574166155E-16, 0.002004993803842844771 ),
 .UNSPECIFIED. ) ;
#16512=CARTESIAN_POINT ( 'NONE',  ( 2.002547531651519996, 12.17374746633582561, -3.242439124566524278 ) ) ;
#16517=CARTESIAN_POINT ( 'NONE',  ( 8.438534575730034959, 6.454982381540289360, 2.341351102130301065 ) ) ;
#16518=CARTESIAN_POINT ( 'NONE',  ( 1.861706995891674099, -12.44571539481144384, 0.5394761475745415424 ) ) ;
#16523=CARTESIAN_POINT ( 'NONE',  ( 2.320521194583481606, -1.795798718314370213, -15.64520804578356561 ) ) ;
#16525=CARTESIAN_POINT ( 'NONE',  ( 1.861628059977341154, -11.66985327793196170, -4.358833901513171405 ) ) ;
#16528=CARTESIAN_POINT ( 'NONE',  ( 16.56753206892534891, 0.004253784598196760393, 0.008490833999798020129 ) ) ;
#16534=DIRECTION ( 'NONE',  ( -0.7561779333270775005, -0.3559159372837353286, 0.5491072561318327550 ) ) ;
#16537=CARTESIAN_POINT ( 'NONE',  ( 8.438534575730034959, -4.221456476902702981, 5.415535776177505589 ) ) ;
#16538=CARTESIAN_POINT ( 'NONE',  ( 3.512766787570765548, -13.25664064834477429, 7.127386085302765295 ) ) ;
#16542=EDGE_CURVE ( 'NONE', #10380, #9212, #5984, .T. ) ;
#16545=CARTESIAN_POINT ( 'NONE',  ( 16.57210152137263393, -0.01361613799508851197, -0.005118120558001528972 ) ) ;
#16551=VERTEX_POINT ( 'NONE', #5182 ) ;
#16562=CARTESIAN_POINT ( 'NONE',  ( 0.3148213771069373057, 13.73693585713733967, 0.2297580318215192152 ) ) ;
#16563=CARTESIAN_POINT ( 'NONE',  ( 2.636624412714237309, 11.10302021257826866, 11.60464335004050973 ) ) ;
#16566=CARTESIAN_POINT ( 'NONE',  ( 1.847168016377980670, -9.955470380986684020, 7.464000291196382086 ) ) ;
#16568=FACE_OUTER_BOUND ( 'NONE', #14653, .T. ) ;
#16570=CARTESIAN_POINT ( 'NONE',  ( 0.3058872367615226295, 10.75034008168916166, 8.562166468153757037 ) ) ;
#16573=CARTESIAN_POINT ( 'NONE',  ( 0.8740764193766107359, 7.708542792189345683, 12.04241474977975557 ) ) ;
#16574=ORIENTED_EDGE ( 'NONE', *, *, #15085, .F. ) ;
#16577=ORIENTED_EDGE ( 'NONE', *, *, #9849, .T. ) ;
#16578=LINE ( 'NONE', #526, #7486 ) ;
#16582=B_SPLINE_CURVE_WITH_KNOTS ( 'NONE', 3,
 ( #4026, #9841, #15872, #15776, #12725, #1057, #5632, #2763, #17035, #8611, #5730, #1447, #11581 ),
 .UNSPECIFIED., .F., .F.,
 ( 4, 3, 3, 3, 4 ),
 ( 4.670885906470169154E-18, 0.0002299780670421044384, 0.0004599561239687884940, 0.0006896788984287876298, 0.0009194956271626387621 ),
 .UNSPECIFIED. ) ;
#16583=CARTESIAN_POINT ( 'NONE',  ( 0.3145734862173260593, -13.73540602248380615, -0.3064017202076792512 ) ) ;
#16588=CARTESIAN_POINT ( 'NONE',  ( 2.636624412715137922, -15.91454522070252153, 2.161493821597598508 ) ) ;
#16589=CARTESIAN_POINT ( 'NONE',  ( 16.57778382496167424, -0.01482878558584693925, 0.001819584982831843212 ) ) ;
#16592=CARTESIAN_POINT ( 'NONE',  ( 3.353306896162453477, -9.252610477110343012, 10.44017738170053278 ) ) ;
#16594=CARTESIAN_POINT ( 'NONE',  ( 1.847372867223022963, -11.80112642014552371, -3.945260592619169948 ) ) ;
#16602=ADVANCED_FACE ( 'NONE', ( #973 ), #2397, .F. ) ;
#16603=CARTESIAN_POINT ( 'NONE',  ( 2.002547531651520885, 10.57595306287292480, 6.845637710436228929 ) ) ;
#16606=CARTESIAN_POINT ( 'NONE',  ( 1.959212340397940899, -3.239239832448945755, -12.12975361829679066 ) ) ;
#16607=DIRECTION ( 'NONE',  ( 0.7561779333270775005, -0.3559159372837316093, -0.5491072561318351974 ) ) ;
#16608=CARTESIAN_POINT ( 'NONE',  ( 1.977436885026095270, -6.153171729168663617, 14.12046670317548980 ) ) ;
#16610=AXIS2_PLACEMENT_3D ( 'NONE', #2556, #14513, #1232 ) ;
#16613=ORIENTED_EDGE ( 'NONE', *, *, #11594, .T. ) ;
#16616=EDGE_LOOP ( 'NONE', ( #15902, #14372, #5700, #15870 ) ) ;
#16617=DIRECTION ( 'NONE',  ( -1.000000000000000000, -0.000000000000000000, -0.000000000000000000 ) ) ;
#16625=CARTESIAN_POINT ( 'NONE',  ( 1.254009781011254487, 14.64464726212552037, -1.011465182607978130 ) ) ;
#16628=EDGE_CURVE ( 'NONE', #14233, #16174, #13495, .T. ) ;
#16630=CARTESIAN_POINT ( 'NONE',  ( 16.56872352241294521, -0.009207754980063714498, -0.004907101719994726684 ) ) ;
#16631=CARTESIAN_POINT ( 'NONE',  ( 0.3720661004400040439, 3.575426119359372823, -13.34435358167249142 ) ) ;
#16632=CARTESIAN_POINT ( 'NONE',  ( 3.664313757352971379, -1.627055439596372777, 14.16986885736092461 ) ) ;
#16633=CARTESIAN_POINT ( 'NONE',  ( 2.636624412716913390, 14.14563173255587536, -7.605649742760633991 ) ) ;
#16637=CARTESIAN_POINT ( 'NONE',  ( 16.56753206892534891, -0.004253784598196824578, -0.008490833999797990639 ) ) ;
#16638=ORIENTED_EDGE ( 'NONE', *, *, #4472, .T. ) ;
#16639=CARTESIAN_POINT ( 'NONE',  ( 0.3308579732647025096, 12.88563776947746398, 4.812490080619245880 ) ) ;
#16641=ORIENTED_EDGE ( 'NONE', *, *, #15873, .F. ) ;
#16645=CARTESIAN_POINT ( 'NONE',  ( 0.3142011359265305392, 13.73310835363014348, -0.3830873813806805472 ) ) ;
#16646=AXIS2_PLACEMENT_3D ( 'NONE', #2773, #4325, #9954 ) ;
#16649=CARTESIAN_POINT ( 'NONE',  ( 1.977436885025426694, 15.33079650480377154, 1.488549889121579817 ) ) ;
#16653=CARTESIAN_POINT ( 'NONE',  ( 1.846613052777651198, -9.862487290071051405, 7.585914669018136713 ) ) ;
#16654=B_SPLINE_CURVE_WITH_KNOTS ( 'NONE', 3,
 ( #3766, #18567, #5473, #8440, #14275, #8535 ),
 .UNSPECIFIED., .F., .F.,
 ( 4, 2, 4 ),
 ( 5.421010862427522170E-20, 0.0001828790815886950779, 0.0003657581631773901016 ),
 .UNSPECIFIED. ) ;
#16661=CARTESIAN_POINT ( 'NONE',  ( 3.074695600507260984, -14.01296402267893448, 6.754521329824735076 ) ) ;
#16669=ORIENTED_EDGE ( 'NONE', *, *, #14386, .F. ) ;
#16671=CARTESIAN_POINT ( 'NONE',  ( 3.950837973638677170, -1.958075594453692503, -14.41405733518062959 ) ) ;
#16675=CARTESIAN_POINT ( 'NONE',  ( 3.950837973638668288, 0.000000000000000000, 0.000000000000000000 ) ) ;
#16685=CARTESIAN_POINT ( 'NONE',  ( 0.4754618798421162973, -8.775436892861034011, -10.80499583390522567 ) ) ;
#16687=CARTESIAN_POINT ( 'NONE',  ( 0.3137051932979792457, -13.20008686438103140, -3.805684345189927154 ) ) ;
#16688=VERTEX_POINT ( 'NONE', #11800 ) ;
#16690=EDGE_LOOP ( 'NONE', ( #15124, #6776 ) ) ;
#16700=VECTOR ( 'NONE', #12305, 1000.000000000000000 ) ;
#16702=CARTESIAN_POINT ( 'NONE',  ( 3.950837973638676281, -12.81214529934970336, -6.888253895133431115 ) ) ;
#16703=DIRECTION ( 'NONE',  ( -1.000000000000000000, -0.000000000000000000, -0.000000000000000000 ) ) ;
#16709=B_SPLINE_CURVE_WITH_KNOTS ( 'NONE', 3,
 ( #6960, #5233, #2363, #3983, #11168, #16804 ),
 .UNSPECIFIED., .F., .F.,
 ( 4, 2, 4 ),
 ( 8.673617379884035472E-19, 0.001500839035891551572, 0.003001678071783102277 ),
 .UNSPECIFIED. ) ;
#16710=B_SPLINE_CURVE_WITH_KNOTS ( 'NONE', 3,
 ( #7715, #6459, #13522, #1875, #16500, #9421 ),
 .UNSPECIFIED., .F., .F.,
 ( 4, 2, 4 ),
 ( 0.000000000000000000, 0.001500839035891550922, 0.003001678071783101844 ),
 .UNSPECIFIED. ) ;
#16712=EDGE_CURVE ( 'NONE', #6853, #11007, #12814, .T. ) ;
#16713=ORIENTED_EDGE ( 'NONE', *, *, #18030, .T. ) ;
#16715=EDGE_LOOP ( 'NONE', ( #9895, #3172, #1328, #8374 ) ) ;
#16722=ORIENTED_EDGE ( 'NONE', *, *, #8065, .T. ) ;
#16728=CARTESIAN_POINT ( 'NONE',  ( 16.56753206892534891, -0.006760771273035160941, 0.006669401563385170262 ) ) ;
#16736=ADVANCED_FACE ( 'NONE', ( #13795 ), #10446, .F. ) ;
#16738=ORIENTED_EDGE ( 'NONE', *, *, #9427, .F. ) ;
#16742=CARTESIAN_POINT ( 'NONE',  ( 0.4862570985993252548, -12.97920246947875889, -5.003653737315625349 ) ) ;
#16749=CARTESIAN_POINT ( 'NONE',  ( 0.3132642857406489623, -11.41580579227782444, 7.641821025099830855 ) ) ;
#16763=CARTESIAN_POINT ( 'NONE',  ( 3.950837973638668288, 14.41405733518061716, 1.958075594453843493 ) ) ;
#16764=CARTESIAN_POINT ( 'NONE',  ( 1.342453679581834924, -12.51077660954460136, -7.902645620902585932 ) ) ;
#16771=CARTESIAN_POINT ( 'NONE',  ( 2.353870697619112384, 12.92712089195302738, 0.7635393531606785578 ) ) ;
#16775=B_SPLINE_CURVE_WITH_KNOTS ( 'NONE', 3,
 ( #1624, #104, #1827, #17700, #3040, #6130, #11667, #4506, #11765, #14912 ),
 .UNSPECIFIED., .F., .F.,
 ( 4, 3, 3, 4 ),
 ( 0.0004597478348664300451, 0.0004599561239687907166, 0.0006896788984287883888, 0.0009194956271626400631 ),
 .UNSPECIFIED. ) ;
#16778=ADVANCED_FACE ( 'NONE', ( #5100 ), #14967, .F. ) ;
#16782=EDGE_CURVE ( 'NONE', #15522, #6394, #1174, .T. ) ;
#16783=ORIENTED_EDGE ( 'NONE', *, *, #11830, .F. ) ;
#16785=ORIENTED_EDGE ( 'NONE', *, *, #1777, .F. ) ;
#16787=CARTESIAN_POINT ( 'NONE',  ( 1.846613052777650976, -0.3401093050880946711, -12.43780859207240219 ) ) ;
#16790=CARTESIAN_POINT ( 'NONE',  ( 0.8740764193768816304, 0.8420116711623857331, -14.27348595579795010 ) ) ;
#16792=EDGE_CURVE ( 'NONE', #10630, #12492, #5494, .T. ) ;
#16798=ORIENTED_EDGE ( 'NONE', *, *, #10049, .T. ) ;
#16799=ORIENTED_EDGE ( 'NONE', *, *, #1071, .T. ) ;
#16800=ORIENTED_EDGE ( 'NONE', *, *, #5194, .F. ) ;
#16804=CARTESIAN_POINT ( 'NONE',  ( 3.950837973638675393, -13.10350451991835818, -6.316429227969608817 ) ) ;
#16805=CARTESIAN_POINT ( 'NONE',  ( 0.3095370825347224519, -13.73357284481725138, 0.4597470195089713441 ) ) ;
#16808=CARTESIAN_POINT ( 'NONE',  ( 16.57210152137263393, 0.01136813053532160708, -0.009075239946109073599 ) ) ;
#16817=CARTESIAN_POINT ( 'NONE',  ( 1.861628059977343153, -4.358833901513129661, 11.66985327793197236 ) ) ;
#16838=CARTESIAN_POINT ( 'NONE',  ( 0.3095370825347224519, 7.700448427572037069, -11.38092634279620263 ) ) ;
#16841=CARTESIAN_POINT ( 'NONE',  ( 1.254009781012375813, 11.25324419414251942, -9.426200207652035701 ) ) ;
#16842=CARTESIAN_POINT ( 'NONE',  ( 0.3170788640506441158, 4.100430649998145327, -13.11595226728153385 ) ) ;
#16847=CARTESIAN_POINT ( 'NONE',  ( 2.636624412714994037, -14.46769361191274328, -6.973567714907344950 ) ) ;
#16849=CARTESIAN_POINT ( 'NONE',  ( 2.123976203522053741, -1.531817366691644144, -15.54801196254788742 ) ) ;
#16850=CARTESIAN_POINT ( 'NONE',  ( 0.3095370825347233956, -13.73357284481725138, 0.4597470195089733425 ) ) ;
#16855=CARTESIAN_POINT ( 'NONE',  ( 16.58200780006414732, 0.002844973367391573534, -0.01080144354108867819 ) ) ;
#16861=DIRECTION ( 'NONE',  ( 0.000000000000000000, 0.000000000000000000, 1.000000000000000000 ) ) ;
#16865=CARTESIAN_POINT ( 'NONE',  ( 2.353870697619111496, -10.90705766126224674, 6.980654702310806314 ) ) ;
#16866=CARTESIAN_POINT ( 'NONE',  ( 1.846138399168762101, -10.30487220521574976, 6.971848976710974810 ) ) ;
#16867=EDGE_CURVE ( 'NONE', #4709, #7061, #14269, .T. ) ;
#16871=B_SPLINE_CURVE_WITH_KNOTS ( 'NONE', 3,
 ( #13592, #10642, #5080, #511, #18089, #14929 ),
 .UNSPECIFIED., .F., .F.,
 ( 4, 2, 4 ),
 ( 0.000000000000000000, 0.0001828790815886942919, 0.0003657581631773885837 ),
 .UNSPECIFIED. ) ;
#16882=CARTESIAN_POINT ( 'NONE',  ( 0.4862570985993235340, 8.769551628660890330, -10.79774104611363761 ) ) ;
#16883=CARTESIAN_POINT ( 'NONE',  ( 2.636624412715137922, -6.973567714907947135, 14.46769361191283920 ) ) ;
#16884=VECTOR ( 'NONE', #14357, 1000.000000000000000 ) ;
#16886=( BOUNDED_SURFACE ( )  B_SPLINE_SURFACE ( 3, 1, ( 
 ( #11484, #3043 ),
 ( #5631, #106 ),
 ( #5923, #14435 ),
 ( #8890, #15871 ) ),
 .UNSPECIFIED., .F., .F., .T. ) 
 B_SPLINE_SURFACE_WITH_KNOTS ( ( 4, 4 ),
 ( 2, 2 ),
 ( 0.000000000000000000, 1.000000000000000000 ),
 ( 0.000000000000000000, 1.000000000000000000 ),
 .UNSPECIFIED. ) 
 GEOMETRIC_REPRESENTATION_ITEM ( )  RATIONAL_B_SPLINE_SURFACE ( (
 ( 1.000000000000000000, 1.000000000000000000),
 ( 0.9593108457356467333, 0.9995965569486454649),
 ( 0.9593108457356467333, 0.9995965569486454649),
 ( 1.000000000000000000, 1.000000000000000000) ) ) 
 REPRESENTATION_ITEM ( '' )  SURFACE ( )  );
#16891=EDGE_CURVE ( 'NONE', #10630, #16551, #13009, .T. ) ;
#16892=FACE_OUTER_BOUND ( 'NONE', #10203, .T. ) ;
#16893=CARTESIAN_POINT ( 'NONE',  ( 1.846138399168762101, 9.815003036200520725, -7.646096044339786069 ) ) ;
#16911=EDGE_CURVE ( 'NONE', #12492, #4457, #2545, .T. ) ;
#16912=AXIS2_PLACEMENT_3D ( 'NONE', #1304, #5690, #18692 ) ;
#16914=ORIENTED_EDGE ( 'NONE', *, *, #10426, .F. ) ;
#16915=DIRECTION ( 'NONE',  ( 0.7561779333270775005, 0.6106991889125038542, 0.2350349629540249285 ) ) ;
#16918=VERTEX_POINT ( 'NONE', #2772 ) ;
#16921=CARTESIAN_POINT ( 'NONE',  ( 1.977436885025663837, -15.04044112860237625, 3.321781585408698056 ) ) ;
#16922=LINE ( 'NONE', #871, #4253 ) ;
#16923=( BOUNDED_SURFACE ( )  B_SPLINE_SURFACE ( 3, 1, ( 
 ( #9574, #520 ),
 ( #13876, #17914 ),
 ( #5089, #4996 ),
 ( #4819, #10838 ) ),
 .UNSPECIFIED., .F., .F., .T. ) 
 B_SPLINE_SURFACE_WITH_KNOTS ( ( 4, 4 ),
 ( 2, 2 ),
 ( 0.000000000000000000, 1.000000000000000000 ),
 ( 0.000000000000000000, 1.000000000000000000 ),
 .UNSPECIFIED. ) 
 GEOMETRIC_REPRESENTATION_ITEM ( )  RATIONAL_B_SPLINE_SURFACE ( (
 ( 1.000000000000000000, 1.000000000000000000),
 ( 0.9933953342250436691, 0.8357391271907733676),
 ( 0.9933953342250436691, 0.8357391271907733676),
 ( 1.000000000000000000, 1.000000000000000000) ) ) 
 REPRESENTATION_ITEM ( '' )  SURFACE ( )  );
#16929=CARTESIAN_POINT ( 'NONE',  ( 8.438534575730034959, -3.845978796785994192, -5.688336279099088344 ) ) ;
#16934=CARTESIAN_POINT ( 'NONE',  ( 16.57778382496167424, -0.01466529584256673520, 0.002851818597093359019 ) ) ;
#16938=B_SPLINE_CURVE_WITH_KNOTS ( 'NONE', 3,
 ( #12721, #2396, #18550, #5455, #17208, #8421 ),
 .UNSPECIFIED., .F., .F.,
 ( 4, 2, 4 ),
 ( 4.269227611140977934E-17, 0.0002014099069817279985, 0.0004028198139634133336 ),
 .UNSPECIFIED. ) ;
#16939=ORIENTED_EDGE ( 'NONE', *, *, #17842, .T. ) ;
#16940=EDGE_CURVE ( 'NONE', #12010, #2621, #16250, .T. ) ;
#16941=ORIENTED_EDGE ( 'NONE', *, *, #10701, .T. ) ;
#16943=CARTESIAN_POINT ( 'NONE',  ( 1.861706995891676764, 12.44571539481144384, -0.5394761475746276957 ) ) ;
#16946=CARTESIAN_POINT ( 'NONE',  ( 2.747332970342022840, -2.409922051470567261, -16.17136872824901062 ) ) ;
#16954=CARTESIAN_POINT ( 'NONE',  ( 16.56782317627811096, 0.005492611183758417011, 0.008141063682853501640 ) ) ;
#16958=CARTESIAN_POINT ( 'NONE',  ( 0.3132635586635976188, -4.743936529203153007, -12.89236642382226172 ) ) ;
#16959=CARTESIAN_POINT ( 'NONE',  ( 0.3058872367615230181, 13.24582953854925371, 3.664492643742809364 ) ) ;
#16961=CARTESIAN_POINT ( 'NONE',  ( 0.3058872367615230181, 8.562166468153717958, 10.75034008168919009 ) ) ;
#16963=EDGE_CURVE ( 'NONE', #17568, #16417, #11913, .T. ) ;
#16965=EDGE_CURVE ( 'NONE', #4894, #17234, #5071, .T. ) ;
#16966=ORIENTED_EDGE ( 'NONE', *, *, #9893, .T. ) ;
#16968=VERTEX_POINT ( 'NONE', #1742 ) ;
#16972=B_SPLINE_CURVE_WITH_KNOTS ( 'NONE', 3,
 ( #10160, #15983, #8446, #5653, #2875, #8727 ),
 .UNSPECIFIED., .F., .F.,
 ( 4, 2, 4 ),
 ( 2.168404344971008868E-18, 0.001500839035891550922, 0.003001678071783099675 ),
 .UNSPECIFIED. ) ;
#16978=CARTESIAN_POINT ( 'NONE',  ( 0.3095370825347234511, 12.91933430393608084, 4.681152801286207144 ) ) ;
#16982=ORIENTED_EDGE ( 'NONE', *, *, #3475, .F. ) ;
#16983=ORIENTED_EDGE ( 'NONE', *, *, #3550, .F. ) ;
#16990=CARTESIAN_POINT ( 'NONE',  ( 3.950837973638676281, 1.958075594453990487, -14.41405733518058341 ) ) ;
#16994=CARTESIAN_POINT ( 'NONE',  ( 2.636624412714237309, 15.91454522070173638, -2.161493821596664144 ) ) ;
#16995=AXIS2_PLACEMENT_3D ( 'NONE', #7060, #18700, #8579 ) ;
#16997=CARTESIAN_POINT ( 'NONE',  ( 1.845756295923353330, 0.4783934145702027352, 12.43231724724607190 ) ) ;
#16999=CARTESIAN_POINT ( 'NONE',  ( 2.002547531651519996, -3.242439124566736997, 12.17374746633577232 ) ) ;
#17003=CARTESIAN_POINT ( 'NONE',  ( 0.3137051932979809665, -4.679953077377580151, 12.91601973349268917 ) ) ;
#17007=EDGE_LOOP ( 'NONE', ( #13024, #12884, #9793, #5907 ) ) ;
#17010=ORIENTED_EDGE ( 'NONE', *, *, #7530, .T. ) ;
#17022=EDGE_LOOP ( 'NONE', ( #1316, #18028, #2031, #15936 ) ) ;
#17025=CARTESIAN_POINT ( 'NONE',  ( 1.847461586945730483, 12.44326124954594626, -0.03350899125597195383 ) ) ;
#17026=DIRECTION ( 'NONE',  ( 0.000000000000000000, -1.000000000000000000, 0.000000000000000000 ) ) ;
#17028=EDGE_CURVE ( 'NONE', #9866, #2315, #6141, .T. ) ;
#17033=CARTESIAN_POINT ( 'NONE',  ( 0.8740779401512712710, 11.05257166392075341, -9.070947476926923159 ) ) ;
#17035=CARTESIAN_POINT ( 'NONE',  ( 0.3150686449036049219, -13.11344473514185971, -4.099563462784791668 ) ) ;
#17038=DIRECTION ( 'NONE',  ( 0.000000000000000000, 0.000000000000000000, 1.000000000000000000 ) ) ;
#17039=( BOUNDED_SURFACE ( )  B_SPLINE_SURFACE ( 3, 1, ( 
 ( #18736, #1449 ),
 ( #1162, #11490 ),
 ( #2765, #1347 ),
 ( #13105, #14260 ) ),
 .UNSPECIFIED., .F., .F., .T. ) 
 B_SPLINE_SURFACE_WITH_KNOTS ( ( 4, 4 ),
 ( 2, 2 ),
 ( 0.000000000000000000, 1.000000000000000000 ),
 ( 0.000000000000000000, 1.000000000000000000 ),
 .UNSPECIFIED. ) 
 GEOMETRIC_REPRESENTATION_ITEM ( )  RATIONAL_B_SPLINE_SURFACE ( (
 ( 1.000000000000000000, 1.000000000000000000),
 ( 0.9933953342250436691, 0.8357391271907733676),
 ( 0.9933953342250436691, 0.8357391271907733676),
 ( 1.000000000000000000, 1.000000000000000000) ) ) 
 REPRESENTATION_ITEM ( '' )  SURFACE ( )  );
#17041=CARTESIAN_POINT ( 'NONE',  ( 0.3939822652208148646, -4.930560016699156556, 12.90851734139305229 ) ) ;
#17042=CARTESIAN_POINT ( 'NONE',  ( 0.3308579732647018989, 11.46737410776364996, -7.595989242675004860 ) ) ;
#17043=DIRECTION ( 'NONE',  ( 0.000000000000000000, 0.000000000000000000, -1.000000000000000000 ) ) ;
#17048=ADVANCED_FACE ( 'NONE', ( #10535 ), #16372, .F. ) ;
#17049=CARTESIAN_POINT ( 'NONE',  ( 0.000000000000000000, 0.000000000000000000, 0.000000000000000000 ) ) ;
#17050=CARTESIAN_POINT ( 'NONE',  ( 2.705023505549867924, -0.8488853074252048492, -13.27418276223637150 ) ) ;
#17054=CARTESIAN_POINT ( 'NONE',  ( 1.845756295923353996, 6.920504327368345976, -10.33914852636097592 ) ) ;
#17058=ORIENTED_EDGE ( 'NONE', *, *, #1206, .T. ) ;
#17059=CARTESIAN_POINT ( 'NONE',  ( 1.847426409206450959, 1.966388007708274189E-11, -12.44303504652081038 ) ) ;
#17067=FACE_OUTER_BOUND ( 'NONE', #2227, .T. ) ;
#17069=CARTESIAN_POINT ( 'NONE',  ( 0.3150686449036029790, -0.1533607327084788585, -13.73846184595214481 ) ) ;
#17070=CARTESIAN_POINT ( 'NONE',  ( 1.846138399168762989, 11.69739621335922308, 4.238866729160444713 ) ) ;
#17073=ORIENTED_EDGE ( 'NONE', *, *, #17461, .T. ) ;
#17074=B_SPLINE_CURVE_WITH_KNOTS ( 'NONE', 3,
 ( #2317, #13978, #886, #8072, #9843, #14157 ),
 .UNSPECIFIED., .F., .F.,
 ( 4, 2, 4 ),
 ( 3.499941646806256644E-17, 0.0001825746017570586152, 0.0003651492035140799881 ),
 .UNSPECIFIED. ) ;
#17081=CARTESIAN_POINT ( 'NONE',  ( 1.845756295923356438, -11.67600463554276224, 4.296776483139434610 ) ) ;
#17083=CARTESIAN_POINT ( 'NONE',  ( 1.847412631396503357, -7.348689888531914072, 10.04119192206683664 ) ) ;
#17088=CARTESIAN_POINT ( 'NONE',  ( 0.3132642857406528480, 13.72733058964895037, 0.5276792104582755938 ) ) ;
#17089=CARTESIAN_POINT ( 'NONE',  ( 0.4862570985993252548, 13.44146924561381162, 3.580942890621718888 ) ) ;
#17090=CARTESIAN_POINT ( 'NONE',  ( 1.861628059977343597, -10.38573835516717381, 6.879051339207257421 ) ) ;
#17091=FACE_OUTER_BOUND ( 'NONE', #5735, .T. ) ;
#17092=CARTESIAN_POINT ( 'NONE',  ( 2.353870697619111052, 4.720869121224300358, -12.05847592522638934 ) ) ;
#17097=CARTESIAN_POINT ( 'NONE',  ( 1.342453679581834924, 14.34050741580207067, 3.649820028552781093 ) ) ;
#17099=EDGE_CURVE ( 'NONE', #11392, #5432, #2745, .T. ) ;
#17101=CARTESIAN_POINT ( 'NONE',  ( 2.697797270744669351, 3.226410068829429711, 12.89731672021091846 ) ) ;
#17107=CARTESIAN_POINT ( 'NONE',  ( 2.002547531651519996, 3.242439124566821818, -12.17374746633574745 ) ) ;
#17108=CARTESIAN_POINT ( 'NONE',  ( 0.3939822652208129217, -13.80035637018650974, -0.7002900021919380436 ) ) ;
#17110=( BOUNDED_SURFACE ( )  B_SPLINE_SURFACE ( 3, 1, ( 
 ( #8073, #3663 ),
 ( #18102, #7898 ),
 ( #13882, #9579 ),
 ( #12540, #13708 ) ),
 .UNSPECIFIED., .F., .F., .T. ) 
 B_SPLINE_SURFACE_WITH_KNOTS ( ( 4, 4 ),
 ( 2, 2 ),
 ( 0.000000000000000000, 1.000000000000000000 ),
 ( 0.000000000000000000, 1.000000000000000000 ),
 .UNSPECIFIED. ) 
 GEOMETRIC_REPRESENTATION_ITEM ( )  RATIONAL_B_SPLINE_SURFACE ( (
 ( 1.000000000000000000, 1.000000000000000000),
 ( 0.9933953342250438912, 0.8357391271907739227),
 ( 0.9933953342250438912, 0.8357391271907739227),
 ( 1.000000000000000000, 1.000000000000000000) ) ) 
 REPRESENTATION_ITEM ( '' )  SURFACE ( )  );
#17122=ORIENTED_EDGE ( 'NONE', *, *, #13531, .F. ) ;
#17127=CARTESIAN_POINT ( 'NONE',  ( 1.847247051441587518, -9.967131402978145260, -7.448813758297282206 ) ) ;
#17130=ORIENTED_EDGE ( 'NONE', *, *, #8833, .T. ) ;
#17141=EDGE_LOOP ( 'NONE', ( #5253, #16233, #4511, #7217 ) ) ;
#17144=ORIENTED_EDGE ( 'NONE', *, *, #10921, .T. ) ;
#17150=CARTESIAN_POINT ( 'NONE',  ( 0.4754618798421162973, -10.80499583390506224, -8.775436892861234739 ) ) ;
#17154=CARTESIAN_POINT ( 'NONE',  ( 16.57210152137263393, -0.01453130299868521901, -0.0006600038696347544425 ) ) ;
#17156=LINE ( 'NONE', #14199, #6222 ) ;
#17159=ORIENTED_EDGE ( 'NONE', *, *, #2351, .T. ) ;
#17163=EDGE_CURVE ( 'NONE', #6853, #10307, #16922, .T. ) ;
#17169=ORIENTED_EDGE ( 'NONE', *, *, #5905, .T. ) ;
#17172=LINE ( 'NONE', #4084, #18302 ) ;
#17173=CARTESIAN_POINT ( 'NONE',  ( 0.4862570985993235340, -13.44146924561378498, -3.580942890621813923 ) ) ;
#17174=AXIS2_PLACEMENT_3D ( 'NONE', #6478, #16703, #12303 ) ;
#17177=CARTESIAN_POINT ( 'NONE',  ( 0.3939822652208163078, 4.930560016699244485, -12.90851734139301499 ) ) ;
#17182=CARTESIAN_POINT ( 'NONE',  ( 2.123976203522053741, 15.26039569100260174, 3.347755036805956763 ) ) ;
#17183=ORIENTED_EDGE ( 'NONE', *, *, #17240, .T. ) ;
#17185=CARTESIAN_POINT ( 'NONE',  ( 0.3720661004400040439, -10.73619472937708252, 8.694226082900557984 ) ) ;
#17187=VECTOR ( 'NONE', #16474, 1000.000000000000000 ) ;
#17190=ORIENTED_EDGE ( 'NONE', *, *, #15086, .T. ) ;
#17194=FACE_OUTER_BOUND ( 'NONE', #16136, .T. ) ;
#17195=CARTESIAN_POINT ( 'NONE',  ( 3.512766787570690497, 2.682019731918607430, -14.81029789862162893 ) ) ;
#17197=CARTESIAN_POINT ( 'NONE',  ( 1.861628059977344041, 0.5393144007391995620, -12.44564375541076551 ) ) ;
#17202=( LENGTH_UNIT ( ) NAMED_UNIT ( * ) SI_UNIT ( .MILLI., .METRE. ) );
#17203=CARTESIAN_POINT ( 'NONE',  ( 0.000000000000000000, 6.123233995736766282E-16, -5.000000000000000000 ) ) ;
#17204=VECTOR ( 'NONE', #8032, 1000.000000000000114 ) ;
#17208=CARTESIAN_POINT ( 'NONE',  ( 0.3132642857406495174, 0.5276792104584192566, -13.72733058964894681 ) ) ;
#17209=CARTESIAN_POINT ( 'NONE',  ( 1.254009781011619751, -13.61532727684435251, 5.487405433548490308 ) ) ;
#17212=CARTESIAN_POINT ( 'NONE',  ( 0.3151928479966097374, 0.000000000000000000, -13.73922861026898623 ) ) ;
#17214=CARTESIAN_POINT ( 'NONE',  ( 16.56679352167444819, -0.009190982326619729845, -0.001390132774594407148 ) ) ;
#17231=LINE ( 'NONE', #14364, #543 ) ;
#17234=VERTEX_POINT ( 'NONE', #12987 ) ;
#17236=VERTEX_POINT ( 'NONE', #17388 ) ;
#17239=CARTESIAN_POINT ( 'NONE',  ( 0.3148213771069364175, -0.2297580318215671491, 13.73693585713734144 ) ) ;
#17240=EDGE_CURVE ( 'NONE', #8960, #5922, #14607, .T. ) ;
#17243=CARTESIAN_POINT ( 'NONE',  ( 3.950837973638675393, 2.591948120961804936, 14.31366178983254578 ) ) ;
#17244=CARTESIAN_POINT ( 'NONE',  ( 0.3151930723728407768, 13.09040889075576608, -4.172946285306434078 ) ) ;
#17249=DIRECTION ( 'NONE',  ( 1.000000000000000000, 0.000000000000000000, 0.000000000000000000 ) ) ;
#17254=ORIENTED_EDGE ( 'NONE', *, *, #13769, .T. ) ;
#17256=ORIENTED_EDGE ( 'NONE', *, *, #16341, .T. ) ;
#17257=ORIENTED_EDGE ( 'NONE', *, *, #2128, .T. ) ;
#17261=CARTESIAN_POINT ( 'NONE',  ( 0.3148208552358927603, 7.888357771040864996, -11.24855514421867042 ) ) ;
#17270=CONICAL_SURFACE ( 'NONE', #12397, 12.15840553252917289, 0.7853981625000049371 ) ;
#17272=LINE ( 'NONE', #12784, #18259 ) ;
#17275=VERTEX_POINT ( 'NONE', #2474 ) ;
#17279=CARTESIAN_POINT ( 'NONE',  ( 2.123976203522053297, 6.261444813538757259, -14.31368049382962937 ) ) ;
#17282=DIRECTION ( 'NONE',  ( 1.000000000000000000, 0.000000000000000000, 0.000000000000000000 ) ) ;
#17286=CARTESIAN_POINT ( 'NONE',  ( 0.4754618798421167414, -8.775436892861188554, 10.80499583390510132 ) ) ;
#17295=EDGE_CURVE ( 'NONE', #16918, #6853, #7559, .T. ) ;
#17304=CARTESIAN_POINT ( 'NONE',  ( 2.636624412715435462, -15.80357026013316712, -2.862162146983298516 ) ) ;
#17309=CARTESIAN_POINT ( 'NONE',  ( 0.4862570985993235340, 0.7479633556562450547, 13.89016912371017831 ) ) ;
#17310=EDGE_CURVE ( 'NONE', #11392, #17458, #929, .T. ) ;
#17311=VERTEX_POINT ( 'NONE', #6119 ) ;
#17321=CARTESIAN_POINT ( 'NONE',  ( 0.3720661004400037664, 13.34435358167257313, -3.575426119359045529 ) ) ;
#17330=( NAMED_UNIT ( * ) SI_UNIT ( $, .STERADIAN. ) SOLID_ANGLE_UNIT ( ) );
#17331=ORIENTED_EDGE ( 'NONE', *, *, #17714, .T. ) ;
#17333=CARTESIAN_POINT ( 'NONE',  ( 1.847372867223026294, -0.1054171785007356615, 12.44269075185938789 ) ) ;
#17334=ORIENTED_EDGE ( 'NONE', *, *, #1458, .F. ) ;
#17335=CARTESIAN_POINT ( 'NONE',  ( 16.56782317627811096, 0.002708056627498641941, 0.009439921864426896805 ) ) ;
#17341=CARTESIAN_POINT ( 'NONE',  ( 1.845756295923353996, 9.776763338604718356, -7.694561132136850112 ) ) ;
#17345=CARTESIAN_POINT ( 'NONE',  ( 0.3151928476913565258, -13.06671852871092199, 4.245853234426333778 ) ) ;
#17350=EDGE_LOOP ( 'NONE', ( #2997, #3634, #12447, #1976 ) ) ;
#17353=ORIENTED_EDGE ( 'NONE', *, *, #2348, .F. ) ;
#17356=CARTESIAN_POINT ( 'NONE',  ( 0.3095370825347224519, 8.444334731364007141, 10.84046130709061373 ) ) ;
#17361=CARTESIAN_POINT ( 'NONE',  ( 0.3137051932979775248, 0.4596302728639756197, 13.73004976592202198 ) ) ;
#17367=CARTESIAN_POINT ( 'NONE',  ( 1.847412631396506244, 3.804043368582664009, 11.84727953344284579 ) ) ;
#17369=B_SPLINE_CURVE_WITH_KNOTS ( 'NONE', 3,
 ( #10704, #3526, #12317, #9361 ),
 .UNSPECIFIED., .F., .F.,
 ( 4, 4 ),
 ( 0.000000000000000000, 0.002004993803841771411 ),
 .UNSPECIFIED. ) ;
#17378=ADVANCED_FACE ( 'NONE', ( #10617 ), #12195, .F. ) ;
#17379=ORIENTED_EDGE ( 'NONE', *, *, #6121, .F. ) ;
#17388=CARTESIAN_POINT ( 'NONE',  ( 0.4862570985993252548, 12.97920246947879441, 5.003653737315533867 ) ) ;
#17394=CARTESIAN_POINT ( 'NONE',  ( 1.847372867223025183, 7.398914411685134418, -10.00438561114516034 ) ) ;
#17400=ORIENTED_EDGE ( 'NONE', *, *, #8833, .F. ) ;
#17407=CARTESIAN_POINT ( 'NONE',  ( 0.3095370825347224519, -4.681152801286251552, 12.91933430393606486 ) ) ;
#17410=EDGE_CURVE ( 'NONE', #16292, #17234, #1023, .T. ) ;
#17412=CARTESIAN_POINT ( 'NONE',  ( 1.846524061778019199, -9.853584647934329865, -7.597197846158187495 ) ) ;
#17415=B_SPLINE_CURVE_WITH_KNOTS ( 'NONE', 3,
 ( #7588, #13584, #4608, #10726, #4984, #9191 ),
 .UNSPECIFIED., .F., .F.,
 ( 4, 2, 4 ),
 ( 4.027530160694267299E-17, 0.0002014099069817290827, 0.0004028198139634178872 ),
 .UNSPECIFIED. ) ;
#17418=FACE_OUTER_BOUND ( 'NONE', #4555, .T. ) ;
#17419=CARTESIAN_POINT ( 'NONE',  ( 2.123976203522053297, 10.37815841598508371, -11.67822624909914175 ) ) ;
#17420=CARTESIAN_POINT ( 'NONE',  ( 0.3095370825347233956, -4.681152801286073917, -12.91933430393612525 ) ) ;
#17421=CARTESIAN_POINT ( 'NONE',  ( 2.747332970342022840, 11.66639548242807578, 11.45495994260722306 ) ) ;
#17425=CARTESIAN_POINT ( 'NONE',  ( 16.56753206892534891, 0.006760771273035115839, -0.006669401563385219701 ) ) ;
#17427=B_SPLINE_CURVE_WITH_KNOTS ( 'NONE', 3,
 ( #11923, #4664, #10492, #3207, #1797, #12391 ),
 .UNSPECIFIED., .F., .F.,
 ( 4, 2, 4 ),
 ( 3.361796080452501619E-17, 0.0001825746017570592115, 0.0003651492035140848128 ),
 .UNSPECIFIED. ) ;
#17429=ORIENTED_EDGE ( 'NONE', *, *, #5186, .T. ) ;
#17433=CARTESIAN_POINT ( 'NONE',  ( 2.636624412715137922, -7.605649742761668719, 14.14563173255331741 ) ) ;
#17435=EDGE_CURVE ( 'NONE', #14697, #4455, #17172, .T. ) ;
#17438=CARTESIAN_POINT ( 'NONE',  ( 0.3939875929385642239, 13.34133634968955917, 3.598491969338272867 ) ) ;
#17442=CARTESIAN_POINT ( 'NONE',  ( 0.3148213771069373057, -8.260246460850796169, 10.97836617636221845 ) ) ;
#17443=CARTESIAN_POINT ( 'NONE',  ( 2.002547531651519996, -4.532360870844247991, -11.75462648437106417 ) ) ;
#17447=CARTESIAN_POINT ( 'NONE',  ( 16.57210152137263393, 0.005118120558001383255, -0.01361613799508856922 ) ) ;
#17453=ORIENTED_EDGE ( 'NONE', *, *, #11050, .T. ) ;
#17456=CARTESIAN_POINT ( 'NONE',  ( 2.002547531651519996, -0.6781519942170860515, -12.57989064830760206 ) ) ;
#17457=CARTESIAN_POINT ( 'NONE',  ( 0.3142011359265349801, 7.762194356530932815, -11.33549115679415031 ) ) ;
#17458=VERTEX_POINT ( 'NONE', #265 ) ;
#17461=EDGE_CURVE ( 'NONE', #5518, #15560, #1866, .T. ) ;
#17465=VECTOR ( 'NONE', #5925, 1000.000000000000114 ) ;
#17466=B_SPLINE_CURVE_WITH_KNOTS ( 'NONE', 3,
 ( #9343, #9436, #11059, #18310, #16606, #3504 ),
 .UNSPECIFIED., .F., .F.,
 ( 4, 2, 4 ),
 ( 0.000000000000000000, 0.0001828790815886945087, 0.0003657581631773890174 ),
 .UNSPECIFIED. ) ;
#17469=DIRECTION ( 'NONE',  ( 0.000000000000000000, 0.000000000000000000, 1.000000000000000000 ) ) ;
#17470=CARTESIAN_POINT ( 'NONE',  ( 0.3142011359265305392, 3.879426116491875742, -13.17934269988453977 ) ) ;
#17479=DIRECTION ( 'NONE',  ( -1.000000000000000000, -0.000000000000000000, -0.000000000000000000 ) ) ;
#17482=CARTESIAN_POINT ( 'NONE',  ( 1.918921323896324971, 0.6349083173281891979, -12.49850046818173688 ) ) ;
#17483=CARTESIAN_POINT ( 'NONE',  ( 0.3150686449036048664, -4.391272911157235725, -13.01866258978841628 ) ) ;
#17486=CARTESIAN_POINT ( 'NONE',  ( 1.846613052777652975, 11.93415846513961753, 3.520031056876344433 ) ) ;
#17487=CARTESIAN_POINT ( 'NONE',  ( 2.353870697619111496, -12.92712089195302561, -0.7635393531607687079 ) ) ;
#17489=ORIENTED_EDGE ( 'NONE', *, *, #10814, .T. ) ;
#17498=( BOUNDED_SURFACE ( )  B_SPLINE_SURFACE ( 3, 1, ( 
 ( #11409, #4141 ),
 ( #16954, #9856 ),
 ( #15513, #8267 ),
 ( #901, #3765 ) ),
 .UNSPECIFIED., .F., .F., .T. ) 
 B_SPLINE_SURFACE_WITH_KNOTS ( ( 4, 4 ),
 ( 2, 2 ),
 ( 0.000000000000000000, 1.000000000000000000 ),
 ( 0.000000000000000000, 1.000000000000000000 ),
 .UNSPECIFIED. ) 
 GEOMETRIC_REPRESENTATION_ITEM ( )  RATIONAL_B_SPLINE_SURFACE ( (
 ( 1.000000000000000000, 1.000000000000000000),
 ( 0.9933953342250436691, 0.8357391271907733676),
 ( 0.9933953342250436691, 0.8357391271907733676),
 ( 1.000000000000000000, 1.000000000000000000) ) ) 
 REPRESENTATION_ITEM ( '' )  SURFACE ( )  );
#17503=ORIENTED_EDGE ( 'NONE', *, *, #5487, .F. ) ;
#17504=CARTESIAN_POINT ( 'NONE',  ( 16.56753206892534891, -0.008490833999798956880, -0.004253784598196145433 ) ) ;
#17505=CARTESIAN_POINT ( 'NONE',  ( 1.846138399168762101, 3.446241763653166590, -11.95493567637846866 ) ) ;
#17511=CARTESIAN_POINT ( 'NONE',  ( 0.3307726912345181902, 10.76786801061219734, -8.558645027434160113 ) ) ;
#17513=DIRECTION ( 'NONE',  ( 0.000000000000000000, 0.000000000000000000, 1.000000000000000000 ) ) ;
#17514=CARTESIAN_POINT ( 'NONE',  ( 2.002547531651519996, -6.845637710436110801, -10.57595306287299763 ) ) ;
#17518=CARTESIAN_POINT ( 'NONE',  ( 16.56679352167444819, 0.009190982326619362083, -0.001390132774595485713 ) ) ;
#17519=ORIENTED_EDGE ( 'NONE', *, *, #4635, .F. ) ;
#17527=CARTESIAN_POINT ( 'NONE',  ( 16.58200780006414732, 0.01115192838421469497, -0.0006320991582341122352 ) ) ;
#17529=CARTESIAN_POINT ( 'NONE',  ( 0.3939822652208126996, -8.678192463540247203, 10.75310269629518700 ) ) ;
#17532=( BOUNDED_SURFACE ( )  B_SPLINE_SURFACE ( 3, 1, ( 
 ( #14740, #5847 ),
 ( #17518, #4425 ),
 ( #10259, #14648 ),
 ( #13212, #127 ) ),
 .UNSPECIFIED., .F., .F., .T. ) 
 B_SPLINE_SURFACE_WITH_KNOTS ( ( 4, 4 ),
 ( 2, 2 ),
 ( 0.000000000000000000, 1.000000000000000000 ),
 ( 0.000000000000000000, 1.000000000000000000 ),
 .UNSPECIFIED. ) 
 GEOMETRIC_REPRESENTATION_ITEM ( )  RATIONAL_B_SPLINE_SURFACE ( (
 ( 1.000000000000000000, 1.000000000000000000),
 ( 0.9593108457356467333, 0.9995965569486454649),
 ( 0.9593108457356467333, 0.9995965569486454649),
 ( 1.000000000000000000, 1.000000000000000000) ) ) 
 REPRESENTATION_ITEM ( '' )  SURFACE ( )  );
#17534=( BOUNDED_SURFACE ( )  B_SPLINE_SURFACE ( 3, 1, ( 
 ( #4346, #5764 ),
 ( #6940, #11609 ),
 ( #10171, #11245 ),
 ( #11333, #17150 ) ),
 .UNSPECIFIED., .F., .F., .T. ) 
 B_SPLINE_SURFACE_WITH_KNOTS ( ( 4, 4 ),
 ( 2, 2 ),
 ( 0.000000000000000000, 1.000000000000000000 ),
 ( 0.000000000000000000, 1.000000000000000000 ),
 .UNSPECIFIED. ) 
 GEOMETRIC_REPRESENTATION_ITEM ( )  RATIONAL_B_SPLINE_SURFACE ( (
 ( 1.000000000000000000, 1.000000000000000000),
 ( 0.9933953342250436691, 0.8357391271907733676),
 ( 0.9933953342250436691, 0.8357391271907733676),
 ( 1.000000000000000000, 1.000000000000000000) ) ) 
 REPRESENTATION_ITEM ( '' )  SURFACE ( )  );
#17543=ORIENTED_EDGE ( 'NONE', *, *, #2290, .F. ) ;
#17544=EDGE_CURVE ( 'NONE', #3029, #8074, #6306, .T. ) ;
#17547=ORIENTED_EDGE ( 'NONE', *, *, #14599, .F. ) ;
#17548=VERTEX_POINT ( 'NONE', #17665 ) ;
#17558=CARTESIAN_POINT ( 'NONE',  ( 1.846138399168762101, -11.95493567637852905, 3.446241763652952539 ) ) ;
#17559=CARTESIAN_POINT ( 'NONE',  ( 0.8740764193768836288, 9.070946295054209685, -11.05257066464527327 ) ) ;
#17561=FACE_OUTER_BOUND ( 'NONE', #17007, .T. ) ;
#17563=CARTESIAN_POINT ( 'NONE',  ( 0.4862570985993235340, 8.769551628660735787, 10.79774104611376373 ) ) ;
#17568=VERTEX_POINT ( 'NONE', #18888 ) ;
#17574=ORIENTED_EDGE ( 'NONE', *, *, #272, .F. ) ;
#17576=CARTESIAN_POINT ( 'NONE',  ( 0.8740764193767813772, -12.04241474977994208, 7.708542792189371440 ) ) ;
#17578=CARTESIAN_POINT ( 'NONE',  ( 1.861706995891670546, -12.00328602385077659, -3.332865258614104320 ) ) ;
#17579=ORIENTED_EDGE ( 'NONE', *, *, #9378, .F. ) ;
#17581=ADVANCED_FACE ( 'NONE', ( #1505 ), #3106, .F. ) ;
#17585=B_SPLINE_CURVE_WITH_KNOTS ( 'NONE', 3,
 ( #812, #6551, #10760, #9320, #15050, #4926 ),
 .UNSPECIFIED., .F., .F.,
 ( 4, 2, 4 ),
 ( 3.556447555475521540E-17, 0.0001825746017570587236, 0.0003651492035140818855 ),
 .UNSPECIFIED. ) ;
#17587=CARTESIAN_POINT ( 'NONE',  ( 3.950837973638677170, 10.51028938476232355, -10.05648675950114956 ) ) ;
#17591=EDGE_CURVE ( 'NONE', #7061, #13310, #17466, .T. ) ;
#17592=CARTESIAN_POINT ( 'NONE',  ( 1.846524061778019199, 7.597197846158221246, -9.853584647934303220 ) ) ;
#17595=DIRECTION ( 'NONE',  ( 1.000000000000000000, 0.000000000000000000, 0.000000000000000000 ) ) ;
#17597=EDGE_CURVE ( 'NONE', #10307, #1375, #18148, .T. ) ;
#17604=ORIENTED_EDGE ( 'NONE', *, *, #18161, .T. ) ;
#17606=CARTESIAN_POINT ( 'NONE',  ( 16.58200780006414732, 0.004047297414159048250, -0.01041078477704050417 ) ) ;
#17607=CIRCLE ( 'NONE', #18221, 14.54644660717763927 ) ;
#17613=CARTESIAN_POINT ( 'NONE',  ( 16.56822296793089322, -0.005339139727952723832, 0.008619100080559757848 ) ) ;
#17618=DIRECTION ( 'NONE',  ( -1.000000000000000000, -0.000000000000000000, -0.000000000000000000 ) ) ;
#17621=CARTESIAN_POINT ( 'NONE',  ( 3.950837973638668288, 0.000000000000000000, 0.000000000000000000 ) ) ;
#17622=CARTESIAN_POINT ( 'NONE',  ( 0.3307726912345216319, -13.74203354050372283, 0.5948952607472158816 ) ) ;
#17627=ORIENTED_EDGE ( 'NONE', *, *, #5811, .F. ) ;
#17629=ORIENTED_EDGE ( 'NONE', *, *, #1459, .T. ) ;
#17636=UNCERTAINTY_MEASURE_WITH_UNIT (LENGTH_MEASURE( 1.000000000000000082E-05 ), #9937, 'distance_accuracy_value', 'NONE');
#17637=EDGE_CURVE ( 'NONE', #9622, #11775, #14714, .T. ) ;
#17640=B_SPLINE_CURVE_WITH_KNOTS ( 'NONE', 3,
 ( #15819, #5491, #1099, #8557, #11251, #6950, #17345, #2800, #8648, #12573, #14475, #1388, #3974 ),
 .UNSPECIFIED., .F., .F.,
 ( 4, 3, 3, 3, 4 ),
 ( 2.168404344971008868E-18, 0.0002299780670421057124, 0.0004599561239687910961, 0.0006896788984287892561, 0.0009194956271626406052 ),
 .UNSPECIFIED. ) ;
#17643=CARTESIAN_POINT ( 'NONE',  ( 0.4862570985993235340, 7.559321496869426227, 11.67702470553367711 ) ) ;
#17645=CARTESIAN_POINT ( 'NONE',  ( 8.522092701127531811, 5.397361180353144050, 4.388629235579598387 ) ) ;
#17647=ORIENTED_EDGE ( 'NONE', *, *, #18010, .F. ) ;
#17648=AXIS2_PLACEMENT_3D ( 'NONE', #5939, #7204, #10442 ) ;
#17654=( BOUNDED_SURFACE ( )  B_SPLINE_SURFACE ( 3, 1, ( 
 ( #3486, #16685 ),
 ( #2070, #12199 ),
 ( #5113, #7910 ),
 ( #6652, #13623 ) ),
 .UNSPECIFIED., .F., .F., .T. ) 
 B_SPLINE_SURFACE_WITH_KNOTS ( ( 4, 4 ),
 ( 2, 2 ),
 ( 0.000000000000000000, 1.000000000000000000 ),
 ( 0.000000000000000000, 1.000000000000000000 ),
 .UNSPECIFIED. ) 
 GEOMETRIC_REPRESENTATION_ITEM ( )  RATIONAL_B_SPLINE_SURFACE ( (
 ( 1.000000000000000000, 1.000000000000000000),
 ( 0.9933953342250438912, 0.8357391271907739227),
 ( 0.9933953342250438912, 0.8357391271907739227),
 ( 1.000000000000000000, 1.000000000000000000) ) ) 
 REPRESENTATION_ITEM ( '' )  SURFACE ( )  );
#17655=( BOUNDED_SURFACE ( )  B_SPLINE_SURFACE ( 3, 1, ( 
 ( #9536, #12497 ),
 ( #12231, #6773 ),
 ( #9453, #3797 ),
 ( #18147, #12582 ) ),
 .UNSPECIFIED., .F., .F., .T. ) 
 B_SPLINE_SURFACE_WITH_KNOTS ( ( 4, 4 ),
 ( 2, 2 ),
 ( 0.000000000000000000, 1.000000000000000000 ),
 ( 0.000000000000000000, 1.000000000000000000 ),
 .UNSPECIFIED. ) 
 GEOMETRIC_REPRESENTATION_ITEM ( )  RATIONAL_B_SPLINE_SURFACE ( (
 ( 1.000000000000000000, 1.000000000000000000),
 ( 0.7792777138730158093, 0.9689936506012928330),
 ( 0.7792777138730158093, 0.9689936506012928330),
 ( 1.000000000000000000, 1.000000000000000000) ) ) 
 REPRESENTATION_ITEM ( '' )  SURFACE ( )  );
#17660=CARTESIAN_POINT ( 'NONE',  ( 8.438534575730034959, 1.899950616255187352, 6.598402093327886853 ) ) ;
#17665=CARTESIAN_POINT ( 'NONE',  ( 2.002547531651519996, 0.6781519942171739812, 12.57989064830759851 ) ) ;
#17667=CARTESIAN_POINT ( 'NONE',  ( 0.3151928476913540278, 8.075884471919755114, 11.11514699826553176 ) ) ;
#17668=B_SPLINE_CURVE_WITH_KNOTS ( 'NONE', 3,
 ( #9420, #17936, #719, #16499, #3387, #633 ),
 .UNSPECIFIED., .F., .F.,
 ( 4, 2, 4 ),
 ( 2.790109556687801444E-18, 0.0002017457492448089095, 0.0004034914984896150001 ),
 .UNSPECIFIED. ) ;
#17671=B_SPLINE_CURVE_WITH_KNOTS ( 'NONE', 3,
 ( #2681, #7196, #1547, #8808 ),
 .UNSPECIFIED., .F., .F.,
 ( 4, 4 ),
 ( 5.784724088816010014E-17, 0.002004993803842651783 ),
 .UNSPECIFIED. ) ;
#17672=CARTESIAN_POINT ( 'NONE',  ( 0.3150686449036074754, -11.20479228691391604, -7.951193823202520328 ) ) ;
#17674=ORIENTED_EDGE ( 'NONE', *, *, #14106, .F. ) ;
#17675=EDGE_CURVE ( 'NONE', #17983, #11605, #12651, .T. ) ;
#17690=ADVANCED_FACE ( 'NONE', ( #7924 ), #3861, .F. ) ;
#17694=CARTESIAN_POINT ( 'NONE',  ( 0.3095370825347224519, 10.84046130709070788, -8.444334731363888125 ) ) ;
#17698=CARTESIAN_POINT ( 'NONE',  ( 3.950837973638676281, -6.888253895133199300, -12.81214529934982949 ) ) ;
#17700=CARTESIAN_POINT ( 'NONE',  ( 0.3151928476913555821, 0.0002082997483780314805, 13.73922860838472104 ) ) ;
#17701=ORIENTED_EDGE ( 'NONE', *, *, #7282, .F. ) ;
#17706=ORIENTED_EDGE ( 'NONE', *, *, #3713, .F. ) ;
#17714=EDGE_CURVE ( 'NONE', #1370, #6249, #7031, .T. ) ;
#17716=CARTESIAN_POINT ( 'NONE',  ( 16.56753206892534891, -0.006669401563384967299, 0.006760771273036151469 ) ) ;
#17718=CARTESIAN_POINT ( 'NONE',  ( 0.4754618798421162973, -5.007009103465161814, -12.98792082933649539 ) ) ;
#17719=CARTESIAN_POINT ( 'NONE',  ( 3.950837973638677170, 12.81214529934985080, -6.888253895133152227 ) ) ;
#17745=CARTESIAN_POINT ( 'NONE',  ( 0.3720661004400037664, -0.7231997263365766981, 13.79610186261029448 ) ) ;
#17751=CARTESIAN_POINT ( 'NONE',  ( 2.353870697619110164, -3.268530966681543859, -12.53036919722787879 ) ) ;
#17761=CARTESIAN_POINT ( 'NONE',  ( 2.636624412714236865, 0.000000000000000000, 0.000000000000000000 ) ) ;
#17763=CARTESIAN_POINT ( 'NONE',  ( 0.3148213771069329203, -10.97836617636219181, -8.260246460850838801 ) ) ;
#17765=CARTESIAN_POINT ( 'NONE',  ( 0.3150692679895985560, 4.391039771493846722, -13.01874238516605331 ) ) ;
#17772=CARTESIAN_POINT ( 'NONE',  ( 2.636624412714236865, 0.000000000000000000, 0.000000000000000000 ) ) ;
#17777=AXIS2_PLACEMENT_3D ( 'NONE', #1520, #14509, #16238 ) ;
#17780=CARTESIAN_POINT ( 'NONE',  ( 1.847168016377981781, -3.666915430942684129, 11.89018175117593934 ) ) ;
#17784=CARTESIAN_POINT ( 'NONE',  ( 1.254255976357135038, 3.563435620217683120, 14.24071337840730322 ) ) ;
#17791=DIRECTION ( 'NONE',  ( 0.000000000000000000, 0.000000000000000000, 1.000000000000000000 ) ) ;
#17793=EDGE_CURVE ( 'NONE', #6897, #16688, #12661, .T. ) ;
#17797=CARTESIAN_POINT ( 'NONE',  ( 16.56872352241294521, -0.007240717549633941472, -0.007512283835804289302 ) ) ;
#17805=DIRECTION ( 'NONE',  ( -0.7561779333270775005, -0.6322161072786931513, -0.1688126975276622865 ) ) ;
#17808=CONICAL_SURFACE ( 'NONE', #17174, 14.54644660717763927, 0.8559913436420816257 ) ;
#17812=CARTESIAN_POINT ( 'NONE',  ( 0.4862570985993252548, 11.67702470553365401, 7.559321496869467971 ) ) ;
#17817=ORIENTED_EDGE ( 'NONE', *, *, #12794, .F. ) ;
#17821=ORIENTED_EDGE ( 'NONE', *, *, #3677, .T. ) ;
#17835=CARTESIAN_POINT ( 'NONE',  ( 0.4754618798421167414, -12.98792082933641012, -5.007009103465385635 ) ) ;
#17838=FACE_OUTER_BOUND ( 'NONE', #2655, .T. ) ;
#17841=ORIENTED_EDGE ( 'NONE', *, *, #17028, .T. ) ;
#17842=EDGE_CURVE ( 'NONE', #12032, #16368, #14045, .T. ) ;
#17845=CARTESIAN_POINT ( 'NONE',  ( 3.664313757352975376, -2.831308606787148463, -13.97913389346637025 ) ) ;
#17846=DIRECTION ( 'NONE',  ( 1.000000000000000000, 0.000000000000000000, 0.000000000000000000 ) ) ;
#17848=( BOUNDED_SURFACE ( )  B_SPLINE_SURFACE ( 3, 1, ( 
 ( #14457, #12745 ),
 ( #1467, #7213 ),
 ( #1183, #15893 ),
 ( #17425, #18574 ) ),
 .UNSPECIFIED., .F., .F., .T. ) 
 B_SPLINE_SURFACE_WITH_KNOTS ( ( 4, 4 ),
 ( 2, 2 ),
 ( 0.000000000000000000, 1.000000000000000000 ),
 ( 0.000000000000000000, 1.000000000000000000 ),
 .UNSPECIFIED. ) 
 GEOMETRIC_REPRESENTATION_ITEM ( )  RATIONAL_B_SPLINE_SURFACE ( (
 ( 1.000000000000000000, 1.000000000000000000),
 ( 0.9933953342250438912, 0.8357391271907739227),
 ( 0.9933953342250438912, 0.8357391271907739227),
 ( 1.000000000000000000, 1.000000000000000000) ) ) 
 REPRESENTATION_ITEM ( '' )  SURFACE ( )  );
#17851=CARTESIAN_POINT ( 'NONE',  ( 1.959283090834842200, -3.239245055717051791, 12.12982544407804220 ) ) ;
#17852=CARTESIAN_POINT ( 'NONE',  ( 0.4862570985993235340, -7.559321496869506163, 11.67702470553362559 ) ) ;
#17856=CARTESIAN_POINT ( 'NONE',  ( 1.847168016377980670, 11.77471791462004802, -4.022276579849838996 ) ) ;
#17864=VECTOR ( 'NONE', #3901, 1000.000000000000000 ) ;
#17880=CARTESIAN_POINT ( 'NONE',  ( 0.8740764193765260259, 3.609949042658226581, 13.83508774435983035 ) ) ;
#17882=CARTESIAN_POINT ( 'NONE',  ( 3.950837973638676281, -14.41405733518059229, -1.958075594453940971 ) ) ;
#17885=CARTESIAN_POINT ( 'NONE',  ( 0.8740779401508858015, -11.05257166392043722, 9.070947476926702890 ) ) ;
#17886=ORIENTED_EDGE ( 'NONE', *, *, #14180, .F. ) ;
#17890=FACE_OUTER_BOUND ( 'NONE', #1253, .T. ) ;
#17891=CARTESIAN_POINT ( 'NONE',  ( 8.438534575730034959, -6.454982381540305347, 2.341351102130253103 ) ) ;
#17897=CARTESIAN_POINT ( 'NONE',  ( 1.847380140988742925, 3.740232970470921625, -11.86779270755354432 ) ) ;
#17902=EDGE_CURVE ( 'NONE', #11651, #10942, #14960, .T. ) ;
#17904=CARTESIAN_POINT ( 'NONE',  ( 1.847380140988738262, -10.00162556679656234, 7.402792205949069171 ) ) ;
#17910=ORIENTED_EDGE ( 'NONE', *, *, #17597, .T. ) ;
#17914=CARTESIAN_POINT ( 'NONE',  ( 0.3058872367615226295, -13.24582953854928036, 3.664492643742712108 ) ) ;
#17915=ADVANCED_FACE ( 'NONE', ( #7613 ), #8398, .T. ) ;
#17917=ORIENTED_EDGE ( 'NONE', *, *, #16190, .F. ) ;
#17919=AXIS2_PLACEMENT_3D ( 'NONE', #9273, #15378, #860 ) ;
#17925=CARTESIAN_POINT ( 'NONE',  ( 0.3148213771069381384, -13.73693585713733611, -0.2297580318216151940 ) ) ;
#17927=CARTESIAN_POINT ( 'NONE',  ( 0.3137051932979792457, -8.442169467526928983, 10.83767969834800127 ) ) ;
#17934=EDGE_CURVE ( 'NONE', #15231, #2734, #10392, .T. ) ;
#17936=CARTESIAN_POINT ( 'NONE',  ( 0.3132635586635982294, 3.740017578711948953, -13.21855946425832684 ) ) ;
#17941=CARTESIAN_POINT ( 'NONE',  ( 1.847380140988742703, -11.86779270755355853, -3.740232970470879881 ) ) ;
#17942=ORIENTED_EDGE ( 'NONE', *, *, #1120, .F. ) ;
#17946=ORIENTED_EDGE ( 'NONE', *, *, #6158, .F. ) ;
#17947=CARTESIAN_POINT ( 'NONE',  ( 0.3137051932979792457, -7.698472063774386420, -11.37800749014139612 ) ) ;
#17953=ORIENTED_EDGE ( 'NONE', *, *, #18690, .F. ) ;
#17954=CARTESIAN_POINT ( 'NONE',  ( 1.846138399168762101, -12.43476674860266229, -0.4167076046096845898 ) ) ;
#17955=CARTESIAN_POINT ( 'NONE',  ( 1.847034903785822690, -11.90269060117936739, 3.625649561595261083 ) ) ;
#17960=CARTESIAN_POINT ( 'NONE',  ( 0.3720661004400040439, -11.58636699658209679, -7.524064345033593781 ) ) ;
#17961=VECTOR ( 'NONE', #12281, 1000.000000000000000 ) ;
#17962=ORIENTED_EDGE ( 'NONE', *, *, #9134, .F. ) ;
#17967=CARTESIAN_POINT ( 'NONE',  ( 1.847461586945729595, -7.341074796295863791, -10.04711372545053116 ) ) ;
#17974=CARTESIAN_POINT ( 'NONE',  ( 0.3132642857406563452, -0.5276792104583234444, 13.72733058964894326 ) ) ;
#17983=VERTEX_POINT ( 'NONE', #1666 ) ;
#17984=CARTESIAN_POINT ( 'NONE',  ( 0.3307726912345234083, 11.46720933246398388, 7.596084275798933305 ) ) ;
#17985=ADVANCED_FACE ( 'NONE', ( #11900 ), #16300, .T. ) ;
#17987=EDGE_CURVE ( 'NONE', #18610, #16059, #11313, .T. ) ;
#17989=CARTESIAN_POINT ( 'NONE',  ( 16.56679352167444819, 0.009190982326619719436, 0.001390132774594471984 ) ) ;
#17993=CARTESIAN_POINT ( 'NONE',  ( 2.747332970342022840, -16.17136872824897154, -2.409922051470850146 ) ) ;
#17997=VECTOR ( 'NONE', #7006, 1000.000000000000114 ) ;
#18000=DIRECTION ( 'NONE',  ( -1.000000000000000000, -0.000000000000000000, -0.000000000000000000 ) ) ;
#18001=CARTESIAN_POINT ( 'NONE',  ( 2.705023505549863039, -12.36217802824809020, 4.909285963184022883 ) ) ;
#18010=EDGE_CURVE ( 'NONE', #5801, #4529, #18378, .T. ) ;
#18016=DIRECTION ( 'NONE',  ( -0.7561779333270775005, 0.6322161072786942615, 0.1688126975276577901 ) ) ;
#18019=CARTESIAN_POINT ( 'NONE',  ( 2.747332970342022840, 14.63517873738956965, -7.289199830146954717 ) ) ;
#18021=CARTESIAN_POINT ( 'NONE',  ( 1.847426409206450959, 1.966388007708274189E-11, -12.44303504652081038 ) ) ;
#18026=CARTESIAN_POINT ( 'NONE',  ( 0.3095370825347224519, 13.20347358821919670, -3.806662003783277459 ) ) ;
#18028=ORIENTED_EDGE ( 'NONE', *, *, #16193, .F. ) ;
#18030=EDGE_CURVE ( 'NONE', #4049, #5922, #15047, .T. ) ;
#18031=EDGE_CURVE ( 'NONE', #13922, #18593, #18177, .T. ) ;
#18038=CARTESIAN_POINT ( 'NONE',  ( 2.705023505549865703, 11.23800170568056878, 7.115606223895208693 ) ) ;
#18041=CARTESIAN_POINT ( 'NONE',  ( 16.57605080000000086, 0.000000000000000000, 0.000000000000000000 ) ) ;
#18042=CARTESIAN_POINT ( 'NONE',  ( 0.4862570985993235340, -11.67702470553370553, 7.559321496869385371 ) ) ;
#18043=CARTESIAN_POINT ( 'NONE',  ( 2.123976203522053741, 11.67822624909940821, -10.37815841598478883 ) ) ;
#18045=CARTESIAN_POINT ( 'NONE',  ( 2.320520222538102306, -7.743191299716920106, -13.71278186123380927 ) ) ;
#18047=CARTESIAN_POINT ( 'NONE',  ( 0.4754618798421162973, -11.68486377711960955, -7.564402563418597403 ) ) ;
#18048=ORIENTED_EDGE ( 'NONE', *, *, #962, .T. ) ;
#18050=ORIENTED_EDGE ( 'NONE', *, *, #6993, .F. ) ;
#18052=ORIENTED_EDGE ( 'NONE', *, *, #332, .T. ) ;
#18053=LINE ( 'NONE', #281, #10134 ) ;
#18058=CARTESIAN_POINT ( 'NONE',  ( 16.56679352167444819, 0.009170718284672562878, -0.001518074900131760043 ) ) ;
#18065=B_SPLINE_CURVE_WITH_KNOTS ( 'NONE', 3,
 ( #6274, #6176, #4743, #4552, #13238, #7063 ),
 .UNSPECIFIED., .F., .F.,
 ( 4, 2, 4 ),
 ( 0.000000000000000000, 0.001657017934710632240, 0.003314035869421264480 ),
 .UNSPECIFIED. ) ;
#18069=B_SPLINE_CURVE_WITH_KNOTS ( 'NONE', 3,
 ( #11758, #11662, #4392, #10417, #9175, #14615 ),
 .UNSPECIFIED., .F., .F.,
 ( 4, 2, 4 ),
 ( 3.303099811781675862E-17, 0.0001825746017570575581, 0.0003651492035140820481 ),
 .UNSPECIFIED. ) ;
#18072=FACE_OUTER_BOUND ( 'NONE', #4355, .T. ) ;
#18074=CARTESIAN_POINT ( 'NONE',  ( 0.3939822652208138098, 12.90851734139308071, 4.930560016699109482 ) ) ;
#18079=CARTESIAN_POINT ( 'NONE',  ( 2.636624412714763555, 6.973567714907159321, 14.46769361191226722 ) ) ;
#18082=ORIENTED_EDGE ( 'NONE', *, *, #6993, .T. ) ;
#18083=CARTESIAN_POINT ( 'NONE',  ( 1.846138399168762101, 3.446241763653166590, -11.95493567637846866 ) ) ;
#18084=CARTESIAN_POINT ( 'NONE',  ( 0.3145729642390356351, 13.73540280162741034, -0.3065092323351694126 ) ) ;
#18089=CARTESIAN_POINT ( 'NONE',  ( 1.959212340397961327, 12.53706137681889743, 0.6675998551412224424 ) ) ;
#18093=CARTESIAN_POINT ( 'NONE',  ( 3.950837973638675393, -2.591948120961912849, 14.31366178983252446 ) ) ;
#18096=CARTESIAN_POINT ( 'NONE',  ( 3.950837973638668288, 0.000000000000000000, 0.000000000000000000 ) ) ;
#18098=ORIENTED_EDGE ( 'NONE', *, *, #15650, .F. ) ;
#18099=VERTEX_POINT ( 'NONE', #8794 ) ;
#18102=CARTESIAN_POINT ( 'NONE',  ( 16.56822296793089322, -0.002414375228568911048, -0.009847136207495301580 ) ) ;
#18105=CARTESIAN_POINT ( 'NONE',  ( 0.3137051932979792457, -13.73004976592202375, 0.4596302728639276580 ) ) ;
#18106=CARTESIAN_POINT ( 'NONE',  ( 0.3137051932979792457, 11.37800749014142276, -7.698472063774345564 ) ) ;
#18107=CARTESIAN_POINT ( 'NONE',  ( 1.342453679581834924, 13.74702459364891993, -5.476372339889874041 ) ) ;
#18113=CARTESIAN_POINT ( 'NONE',  ( 2.636624412714236865, 0.000000000000000000, 0.000000000000000000 ) ) ;
#18115=CARTESIAN_POINT ( 'NONE',  ( 2.353870697619111496, -8.216087327473003299, 10.00946331859660710 ) ) ;
#18116=CARTESIAN_POINT ( 'NONE',  ( 0.8740764193766143997, 13.31469591265758545, 5.211550415968988936 ) ) ;
#18118=ORIENTED_EDGE ( 'NONE', *, *, #7259, .T. ) ;
#18119=VECTOR ( 'NONE', #3674, 1000.000000000000000 ) ;
#18120=ORIENTED_EDGE ( 'NONE', *, *, #17902, .F. ) ;
#18121=EDGE_LOOP ( 'NONE', ( #8161, #4613, #9815, #13567 ) ) ;
#18123=( BOUNDED_SURFACE ( )  B_SPLINE_SURFACE ( 3, 1, ( 
 ( #920, #18775 ),
 ( #6762, #12571 ),
 ( #8556, #18399 ),
 ( #6949, #3973 ) ),
 .UNSPECIFIED., .F., .F., .T. ) 
 B_SPLINE_SURFACE_WITH_KNOTS ( ( 4, 4 ),
 ( 2, 2 ),
 ( 0.000000000000000000, 1.000000000000000000 ),
 ( 0.000000000000000000, 1.000000000000000000 ),
 .UNSPECIFIED. ) 
 GEOMETRIC_REPRESENTATION_ITEM ( )  RATIONAL_B_SPLINE_SURFACE ( (
 ( 1.000000000000000000, 1.000000000000000000),
 ( 0.7792777138730160313, 0.9689936506012927220),
 ( 0.7792777138730160313, 0.9689936506012927220),
 ( 1.000000000000000000, 1.000000000000000000) ) ) 
 REPRESENTATION_ITEM ( '' )  SURFACE ( )  );
#18139=B_SPLINE_CURVE_WITH_KNOTS ( 'NONE', 3,
 ( #8345, #2489, #8428, #18287, #10682, #18373, #1166, #13637, #6640, #6814, #2585, #7004, #14160 ),
 .UNSPECIFIED., .F., .F.,
 ( 4, 3, 3, 3, 4 ),
 ( 2.602085213965210642E-18, 0.0002299780670421064713, 0.0004599561239687913672, 0.0006896788984287877382, 0.0009194956271626401716 ),
 .UNSPECIFIED. ) ;
#18140=EDGE_LOOP ( 'NONE', ( #7069, #10450, #5845, #11258, #4387, #8983 ) ) ;
#18143=CARTESIAN_POINT ( 'NONE',  ( 2.320521194584406199, 14.32454473830047270, -6.542541239687196253 ) ) ;
#18146=CARTESIAN_POINT ( 'NONE',  ( 1.977436885027552549, 15.04044112860454518, -3.321781585407754811 ) ) ;
#18147=CARTESIAN_POINT ( 'NONE',  ( 16.56872352241294521, 0.009207754980063749192, 0.004907101719994666836 ) ) ;
#18148=B_SPLINE_CURVE_WITH_KNOTS ( 'NONE', 3,
 ( #17954, #9520, #3404, #10969, #5217, #13819 ),
 .UNSPECIFIED., .F., .F.,
 ( 4, 2, 4 ),
 ( 2.168404344971008868E-19, 0.0001828790815886944003, 0.0003657581631773885837 ),
 .UNSPECIFIED. ) ;
#18151=CARTESIAN_POINT ( 'NONE',  ( 16.58200780006414732, 0.0006320991582349651770, -0.01115192838421568376 ) ) ;
#18152=CARTESIAN_POINT ( 'NONE',  ( 8.522092701127531811, -5.841710761610102942, -3.777034505568587885 ) ) ;
#18158=( BOUNDED_SURFACE ( )  B_SPLINE_SURFACE ( 3, 1, ( 
 ( #8897, #2859 ),
 ( #18739, #8807 ),
 ( #17214, #15969 ),
 ( #5638, #4130 ) ),
 .UNSPECIFIED., .F., .F., .T. ) 
 B_SPLINE_SURFACE_WITH_KNOTS ( ( 4, 4 ),
 ( 2, 2 ),
 ( 0.000000000000000000, 1.000000000000000000 ),
 ( 0.000000000000000000, 1.000000000000000000 ),
 .UNSPECIFIED. ) 
 GEOMETRIC_REPRESENTATION_ITEM ( )  RATIONAL_B_SPLINE_SURFACE ( (
 ( 1.000000000000000000, 1.000000000000000000),
 ( 0.9593108457356467333, 0.9995965569486454649),
 ( 0.9593108457356467333, 0.9995965569486454649),
 ( 1.000000000000000000, 1.000000000000000000) ) ) 
 REPRESENTATION_ITEM ( '' )  SURFACE ( )  );
#18161=EDGE_CURVE ( 'NONE', #10527, #12010, #16327, .T. ) ;
#18163=CARTESIAN_POINT ( 'NONE',  ( 3.950837973638675393, 6.888253895133479965, -12.81214529934967672 ) ) ;
#18166=AXIS2_PLACEMENT_3D ( 'NONE', #8502, #17282, #8233 ) ;
#18173=CARTESIAN_POINT ( 'NONE',  ( 1.254255976357671720, -9.426444230097072108, 11.25336128106933664 ) ) ;
#18177=CIRCLE ( 'NONE', #13279, 14.54644660717763927 ) ;
#18189=FACE_OUTER_BOUND ( 'NONE', #10009, .T. ) ;
#18190=EDGE_LOOP ( 'NONE', ( #1203, #11843, #10180, #17547 ) ) ;
#18203=CARTESIAN_POINT ( 'NONE',  ( 1.846138399168762101, 10.30487220521580305, -6.971848976710897539 ) ) ;
#18204=LINE ( 'NONE', #13894, #5713 ) ;
#18208=CARTESIAN_POINT ( 'NONE',  ( 0.3307726912345229087, -13.25328329128663007, -3.680742887039447631 ) ) ;
#18221=AXIS2_PLACEMENT_3D ( 'NONE', #6321, #13678, #13850 ) ;
#18224=CARTESIAN_POINT ( 'NONE',  ( 2.636624412715137922, -7.605649742761668719, 14.14563173255331741 ) ) ;
#18227=CARTESIAN_POINT ( 'NONE',  ( 0.4754618798421171855, -3.583352865732766901, 13.45049478164058598 ) ) ;
#18232=( BOUNDED_SURFACE ( )  B_SPLINE_SURFACE ( 3, 1, ( 
 ( #17716, #11503 ),
 ( #4416, #8815 ),
 ( #17613, #17321 ),
 ( #14451, #4616 ) ),
 .UNSPECIFIED., .F., .F., .T. ) 
 B_SPLINE_SURFACE_WITH_KNOTS ( ( 4, 4 ),
 ( 2, 2 ),
 ( 0.000000000000000000, 1.000000000000000000 ),
 ( 0.000000000000000000, 1.000000000000000000 ),
 .UNSPECIFIED. ) 
 GEOMETRIC_REPRESENTATION_ITEM ( )  RATIONAL_B_SPLINE_SURFACE ( (
 ( 1.000000000000000000, 1.000000000000000000),
 ( 0.9933953342250436691, 0.8357391271907733676),
 ( 0.9933953342250436691, 0.8357391271907733676),
 ( 1.000000000000000000, 1.000000000000000000) ) ) 
 REPRESENTATION_ITEM ( '' )  SURFACE ( )  );
#18234=ORIENTED_EDGE ( 'NONE', *, *, #16867, .T. ) ;
#18236=CARTESIAN_POINT ( 'NONE',  ( 0.3720661004400037664, -13.79610186261029270, -0.7231997263366251039 ) ) ;
#18240=EDGE_CURVE ( 'NONE', #10527, #12474, #10619, .T. ) ;
#18244=CARTESIAN_POINT ( 'NONE',  ( 3.950837973638668288, 0.000000000000000000, 0.000000000000000000 ) ) ;
#18245=ORIENTED_EDGE ( 'NONE', *, *, #801, .F. ) ;
#18246=CARTESIAN_POINT ( 'NONE',  ( 16.56753206892534891, -0.001421777558676013808, 0.009389754735542241854 ) ) ;
#18248=B_SPLINE_CURVE_WITH_KNOTS ( 'NONE', 3,
 ( #2282, #944, #6599, #12423, #5337, #12073 ),
 .UNSPECIFIED., .F., .F.,
 ( 4, 2, 4 ),
 ( 0.000000000000000000, 0.001656992708823338926, 0.003313985417646677853 ),
 .UNSPECIFIED. ) ;
#18256=PLANE ( 'NONE',  #17919 ) ;
#18258=CARTESIAN_POINT ( 'NONE',  ( 0.4384471787762814765, 4.978024343489044767, 12.93784327393174571 ) ) ;
#18259=VECTOR ( 'NONE', #15935, 1000.000000000000114 ) ;
#18269=( BOUNDED_SURFACE ( )  B_SPLINE_SURFACE ( 3, 1, ( 
 ( #6683, #16805 ),
 ( #2272, #18326 ),
 ( #18058, #5323 ),
 ( #15277, #9628 ) ),
 .UNSPECIFIED., .F., .F., .T. ) 
 B_SPLINE_SURFACE_WITH_KNOTS ( ( 4, 4 ),
 ( 2, 2 ),
 ( 0.000000000000000000, 1.000000000000000000 ),
 ( 0.000000000000000000, 1.000000000000000000 ),
 .UNSPECIFIED. ) 
 GEOMETRIC_REPRESENTATION_ITEM ( )  RATIONAL_B_SPLINE_SURFACE ( (
 ( 1.000000000000000000, 1.000000000000000000),
 ( 0.9593108457356467333, 0.9995965569486454649),
 ( 0.9593108457356467333, 0.9995965569486454649),
 ( 1.000000000000000000, 1.000000000000000000) ) ) 
 REPRESENTATION_ITEM ( '' )  SURFACE ( )  );
#18270=DIRECTION ( 'NONE',  ( -1.000000000000000000, -0.000000000000000000, -0.000000000000000000 ) ) ;
#18273=CARTESIAN_POINT ( 'NONE',  ( 2.320521194584054037, 7.743190876765937425, -13.71278319228217946 ) ) ;
#18275=CARTESIAN_POINT ( 'NONE',  ( 0.3058872367615230181, -0.6080468242579999405, -13.72992299905060776 ) ) ;
#18277=CARTESIAN_POINT ( 'NONE',  ( 0.4754618798421171855, -5.007009103465158262, -12.98792082933649716 ) ) ;
#18278=B_SPLINE_CURVE_WITH_KNOTS ( 'NONE', 3,
 ( #15743, #15934, #17177, #15841, #14121, #15558 ),
 .UNSPECIFIED., .F., .F.,
 ( 4, 2, 4 ),
 ( 4.005364051932256883E-17, 0.0002014099069817290285, 0.0004028198139634179956 ),
 .UNSPECIFIED. ) ;
#18287=CARTESIAN_POINT ( 'NONE',  ( 0.3148213771069390265, 4.026433757158980775, 13.13560149728601978 ) ) ;
#18288=CARTESIAN_POINT ( 'NONE',  ( 16.57778382496167424, 0.01482878558584695486, -0.001819584982831739346 ) ) ;
#18290=CARTESIAN_POINT ( 'NONE',  ( 0.4754618798421162973, -11.68486377711971969, 7.564402563418428649 ) ) ;
#18297=CARTESIAN_POINT ( 'NONE',  ( 0.3137051932979775248, -12.91601973349273891, 4.679953077377436266 ) ) ;
#18302=VECTOR ( 'NONE', #3008, 1000.000000000000114 ) ;
#18303=ORIENTED_EDGE ( 'NONE', *, *, #14386, .T. ) ;
#18306=VERTEX_POINT ( 'NONE', #17587 ) ;
#18310=CARTESIAN_POINT ( 'NONE',  ( 1.918921323896323639, -3.258415356426438869, -12.08297777410668417 ) ) ;
#18313=CARTESIAN_POINT ( 'NONE',  ( 2.747332970342022840, 11.66639548242823921, -11.45495994260705075 ) ) ;
#18316=CARTESIAN_POINT ( 'NONE',  ( 16.56679352167444819, 0.001390132774595458174, 0.009190982326619367287 ) ) ;
#18317=CARTESIAN_POINT ( 'NONE',  ( 16.56822296793089322, 0.002414375228568836022, 0.009847136207495320662 ) ) ;
#18321=VERTEX_POINT ( 'NONE', #9174 ) ;
#18326=CARTESIAN_POINT ( 'NONE',  ( 0.3170788640506441158, -13.74111462631963576, 0.1533108587035682813 ) ) ;
#18330=CARTESIAN_POINT ( 'NONE',  ( 1.918918678667072886, 0.6348738215465219437, 12.49849921341423453 ) ) ;
#18331=B_SPLINE_CURVE_WITH_KNOTS ( 'NONE', 3,
 ( #16427, #7439, #13540, #9151, #267, #14974, #17667, #13355, #1896, #13448, #7731, #11829, #16225 ),
 .UNSPECIFIED., .F., .F.,
 ( 4, 3, 3, 3, 4 ),
 ( 3.127317220692750759E-18, 0.0002299780670421087210, 0.0004599561239687931019, 0.0006896788984287912077, 0.0009194956271626412558 ),
 .UNSPECIFIED. ) ;
#18338=EDGE_CURVE ( 'NONE', #8143, #8310, #1686, .T. ) ;
#18339=CARTESIAN_POINT ( 'NONE',  ( 2.353870697619111496, 12.53036919722789477, -3.268530966681500782 ) ) ;
#18342=B_SPLINE_CURVE_WITH_KNOTS ( 'NONE', 3,
 ( #362, #9152, #1695, #17856, #1598, #11733, #6189, #16227, #5994, #8956, #14782, #463, #7442 ),
 .UNSPECIFIED., .F., .F.,
 ( 4, 3, 3, 3, 4 ),
 ( 1.734723475976806902E-18, 0.0002299804304191488261, 0.0004599608082120263644, 0.0006467586077648019086, 0.0008336169836826000249 ),
 .UNSPECIFIED. ) ;
#18351=ORIENTED_EDGE ( 'NONE', *, *, #17099, .F. ) ;
#18357=B_SPLINE_CURVE_WITH_KNOTS ( 'NONE', 3,
 ( #593, #4974, #494, #18163 ),
 .UNSPECIFIED., .F., .F.,
 ( 4, 4 ),
 ( 4.589925559575316169E-16, 0.002004993803842821786 ),
 .UNSPECIFIED. ) ;
#18363=DIRECTION ( 'NONE',  ( -1.000000000000000000, -0.000000000000000000, -0.000000000000000000 ) ) ;
#18366=CARTESIAN_POINT ( 'NONE',  ( 0.4384471787762829753, 8.732395932355681012, 10.76632603192789617 ) ) ;
#18373=CARTESIAN_POINT ( 'NONE',  ( 0.3151930723728439410, 4.172946285306569969, 13.09040889075571990 ) ) ;
#18378=B_SPLINE_CURVE_WITH_KNOTS ( 'NONE', 3,
 ( #16494, #9219, #538, #18445 ),
 .UNSPECIFIED., .F., .F.,
 ( 4, 4 ),
 ( 0.000000000000000000, 0.002004993803842688646 ),
 .UNSPECIFIED. ) ;
#18379=CARTESIAN_POINT ( 'NONE',  ( 3.074695600507272086, 15.41438262616223298, -2.093687500612007923 ) ) ;
#18388=EDGE_LOOP ( 'NONE', ( #14575, #9854, #10228, #34 ) ) ;
#18389=ORIENTED_EDGE ( 'NONE', *, *, #15651, .F. ) ;
#18392=ORIENTED_EDGE ( 'NONE', *, *, #2443, .F. ) ;
#18398=CARTESIAN_POINT ( 'NONE',  ( 0.3095370825347224519, 13.73357284481724783, -0.4597470195090672673 ) ) ;
#18399=CARTESIAN_POINT ( 'NONE',  ( 2.123976203522053297, -6.261444813538658671, 14.31368049382967556 ) ) ;
#18402=FACE_OUTER_BOUND ( 'NONE', #7219, .T. ) ;
#18404=CIRCLE ( 'NONE', #426, 14.54644660717763927 ) ;
#18412=CARTESIAN_POINT ( 'NONE',  ( 3.664313757352976264, 1.627055439596472475, -14.16986885736090329 ) ) ;
#18413=CARTESIAN_POINT ( 'NONE',  ( 1.847168016377985333, -7.161712042621529939, 10.17509564929255994 ) ) ;
#18414=ORIENTED_EDGE ( 'NONE', *, *, #13374, .F. ) ;
#18415=CARTESIAN_POINT ( 'NONE',  ( 0.3058872367615226295, 8.562166468153870724, -10.75034008168906396 ) ) ;
#18417=ADVANCED_FACE ( 'NONE', ( #940 ), #7676, .F. ) ;
#18418=FACE_OUTER_BOUND ( 'NONE', #13812, .T. ) ;
#18426=CARTESIAN_POINT ( 'NONE',  ( 2.123976203522053741, -10.37815841598482969, -11.67822624909937090 ) ) ;
#18436=CARTESIAN_POINT ( 'NONE',  ( 8.438534575730034959, 6.454982381540319558, -2.341351102130211359 ) ) ;
#18444=( BOUNDED_SURFACE ( )  B_SPLINE_SURFACE ( 3, 1, ( 
 ( #16637, #10623 ),
 ( #9179, #769 ),
 ( #3439, #9550 ),
 ( #3539, #4787 ) ),
 .UNSPECIFIED., .F., .F., .T. ) 
 B_SPLINE_SURFACE_WITH_KNOTS ( ( 4, 4 ),
 ( 2, 2 ),
 ( 0.000000000000000000, 1.000000000000000000 ),
 ( 0.000000000000000000, 1.000000000000000000 ),
 .UNSPECIFIED. ) 
 GEOMETRIC_REPRESENTATION_ITEM ( )  RATIONAL_B_SPLINE_SURFACE ( (
 ( 1.000000000000000000, 1.000000000000000000),
 ( 0.9593108457356467333, 0.9995965569486454649),
 ( 0.9593108457356467333, 0.9995965569486454649),
 ( 1.000000000000000000, 1.000000000000000000) ) ) 
 REPRESENTATION_ITEM ( '' )  SURFACE ( )  );
#18445=CARTESIAN_POINT ( 'NONE',  ( 2.636624412714756005, -2.161493821597335607, 15.91454522070219113 ) ) ;
#18446=( NAMED_UNIT ( * ) PLANE_ANGLE_UNIT ( ) SI_UNIT ( $, .RADIAN. ) );
#18448=CIRCLE ( 'NONE', #11142, 14.54644660717763927 ) ;
#18450=CARTESIAN_POINT ( 'NONE',  ( 2.123976203522053297, 3.347755036805901252, 15.26039569100260884 ) ) ;
#18453=CARTESIAN_POINT ( 'NONE',  ( 0.4862570985993235340, 11.67702470553376060, -7.559321496869298329 ) ) ;
#18455=ORIENTED_EDGE ( 'NONE', *, *, #11319, .F. ) ;
#18458=FACE_OUTER_BOUND ( 'NONE', #11002, .T. ) ;
#18460=ORIENTED_EDGE ( 'NONE', *, *, #18778, .F. ) ;
#18462=VECTOR ( 'NONE', #7631, 999.9999999999998863 ) ;
#18468=CARTESIAN_POINT ( 'NONE',  ( 0.3145734862173242274, -11.29227530924451273, 7.825584895511488170 ) ) ;
#18472=CARTESIAN_POINT ( 'NONE',  ( 3.950837973638668288, 0.000000000000000000, 0.000000000000000000 ) ) ;
#18473=LINE ( 'NONE', #5554, #4209 ) ;
#18477=CARTESIAN_POINT ( 'NONE',  ( 1.846613052777651198, -4.166957398589769213, -11.72395935470502870 ) ) ;
#18478=DIRECTION ( 'NONE',  ( -1.000000000000000000, -0.000000000000000000, -0.000000000000000000 ) ) ;
#18481=SURFACE_STYLE_USAGE ( .BOTH. , #12929 ) ;
#18482=ORIENTED_EDGE ( 'NONE', *, *, #16255, .F. ) ;
#18484=B_SPLINE_CURVE_WITH_KNOTS ( 'NONE', 3,
 ( #5400, #13815, #2343, #12296, #8278, #7920 ),
 .UNSPECIFIED., .F., .F.,
 ( 4, 2, 4 ),
 ( 1.748223473168675632E-18, 0.0002017457492448079337, 0.0004034914984896141327 ),
 .UNSPECIFIED. ) ;
#18491=CARTESIAN_POINT ( 'NONE',  ( 3.664313757352971823, 7.012524439851495650, 12.42002390572628201 ) ) ;
#18499=VECTOR ( 'NONE', #9215, 1000.000000000000114 ) ;
#18501=ORIENTED_EDGE ( 'NONE', *, *, #4521, .T. ) ;
#18507=CARTESIAN_POINT ( 'NONE',  ( 3.950837973638675393, 6.888253895133292559, 12.81214529934977797 ) ) ;
#18509=CARTESIAN_POINT ( 'NONE',  ( 16.57778382496167424, 0.01306626476309289374, -0.007244066302946823403 ) ) ;
#18510=ORIENTED_EDGE ( 'NONE', *, *, #3804, .T. ) ;
#18511=CARTESIAN_POINT ( 'NONE',  ( 1.847247051441594179, 9.967131402978196775, 7.448813758297206711 ) ) ;
#18518=DIRECTION ( 'NONE',  ( -1.000000000000000000, -0.000000000000000000, -0.000000000000000000 ) ) ;
#18522=B_SPLINE_CURVE_WITH_KNOTS ( 'NONE', 3,
 ( #18297, #14957, #814, #634, #12100, #5114 ),
 .UNSPECIFIED., .F., .F.,
 ( 4, 2, 4 ),
 ( 3.490137563248181679E-18, 0.0002017457492448096685, 0.0004034914984896158133 ),
 .UNSPECIFIED. ) ;
#18525=ORIENTED_EDGE ( 'NONE', *, *, #11571, .F. ) ;
#18532=CARTESIAN_POINT ( 'NONE',  ( 16.56753206892534891, 0.006669401563385194548, 0.006760771273035138390 ) ) ;
#18533=ORIENTED_EDGE ( 'NONE', *, *, #14431, .T. ) ;
#18534=CARTESIAN_POINT ( 'NONE',  ( 0.4862570985993235340, -13.44146924561383827, 3.580942890621619412 ) ) ;
#18541=CARTESIAN_POINT ( 'NONE',  ( 1.846524061778019199, 12.43723828841088341, 0.3544704288992919228 ) ) ;
#18542=DIRECTION ( 'NONE',  ( -1.000000000000000000, -0.000000000000000000, -0.000000000000000000 ) ) ;
#18543=CARTESIAN_POINT ( 'NONE',  ( 1.847461586945732703, 11.84459954310610463, 3.813310247068479431 ) ) ;
#18547=CARTESIAN_POINT ( 'NONE',  ( 0.4862570985993235340, -0.7479633556563419772, 13.89016912371017121 ) ) ;
#18548=CARTESIAN_POINT ( 'NONE',  ( 16.58200780006414732, -0.007066318000005944282, 0.008650561019685880718 ) ) ;
#18550=CARTESIAN_POINT ( 'NONE',  ( 0.3939822652208109788, 0.7002900021919884477, -13.80035637018651684 ) ) ;
#18552=EDGE_CURVE ( 'NONE', #12155, #16968, #3752, .T. ) ;
#18556=CARTESIAN_POINT ( 'NONE',  ( 1.846138399168762101, 10.30487220521580305, -6.971848976710897539 ) ) ;
#18558=CARTESIAN_POINT ( 'NONE',  ( 0.3132642857406540138, -4.743831191224475496, 12.89240536501344536 ) ) ;
#18559=CARTESIAN_POINT ( 'NONE',  ( 16.56872352241294521, 0.007512283835805451566, 0.007240717549634016065 ) ) ;
#18563=ORIENTED_EDGE ( 'NONE', *, *, #15715, .F. ) ;
#18566=CARTESIAN_POINT ( 'NONE',  ( 1.918921323896324749, 7.860085869556325378, -9.738309537478915701 ) ) ;
#18567=CARTESIAN_POINT ( 'NONE',  ( 1.845755665166725068, -0.4784952423729416648, 12.43231320373360838 ) ) ;
#18569=CARTESIAN_POINT ( 'NONE',  ( 1.847034903785823134, -3.625649561595226888, -11.90269060117937627 ) ) ;
#18574=CARTESIAN_POINT ( 'NONE',  ( 0.3095370825347233956, -3.806662003783505277, 13.20347358821913275 ) ) ;
#18576=EDGE_LOOP ( 'NONE', ( #2219, #1839, #8734, #1541 ) ) ;
#18584=CARTESIAN_POINT ( 'NONE',  ( 16.57778382496167424, -0.01354073047775762942, -0.006312874906843820091 ) ) ;
#18585=CIRCLE ( 'NONE', #5174, 16.06066017081991149 ) ;
#18593=VERTEX_POINT ( 'NONE', #9729 ) ;
#18598=CARTESIAN_POINT ( 'NONE',  ( 2.002547531651519996, -11.75462648437105173, 4.532360870844282630 ) ) ;
#18600=CARTESIAN_POINT ( 'NONE',  ( 1.847380140988742925, -7.224522571381399416, 10.13114603776194045 ) ) ;
#18603=CARTESIAN_POINT ( 'NONE',  ( 1.846138399168762101, -4.238866729160323032, -11.69739621335926394 ) ) ;
#18605=LINE ( 'NONE', #11448, #3334 ) ;
#18610=VERTEX_POINT ( 'NONE', #2453 ) ;
#18617=DIRECTION ( 'NONE',  ( -1.000000000000000000, -0.000000000000000000, -0.000000000000000000 ) ) ;
#18624=CARTESIAN_POINT ( 'NONE',  ( 1.846138399168762989, -3.446241763653083101, 11.95493567637849530 ) ) ;
#18629=EDGE_CURVE ( 'NONE', #7718, #8099, #18773, .T. ) ;
#18634=ADVANCED_FACE ( 'NONE', ( #12689 ), #14210, .T. ) ;
#18636=CARTESIAN_POINT ( 'NONE',  ( 2.747332970342022840, 2.705255688517843371, 16.12459247543627683 ) ) ;
#18639=B_SPLINE_CURVE_WITH_KNOTS ( 'NONE', 3,
 ( #16149, #5714, #5812, #4109, #15760, #11753 ),
 .UNSPECIFIED., .F., .F.,
 ( 4, 2, 4 ),
 ( 4.336808689942017736E-19, 0.0001828790815886937498, 0.0003657581631773870658 ),
 .UNSPECIFIED. ) ;
#18640=EDGE_CURVE ( 'NONE', #11305, #11392, #7878, .T. ) ;
#18641=CARTESIAN_POINT ( 'NONE',  ( 3.377929128793396352, -12.02809354424095822, -7.136734442940969814 ) ) ;
#18644=CARTESIAN_POINT ( 'NONE',  ( 0.3148213771069364175, 0.2297580318216631001, -13.73693585713733967 ) ) ;
#18649=DIRECTION ( 'NONE',  ( 0.000000000000000000, 0.000000000000000000, 1.000000000000000000 ) ) ;
#18654=EDGE_CURVE ( 'NONE', #12518, #12767, #11455, .T. ) ;
#18656=CARTESIAN_POINT ( 'NONE',  ( 0.3939875929385652231, -10.75308190953749410, 8.678227324501083473 ) ) ;
#18661=CARTESIAN_POINT ( 'NONE',  ( 1.918918678667046684, -7.860057224348774518, -9.738328798462466906 ) ) ;
#18665=ORIENTED_EDGE ( 'NONE', *, *, #18629, .F. ) ;
#18666=CARTESIAN_POINT ( 'NONE',  ( 0.3151928479966097374, 1.775918418904422640E-15, 13.73922861026898623 ) ) ;
#18669=CARTESIAN_POINT ( 'NONE',  ( 1.846138399168762989, 3.446241763652997836, 11.95493567637851839 ) ) ;
#18670=CARTESIAN_POINT ( 'NONE',  ( 0.3151926232592466293, 13.04305446098362253, -4.318679262939488339 ) ) ;
#18672=DIRECTION ( 'NONE',  ( -0.7635533937278216055, -0.6204116510013465424, -0.1790966170213987851 ) ) ;
#18675=CARTESIAN_POINT ( 'NONE',  ( 2.636624412717099908, 11.60464335004051861, -11.10302021258208249 ) ) ;
#18676=B_SPLINE_CURVE_WITH_KNOTS ( 'NONE', 3,
 ( #13396, #15019, #3256, #6142, #9101, #11874 ),
 .UNSPECIFIED., .F., .F.,
 ( 4, 2, 4 ),
 ( 0.000000000000000000, 0.001656992708823057468, 0.003313985417646114935 ),
 .UNSPECIFIED. ) ;
#18677=VECTOR ( 'NONE', #3471, 1000.000000000000000 ) ;
#18678=CARTESIAN_POINT ( 'NONE',  ( 2.002547531651519996, 6.845637710436190737, 10.57595306287294612 ) ) ;
#18679=DIRECTION ( 'NONE',  ( 1.000000000000000000, -0.000000000000000000, -0.000000000000000000 ) ) ;
#18687=CARTESIAN_POINT ( 'NONE',  ( 3.950837973638676281, 1.958075594453990487, -14.41405733518058341 ) ) ;
#18688=EDGE_LOOP ( 'NONE', ( #3372, #887, #13571, #11912 ) ) ;
#18690=EDGE_CURVE ( 'NONE', #3191, #11533, #1510, .T. ) ;
#18691=EDGE_CURVE ( 'NONE', #9212, #7718, #18342, .T. ) ;
#18692=DIRECTION ( 'NONE',  ( 0.000000000000000000, 0.000000000000000000, 1.000000000000000000 ) ) ;
#18697=DIRECTION ( 'NONE',  ( 0.000000000000000000, 0.000000000000000000, 1.000000000000000000 ) ) ;
#18698=CARTESIAN_POINT ( 'NONE',  ( 1.845755665166725290, -10.33920510797148395, 6.920419570228313333 ) ) ;
#18699=CARTESIAN_POINT ( 'NONE',  ( 16.56753206892534891, 0.008490833999798002782, -0.004253784598196794220 ) ) ;
#18700=DIRECTION ( 'NONE',  ( -1.000000000000000000, -0.000000000000000000, -0.000000000000000000 ) ) ;
#18702=ORIENTED_EDGE ( 'NONE', *, *, #12213, .T. ) ;
#18704=CARTESIAN_POINT ( 'NONE',  ( 0.3095370825347234511, 3.806662003783410242, 13.20347358821915940 ) ) ;
#18706=CARTESIAN_POINT ( 'NONE',  ( 16.57210152137263393, 0.01214401161737623663, 0.008007331252333469568 ) ) ;
#18714=CARTESIAN_POINT ( 'NONE',  ( 16.58200780006414732, 0.01041078477704048856, 0.004047297414159084679 ) ) ;
#18728=CARTESIAN_POINT ( 'NONE',  ( 1.847412631396503357, 7.348689888531986014, -10.04119192206678512 ) ) ;
#18732=ADVANCED_FACE ( 'NONE', ( #16026 ), #3199, .T. ) ;
#18736=CARTESIAN_POINT ( 'NONE',  ( 16.56753206892534891, -0.001549402974394229436, -0.009369540855502527313 ) ) ;
#18739=CARTESIAN_POINT ( 'NONE',  ( 16.56679352167444819, -0.008252760440870528930, -0.004277682826582232013 ) ) ;
#18740=CARTESIAN_POINT ( 'NONE',  ( 1.846822687350014869, -9.891732594446525084, -7.547953575784235092 ) ) ;
#18742=DIRECTION ( 'NONE',  ( 0.000000000000000000, 0.000000000000000000, 1.000000000000000000 ) ) ;
#18743=CARTESIAN_POINT ( 'NONE',  ( 3.950837973638677170, 6.316429227969654114, -13.10350451991833687 ) ) ;
#18747=DIRECTION ( 'NONE',  ( 0.000000000000000000, 0.000000000000000000, 1.000000000000000000 ) ) ;
#18749=EDGE_CURVE ( 'NONE', #9990, #8563, #8764, .T. ) ;
#18752=CARTESIAN_POINT ( 'NONE',  ( 16.56753206892534891, 0.001549402974393146101, -0.009369540855502138735 ) ) ;
#18755=ORIENTED_EDGE ( 'NONE', *, *, #8602, .F. ) ;
#18757=CARTESIAN_POINT ( 'NONE',  ( 16.56782317627811096, -0.0003415813796015412622, -0.009814734722106366327 ) ) ;
#18766=CARTESIAN_POINT ( 'NONE',  ( 0.3151928479966097929, -0.07658992383253612757, 13.73922861026898623 ) ) ;
#18773=B_SPLINE_CURVE_WITH_KNOTS ( 'NONE', 3,
 ( #14119, #1025, #1408, #8666, #4282, #7252 ),
 .UNSPECIFIED., .F., .F.,
 ( 4, 2, 4 ),
 ( 8.673617379884035472E-19, 0.0001828790815886931534, 0.0003657581631773854395 ),
 .UNSPECIFIED. ) ;
#18775=CARTESIAN_POINT ( 'NONE',  ( 0.4754618798421167414, -5.007009103465340338, 12.98792082933642966 ) ) ;
#18777=CARTESIAN_POINT ( 'NONE',  ( 16.56753206892534891, -0.009369540855502522109, 0.001549402974394263697 ) ) ;
#18778=EDGE_CURVE ( 'NONE', #11575, #4533, #17427, .T. ) ;
#18783=ORIENTED_EDGE ( 'NONE', *, *, #11937, .F. ) ;
#18785=ORIENTED_EDGE ( 'NONE', *, *, #3867, .F. ) ;
#18788=CARTESIAN_POINT ( 'NONE',  ( 16.56679352167444819, -0.004162264567719712108, -0.008311568981097318051 ) ) ;
#18796=CARTESIAN_POINT ( 'NONE',  ( 1.847168016377985333, 4.022276579849959788, 11.77471791462000184 ) ) ;
#18797=B_SPLINE_CURVE_WITH_KNOTS ( 'NONE', 3,
 ( #12122, #8953, #10690, #14780, #16523, #11922 ),
 .UNSPECIFIED., .F., .F.,
 ( 4, 2, 4 ),
 ( 2.438852479171459636E-18, 0.001657017934711444091, 0.003314035869422886013 ),
 .UNSPECIFIED. ) ;
#18804=ADVANCED_FACE ( 'NONE', ( #15072 ), #12294, .F. ) ;
#18808=ORIENTED_EDGE ( 'NONE', *, *, #10540, .F. ) ;
#18810=CARTESIAN_POINT ( 'NONE',  ( 2.002547531651519996, 3.242439124566649511, 12.17374746633579541 ) ) ;
#18821=CARTESIAN_POINT ( 'NONE',  ( 1.847380140988740926, 11.86779270755359050, 3.740232970470796392 ) ) ;
#18827=CARTESIAN_POINT ( 'NONE',  ( 8.522092701127531811, 4.388629235579655230, -5.397361180353095200 ) ) ;
#18829=DIRECTION ( 'NONE',  ( 0.000000000000000000, 0.000000000000000000, -1.000000000000000000 ) ) ;
#18831=ORIENTED_EDGE ( 'NONE', *, *, #849, .T. ) ;
#18834=ADVANCED_FACE ( 'NONE', ( #9613 ), #2501, .F. ) ;
#18837=( BOUNDED_SURFACE ( )  B_SPLINE_SURFACE ( 3, 1, ( 
 ( #5344, #11094 ),
 ( #11189, #17182 ),
 ( #9552, #17097 ),
 ( #4001, #2203 ) ),
 .UNSPECIFIED., .F., .F., .T. ) 
 B_SPLINE_SURFACE_WITH_KNOTS ( ( 4, 4 ),
 ( 2, 2 ),
 ( 0.000000000000000000, 1.000000000000000000 ),
 ( 0.000000000000000000, 1.000000000000000000 ),
 .UNSPECIFIED. ) 
 GEOMETRIC_REPRESENTATION_ITEM ( )  RATIONAL_B_SPLINE_SURFACE ( (
 ( 1.000000000000000000, 1.000000000000000000),
 ( 0.7792777138730158093, 0.9689936506012928330),
 ( 0.7792777138730158093, 0.9689936506012928330),
 ( 1.000000000000000000, 1.000000000000000000) ) ) 
 REPRESENTATION_ITEM ( '' )  SURFACE ( )  );
#18842=CARTESIAN_POINT ( 'NONE',  ( 16.56679352167444819, 0.001390132774594440108, -0.009190982326619726375 ) ) ;
#18843=CARTESIAN_POINT ( 'NONE',  ( 0.3145734862173260038, -4.535879238195024143, 12.96846406299304988 ) ) ;
#18849=DIRECTION ( 'NONE',  ( -1.000000000000000000, -0.000000000000000000, -0.000000000000000000 ) ) ;
#18855=FACE_OUTER_BOUND ( 'NONE', #3981, .T. ) ;
#18859=CARTESIAN_POINT ( 'NONE',  ( 2.123976203522053741, -11.67822624909933005, 10.37815841598487765 ) ) ;
#18860=EDGE_CURVE ( 'NONE', #7279, #1703, #11951, .T. ) ;
#18866=CARTESIAN_POINT ( 'NONE',  ( 1.846138399168762101, 9.815003036200520725, -7.646096044339786069 ) ) ;
#18873=CARTESIAN_POINT ( 'NONE',  ( 1.562796894703937678, 0.000000000000000000, 0.000000000000000000 ) ) ;
#18877=B_SPLINE_CURVE_WITH_KNOTS ( 'NONE', 3,
 ( #3202, #2087, #18038, #16603 ),
 .UNSPECIFIED., .F., .F.,
 ( 4, 4 ),
 ( 1.140836248210248932E-17, 0.003005512676784841391 ),
 .UNSPECIFIED. ) ;
#18880=VERTEX_POINT ( 'NONE', #16702 ) ;
#18882=FACE_OUTER_BOUND ( 'NONE', #18190, .T. ) ;
#18884=ORIENTED_EDGE ( 'NONE', *, *, #12237, .F. ) ;
#18888=CARTESIAN_POINT ( 'NONE',  ( 0.4862570985993235340, -7.559321496869339185, -11.67702470553373750 ) ) ;
#18893=CARTESIAN_POINT ( 'NONE',  ( 1.254009781011619529, -3.563484327698362542, 14.24044713813325558 ) ) ;
#18894=CARTESIAN_POINT ( 'NONE',  ( 3.950837973638668288, 0.000000000000000000, 0.000000000000000000 ) ) ;
#18901=EDGE_LOOP ( 'NONE', ( #10935, #18783, #11865, #5393 ) ) ;
ENDSEC;
END-ISO-10303-21;
